ISO-10303-21;
HEADER;
FILE_DESCRIPTION (('STEP AP214'),
    '1' );
FILE_NAME ('Nipple.step',
    '2026-10-22T18:53:08',
    ( '' ),
    ( '' ),
    'SwSTEP 2.0',
    'SolidWorks 2025',
    '' );
FILE_SCHEMA (( 'AUTOMOTIVE_DESIGN' ));
ENDSEC;

DATA;
#10=CARTESIAN_POINT ( 'NONE',  ( -5.365059087798939252, -7.384370330707086261, -9.933165578109189653 ) ) ;
#24=CARTESIAN_POINT ( 'NONE',  ( 2.935661446562616295, -9.035036904803758873, -7.659589141758144315 ) ) ;
#35=CARTESIAN_POINT ( 'NONE',  ( -6.021009868636381950E-13, 9.295211988927752245, 2.702983250845903740 ) ) ;
#39=CARTESIAN_POINT ( 'NONE',  ( 8.680847955710813579, 2.820578480814259326, 4.733165578109188587 ) ) ;
#50=FACE_OUTER_BOUND ( 'NONE', #14923, .T. ) ;
#58=CARTESIAN_POINT ( 'NONE',  ( 9.500000000000209610, -3.086737114211962396, 11.10674201446023446 ) ) ;
#60=DIRECTION ( 'NONE',  ( -0.000000000000000000, -0.000000000000000000, -1.000000000000000000 ) ) ;
#69=EDGE_CURVE ( 'NONE', #19085, #18693, #18803, .T. ) ;
#71=CARTESIAN_POINT ( 'NONE',  ( -8.680847955711007202, -5.923547351154968927E-13, 7.633165578109188942 ) ) ;
#72=ORIENTED_EDGE ( 'NONE', *, *, #21290, .F. ) ;
#80=CARTESIAN_POINT ( 'NONE',  ( 7.022953521755574080, -5.102474405759714671, -8.433165578109187877 ) ) ;
#92=CARTESIAN_POINT ( 'NONE',  ( 9.500000000000000000, 1.163414459189985485E-15, 11.99999999999999645 ) ) ;
#93=CARTESIAN_POINT ( 'NONE',  ( -6.822232771736904647E-13, 9.988891130263535700, -8.559589141758142006 ) ) ;
#100=CARTESIAN_POINT ( 'NONE',  ( 2.682529543900284974, -8.255977015246234174, -12.23316557810919036 ) ) ;
#105=VERTEX_POINT ( 'NONE', #507 ) ;
#112=DIRECTION ( 'NONE',  ( -0.000000000000000000, -0.000000000000000000, -1.000000000000000000 ) ) ;
#131=B_SPLINE_CURVE_WITH_KNOTS ( 'NONE', 3,
 ( #17555, #9865, #6107, #23059, #11576, #21099, #8039, #15483, #7911, #6478, #12055, #17073, #5983, #17321 ),
 .UNSPECIFIED., .F., .F.,
 ( 4, 2, 2, 2, 2, 2, 4 ),
 ( 6.929308356866153103E-16, 0.001553140985941692384, 0.002329711478912192824, 0.003106281971882693047, 0.004659422957823693492, 0.005435993450794191981, 0.006212563943764690469 ),
 .UNSPECIFIED. ) ;
#132=VECTOR ( 'NONE', #9378, 999.9999999999998863 ) ;
#133=CARTESIAN_POINT ( 'NONE',  ( 7.685661446562381371, -5.583959896777971110, -9.859589141758144493 ) ) ;
#144=CARTESIAN_POINT ( 'NONE',  ( -9.500000000000000000, -6.482511860946779655E-13, -5.059589141758143782 ) ) ;
#150=ORIENTED_EDGE ( 'NONE', *, *, #12548, .T. ) ;
#166=EDGE_CURVE ( 'NONE', #9633, #17850, #16710, .T. ) ;
#170=ORIENTED_EDGE ( 'NONE', *, *, #21885, .F. ) ;
#182=ORIENTED_EDGE ( 'NONE', *, *, #11342, .T. ) ;
#191=DIRECTION ( 'NONE',  ( -0.000000000000000000, -0.000000000000000000, -1.000000000000000000 ) ) ;
#193=CARTESIAN_POINT ( 'NONE',  ( 0.000000000000000000, 0.000000000000000000, 12.50000000000000000 ) ) ;
#195=ORIENTED_EDGE ( 'NONE', *, *, #4432, .F. ) ;
#198=CARTESIAN_POINT ( 'NONE',  ( 6.809999908187194197E-13, -9.988891130263535700, 11.55958914175814201 ) ) ;
#199=EDGE_LOOP ( 'NONE', ( #820, #16806, #2871, #170, #5990, #4363, #16078, #14680, #17872, #2627, #23157, #1528, #15276, #9674 ) ) ;
#206=CARTESIAN_POINT ( 'NONE',  ( -2.682529543899159208, -8.255977015246598327, -12.03316557810918930 ) ) ;
#214=DIRECTION ( 'NONE',  ( -0.000000000000000000, -0.000000000000000000, -1.000000000000000000 ) ) ;
#215=AXIS2_PLACEMENT_3D ( 'NONE', #19096, #13347, #6619 ) ;
#240=CARTESIAN_POINT ( 'NONE',  ( -2.935661446562617183, 9.035036904803758873, -5.806742014460233747 ) ) ;
#244=B_SPLINE_CURVE_WITH_KNOTS ( 'NONE', 3,
 ( #16018, #23954, #6888, #18227 ),
 .UNSPECIFIED., .F., .F.,
 ( 4, 4 ),
 ( 0.000000000000000000, 0.8197781486845410193 ),
 .UNSPECIFIED. ) ;
#272=CARTESIAN_POINT ( 'NONE',  ( 2.935661446561383503, 9.035036904804158553, -6.459589141758144137 ) ) ;
#274=CARTESIAN_POINT ( 'NONE',  ( -2.935661446562617183, 9.035036904803758873, 11.80674201446023375 ) ) ;
#283=CARTESIAN_POINT ( 'NONE',  ( 2.935661446561383503, 9.035036904804158553, -7.606742014460233570 ) ) ;
#315=CARTESIAN_POINT ( 'NONE',  ( 8.680847955711007202, 5.912916378492122225E-13, 4.633165578109188942 ) ) ;
#317=EDGE_CURVE ( 'NONE', #105, #19051, #18113, .T. ) ;
#322=CARTESIAN_POINT ( 'NONE',  ( 8.680847955711199049, -2.820578480813074496, -10.53316557810918752 ) ) ;
#330=ORIENTED_EDGE ( 'NONE', *, *, #3431, .F. ) ;
#332=DIRECTION ( 'NONE',  ( -0.000000000000000000, -0.000000000000000000, -1.000000000000000000 ) ) ;
#340=CARTESIAN_POINT ( 'NONE',  ( -9.500000000000211386, 3.086737114211961064, 4.106742014460232681 ) ) ;
#343=ADVANCED_FACE ( 'NONE', ( #587, #10447 ), #18147, .F. ) ;
#345=UNCERTAINTY_MEASURE_WITH_UNIT (LENGTH_MEASURE( 1.000000000000000082E-05 ), #9120, 'distance_accuracy_value', 'NONE');
#360=ORIENTED_EDGE ( 'NONE', *, *, #21024, .F. ) ;
#361=CARTESIAN_POINT ( 'NONE',  ( -8.680847955711007202, -5.923547351154968927E-13, -7.633165578109188942 ) ) ;
#368=ORIENTED_EDGE ( 'NONE', *, *, #10861, .T. ) ;
#377=CARTESIAN_POINT ( 'NONE',  ( -6.153822176767817416E-13, 9.500000000000000000, -3.500000000000014211 ) ) ;
#394=CYLINDRICAL_SURFACE ( 'NONE', #10525, 9.500000000000000000 ) ;
#395=CARTESIAN_POINT ( 'NONE',  ( 2.682529543899157876, 8.255977015246598327, 11.03316557810918752 ) ) ;
#402=ORIENTED_EDGE ( 'NONE', *, *, #23393, .T. ) ;
#406=CARTESIAN_POINT ( 'NONE',  ( 2.935661446562616295, -9.035036904803758873, -12.80674201446023375 ) ) ;
#412=CARTESIAN_POINT ( 'NONE',  ( -7.648716207067147721, -5.640964897112045406, -3.500655991556068880 ) ) ;
#425=CARTESIAN_POINT ( 'NONE',  ( 5.365059087799946447, -7.384370330706356178, 6.333165578109187344 ) ) ;
#444=ORIENTED_EDGE ( 'NONE', *, *, #13659, .T. ) ;
#454=ADVANCED_FACE ( 'NONE', ( #19970, #10794 ), #8856, .T. ) ;
#479=CARTESIAN_POINT ( 'NONE',  ( -7.022953521755574080, 5.102474405759713783, -7.433165578109188765 ) ) ;
#491=VECTOR ( 'NONE', #23328, 1000.000000000000000 ) ;
#495=CARTESIAN_POINT ( 'NONE',  ( 6.250000000000000000, -10.82531754730548279, 2.500000000000000000 ) ) ;
#496=( BOUNDED_CURVE ( )  B_SPLINE_CURVE ( 2, ( #21372, #6721, #21614, #6228, #11953, #10242, #19421, #13671, #4911, #750, #2697 ),
 .UNSPECIFIED., .F., .T. ) 
 B_SPLINE_CURVE_WITH_KNOTS ( ( 3, 2, 2, 2, 2, 3 ),
 ( 0.006042316813507608332, 0.01999999999999999001, 0.03999999999999997308, 0.05999999999999994921, 0.07999999999999993228, 0.09999999999999992228 ),
 .UNSPECIFIED. ) 
 CURVE ( )  GEOMETRIC_REPRESENTATION_ITEM ( )  RATIONAL_B_SPLINE_CURVE ( ( 0.9793613297716612376, 0.9658431180202251554, 1.000000000000000000, 0.9510565162951535312, 1.000000000000000000, 0.9510565162951535312, 1.000000000000000000, 0.9510565162951535312, 1.000000000000000000, 0.9510565162951537532, 0.9999999999999997780 ) ) 
 REPRESENTATION_ITEM ( '' )  );
#497=CARTESIAN_POINT ( 'NONE',  ( -2.935661446561384391, -9.035036904804158553, -3.459589141758144137 ) ) ;
#507=CARTESIAN_POINT ( 'NONE',  ( -7.561939491010498671, 5.750397476200742375, -11.99999999999999822 ) ) ;
#509=CARTESIAN_POINT ( 'NONE',  ( -9.500000000000000000, -6.482511860946779655E-13, -8.206742014460234103 ) ) ;
#512=CARTESIAN_POINT ( 'NONE',  ( -9.500000000000000000, -6.482511860946779655E-13, 4.206742014460233214 ) ) ;
#513=CARTESIAN_POINT ( 'NONE',  ( 7.685661446561619314, 5.583959896779020049, -5.406742014460233392 ) ) ;
#517=CARTESIAN_POINT ( 'NONE',  ( -8.680847955711007202, -5.923547351154968927E-13, 7.633165578109188942 ) ) ;
#528=CARTESIAN_POINT ( 'NONE',  ( 2.935661446561383503, 9.035036904804158553, -9.606742014460232681 ) ) ;
#534=CARTESIAN_POINT ( 'NONE',  ( -3.064960521623495637, -8.996099670591407360, -3.501175347612584421 ) ) ;
#547=EDGE_LOOP ( 'NONE', ( #14292, #13702, #6261, #2259 ) ) ;
#548=CARTESIAN_POINT ( 'NONE',  ( 2.682529543900284974, -8.255977015246234174, 6.233165578109188587 ) ) ;
#553=CARTESIAN_POINT ( 'NONE',  ( -2.935661446561384391, -9.035036904804158553, 5.459589141758144137 ) ) ;
#557=FACE_OUTER_BOUND ( 'NONE', #10768, .T. ) ;
#558=CARTESIAN_POINT ( 'NONE',  ( -8.680847955711200825, 2.820578480813073607, -3.533165578109187965 ) ) ;
#566=VERTEX_POINT ( 'NONE', #6593 ) ;
#577=CARTESIAN_POINT ( 'NONE',  ( 2.682529543900284974, -8.255977015246234174, -8.233165578109190363 ) ) ;
#582=CARTESIAN_POINT ( 'NONE',  ( -7.022953521755574080, 5.102474405759713783, 9.433165578109189653 ) ) ;
#587=FACE_BOUND ( 'NONE', #13497, .T. ) ;
#589=CARTESIAN_POINT ( 'NONE',  ( 5.871322893123449127, 8.081182679344781405, -10.35958914175814627 ) ) ;
#590=PRODUCT_DEFINITION_CONTEXT ( 'detailed design', #14437, 'design' ) ;
#594=CARTESIAN_POINT ( 'NONE',  ( 7.121611749575534667, -5.132745777193459702, 12.50000000000000533 ) ) ;
#597=ADVANCED_FACE ( 'NONE', ( #13913 ), #1452, .F. ) ;
#605=CARTESIAN_POINT ( 'NONE',  ( -6.249999999999999112, -10.82531754730548279, 2.500000000000000000 ) ) ;
#609=CARTESIAN_POINT ( 'NONE',  ( -9.500000000000000000, -6.482511860946779655E-13, 4.206742014460233214 ) ) ;
#610=CARTESIAN_POINT ( 'NONE',  ( 5.365059087799946447, -7.384370330706356178, -6.333165578109187344 ) ) ;
#613=FACE_OUTER_BOUND ( 'NONE', #4176, .T. ) ;
#644=CARTESIAN_POINT ( 'NONE',  ( -6.822232771736903637E-13, 9.988891130263535700, -7.706742014460232326 ) ) ;
#647=CARTESIAN_POINT ( 'NONE',  ( 7.022953521754877748, 5.102474405760673903, 6.833165578109188232 ) ) ;
#657=ORIENTED_EDGE ( 'NONE', *, *, #14862, .T. ) ;
#660=CARTESIAN_POINT ( 'NONE',  ( -9.499999999999790390, -3.086737114213257804, -10.30674201446023375 ) ) ;
#676=CARTESIAN_POINT ( 'NONE',  ( 2.935661446562616295, -9.035036904803758873, 7.659589141758144315 ) ) ;
#677=EDGE_CURVE ( 'NONE', #3993, #4215, #21013, .T. ) ;
#686=CARTESIAN_POINT ( 'NONE',  ( -6.233975306307046963E-13, 9.127583699786111282, -5.133165578109188054 ) ) ;
#697=CARTESIAN_POINT ( 'NONE',  ( -5.871322893123449127, -8.081182679344781405, -6.506742014460233925 ) ) ;
#701=CARTESIAN_POINT ( 'NONE',  ( -2.682529543900285862, 8.255977015246234174, -7.233165578109188587 ) ) ;
#707=CARTESIAN_POINT ( 'NONE',  ( -6.233975306307046963E-13, 9.127583699786111282, -11.13316557810918894 ) ) ;
#708=CARTESIAN_POINT ( 'NONE',  ( 8.680847955711007202, 5.912916378492122225E-13, 8.633165578109188942 ) ) ;
#718=CARTESIAN_POINT ( 'NONE',  ( 8.746907971560217376, -1.213523871515184149, 12.49999999999999289 ) ) ;
#730=CARTESIAN_POINT ( 'NONE',  ( 7.685661446562381371, -5.583959896777971110, -13.00674201446023304 ) ) ;
#733=CARTESIAN_POINT ( 'NONE',  ( 7.685661446562381371, -5.583959896777971110, 11.85958914175814449 ) ) ;
#734=CARTESIAN_POINT ( 'NONE',  ( -2.935661446561384391, -9.035036904804158553, 10.60674201446023446 ) ) ;
#744=AXIS2_PLACEMENT_3D ( 'NONE', #8652, #10377, #12195 ) ;
#745=CARTESIAN_POINT ( 'NONE',  ( 2.935661446562616295, -9.035036904803758873, -3.659589141758142983 ) ) ;
#750=CARTESIAN_POINT ( 'NONE',  ( -9.499999999999783284, -3.086737114213268018, 11.15958914175814698 ) ) ;
#757=CARTESIAN_POINT ( 'NONE',  ( 2.935661446561383503, 9.035036904804158553, 8.459589141758144137 ) ) ;
#759=CARTESIAN_POINT ( 'NONE',  ( -9.500000000000211386, 3.086737114211961064, -6.106742014460234458 ) ) ;
#763=CARTESIAN_POINT ( 'NONE',  ( -6.233975306307045953E-13, 9.127583699786111282, 11.13316557810918894 ) ) ;
#770=ORIENTED_EDGE ( 'NONE', *, *, #8119, .T. ) ;
#783=DIRECTION ( 'NONE',  ( -0.8191520442889927978, -5.579613378627572123E-14, -0.5735764363510448272 ) ) ;
#786=DIRECTION ( 'NONE',  ( -0.5000000000000002220, 0.8660254037844384856, 0.000000000000000000 ) ) ;
#787=EDGE_CURVE ( 'NONE', #11482, #5195, #15888, .T. ) ;
#790=CARTESIAN_POINT ( 'NONE',  ( 5.871322893123448239, 8.081182679344781405, -4.359589141758143604 ) ) ;
#793=CARTESIAN_POINT ( 'NONE',  ( 9.500000000000209610, -3.086737114211962396, 9.959589141758145914 ) ) ;
#801=CARTESIAN_POINT ( 'NONE',  ( 9.500000000000000000, 6.470877716354879437E-13, 7.206742014460234103 ) ) ;
#816=CARTESIAN_POINT ( 'NONE',  ( 5.365059087798939252, 7.384370330707087149, -4.933165578109186988 ) ) ;
#820=ORIENTED_EDGE ( 'NONE', *, *, #6931, .T. ) ;
#821=CARTESIAN_POINT ( 'NONE',  ( 6.222797240145152671E-13, -9.127583699786111282, 10.13316557810918894 ) ) ;
#828=CARTESIAN_POINT ( 'NONE',  ( 7.751944208201821063, -4.001916517787171834, 12.50000000000000711 ) ) ;
#836=CARTESIAN_POINT ( 'NONE',  ( 9.500000000000000000, 6.470877716354879437E-13, -9.206742014460234103 ) ) ;
#842=CARTESIAN_POINT ( 'NONE',  ( -9.500000000000211386, 3.086737114211961064, -12.10674201446023091 ) ) ;
#843=EDGE_CURVE ( 'NONE', #19427, #5371, #11846, .T. ) ;
#846=CARTESIAN_POINT ( 'NONE',  ( -9.500000000000000000, -6.482511860946779655E-13, 9.059589141758143782 ) ) ;
#859=CARTESIAN_POINT ( 'NONE',  ( -7.685661446562381371, 5.583959896777970222, -2.859589141758144493 ) ) ;
#862=ORIENTED_EDGE ( 'NONE', *, *, #3081, .F. ) ;
#874=CARTESIAN_POINT ( 'NONE',  ( 2.935661446561383503, 9.035036904804158553, -7.606742014460233570 ) ) ;
#878=CARTESIAN_POINT ( 'NONE',  ( 9.500000000000000000, 6.470877716354879437E-13, -6.059589141758143782 ) ) ;
#879=CARTESIAN_POINT ( 'NONE',  ( 8.680847955711199049, -2.820578480813074496, 10.53316557810918752 ) ) ;
#889=CARTESIAN_POINT ( 'NONE',  ( 2.935661446561383503, 9.035036904804158553, -11.60674201446023268 ) ) ;
#892=CARTESIAN_POINT ( 'NONE',  ( -5.614908434072717114, -7.307052314572652918, -12.29292215563023483 ) ) ;
#902=EDGE_CURVE ( 'NONE', #17696, #14019, #8899, .T. ) ;
#912=CARTESIAN_POINT ( 'NONE',  ( -7.685661446562381371, 5.583959896777970222, -4.859589141758143604 ) ) ;
#914=CARTESIAN_POINT ( 'NONE',  ( 9.499999999999790390, 3.086737114213260025, 10.15958914175814520 ) ) ;
#923=CARTESIAN_POINT ( 'NONE',  ( -8.680847955710813579, -2.820578480814258437, -3.733165578109188587 ) ) ;
#937=LINE ( 'NONE', #15814, #20706 ) ;
#943=CARTESIAN_POINT ( 'NONE',  ( 7.022953521755574080, -5.102474405759714671, -8.433165578109187877 ) ) ;
#949=CARTESIAN_POINT ( 'NONE',  ( -6.233975306307046963E-13, 9.127583699786111282, 9.133165578109188942 ) ) ;
#968=CARTESIAN_POINT ( 'NONE',  ( -6.153822176767817416E-13, 9.500000000000000000, -2.846377359933665030 ) ) ;
#975=CARTESIAN_POINT ( 'NONE',  ( 6.809999908187194197E-13, -9.988891130263535700, -12.70674201446023410 ) ) ;
#979=CARTESIAN_POINT ( 'NONE',  ( 6.809999908187194197E-13, -9.988891130263535700, 3.559589141758143338 ) ) ;
#988=EDGE_CURVE ( 'NONE', #8523, #18614, #3318, .T. ) ;
#1011=CARTESIAN_POINT ( 'NONE',  ( 8.680847955711007202, 5.912916378492122225E-13, 4.633165578109188942 ) ) ;
#1012=CARTESIAN_POINT ( 'NONE',  ( 0.000000000000000000, 0.000000000000000000, -12.50000000000000000 ) ) ;
#1017=CARTESIAN_POINT ( 'NONE',  ( 5.871322893124551356, -8.081182679343980269, 5.759589141758143960 ) ) ;
#1027=CARTESIAN_POINT ( 'NONE',  ( -9.499999999999790390, -3.086737114213257804, -11.15958914175814520 ) ) ;
#1032=ORIENTED_EDGE ( 'NONE', *, *, #12208, .F. ) ;
#1043=CARTESIAN_POINT ( 'NONE',  ( -6.250000000000000888, 10.82531754730548279, 2.500000000000000000 ) ) ;
#1047=CARTESIAN_POINT ( 'NONE',  ( -2.935661446562617183, 9.035036904803758873, 4.659589141758143427 ) ) ;
#1051=ORIENTED_EDGE ( 'NONE', *, *, #3127, .F. ) ;
#1055=CARTESIAN_POINT ( 'NONE',  ( 9.499999999999799272, 3.086737114213245370, 7.306742014460232859 ) ) ;
#1065=CARTESIAN_POINT ( 'NONE',  ( 2.935661446561383503, 9.035036904804158553, 5.606742014460233570 ) ) ;
#1067=CARTESIAN_POINT ( 'NONE',  ( -5.871322893124554021, 8.081182679343978492, 4.759589141758143960 ) ) ;
#1070=CARTESIAN_POINT ( 'NONE',  ( 2.682529543900284974, -8.255977015246234174, -10.23316557810918859 ) ) ;
#1079=CARTESIAN_POINT ( 'NONE',  ( -2.682529543899159208, -8.255977015246598327, 4.033165578109189298 ) ) ;
#1081=ORIENTED_EDGE ( 'NONE', *, *, #23581, .T. ) ;
#1083=CARTESIAN_POINT ( 'NONE',  ( 7.685661446561619314, 5.583959896779020049, -11.40674201446023517 ) ) ;
#1086=CARTESIAN_POINT ( 'NONE',  ( 5.871322893124553133, -8.081182679343980269, -11.75958914175814485 ) ) ;
#1089=CARTESIAN_POINT ( 'NONE',  ( -7.685661446562381371, 5.583959896777970222, 4.006742014460233925 ) ) ;
#1103=CARTESIAN_POINT ( 'NONE',  ( -9.499999999999790390, -3.086737114213257804, 7.159589141758144315 ) ) ;
#1105=CARTESIAN_POINT ( 'NONE',  ( -7.685661446561619314, -5.583959896779019161, 12.40674201446023339 ) ) ;
#1122=DIRECTION ( 'NONE',  ( -0.000000000000000000, -0.000000000000000000, -1.000000000000000000 ) ) ;
#1141=CARTESIAN_POINT ( 'NONE',  ( 2.935661446562616295, -9.035036904803758873, -11.65958914175814520 ) ) ;
#1155=( BOUNDED_CURVE ( )  B_SPLINE_CURVE ( 2, ( #3711, #7247, #12841, #7455, #3825, #9187, #11122, #16987, #5526, #11487, #5781 ),
 .UNSPECIFIED., .F., .T. ) 
 B_SPLINE_CURVE_WITH_KNOTS ( ( 3, 2, 2, 2, 2, 3 ),
 ( 0.3000000000000000999, 0.3200000000000001177, 0.3400000000000000799, 0.3600000000000000422, 0.3800000000000000044, 0.4000000000000000222 ),
 .UNSPECIFIED. ) 
 CURVE ( )  GEOMETRIC_REPRESENTATION_ITEM ( )  RATIONAL_B_SPLINE_CURVE ( ( 0.9999999999999997780, 0.9510565162951537532, 1.000000000000000000, 0.9510565162951535312, 1.000000000000000000, 0.9510565162951535312, 1.000000000000000000, 0.9510565162951535312, 1.000000000000000000, 0.9510565162951535312, 1.000000000000000000 ) ) 
 REPRESENTATION_ITEM ( '' )  );
#1159=DIRECTION ( 'NONE',  ( -1.000000000000000000, 0.000000000000000000, 0.000000000000000000 ) ) ;
#1163=CARTESIAN_POINT ( 'NONE',  ( -2.935661446562617183, 9.035036904803758873, 6.659589141758144315 ) ) ;
#1181=CARTESIAN_POINT ( 'NONE',  ( 5.871322893123448239, 8.081182679344781405, 4.359589141758143604 ) ) ;
#1197=CARTESIAN_POINT ( 'NONE',  ( 7.685661446562381371, -5.583959896777971110, -7.859589141758143604 ) ) ;
#1201=CARTESIAN_POINT ( 'NONE',  ( -6.153822176767817416E-13, 9.500000000000000000, 3.568914004820076702 ) ) ;
#1207=VERTEX_POINT ( 'NONE', #10711 ) ;
#1215=CARTESIAN_POINT ( 'NONE',  ( 9.500000000000000000, 6.470877716354879437E-13, -13.20674201446023410 ) ) ;
#1219=CARTESIAN_POINT ( 'NONE',  ( -7.685661446562381371, 5.583959896777970222, 2.859589141758144493 ) ) ;
#1220=CARTESIAN_POINT ( 'NONE',  ( -9.500000000000000000, -6.482511860946779655E-13, 10.20674201446023233 ) ) ;
#1226=CARTESIAN_POINT ( 'NONE',  ( 7.685661446562381371, -5.583959896777971110, -5.006742014460233037 ) ) ;
#1232=VECTOR ( 'NONE', #8932, 1000.000000000000000 ) ;
#1236=VECTOR ( 'NONE', #332, 1000.000000000000000 ) ;
#1238=DIRECTION ( 'NONE',  ( -1.000000000000000000, 0.000000000000000000, 0.000000000000000000 ) ) ;
#1243=CARTESIAN_POINT ( 'NONE',  ( 5.871322893123448239, 8.081182679344781405, -6.359589141758142716 ) ) ;
#1248=DIRECTION ( 'NONE',  ( -0.000000000000000000, -0.000000000000000000, -1.000000000000000000 ) ) ;
#1254=CARTESIAN_POINT ( 'NONE',  ( -5.871322893124554021, 8.081182679343978492, -5.906742014460233392 ) ) ;
#1257=CARTESIAN_POINT ( 'NONE',  ( -4.286858344475962035, -8.121112198674618199, -12.32511944772321044 ) ) ;
#1271=CARTESIAN_POINT ( 'NONE',  ( 7.685661446561619314, 5.583959896779020049, -9.406742014460235168 ) ) ;
#1275=ORIENTED_EDGE ( 'NONE', *, *, #17876, .T. ) ;
#1307=FACE_OUTER_BOUND ( 'NONE', #19962, .T. ) ;
#1310=CARTESIAN_POINT ( 'NONE',  ( -2.682529543899159208, -8.255977015246598327, 6.033165578109189298 ) ) ;
#1317=CARTESIAN_POINT ( 'NONE',  ( -9.499999999999790390, -3.086737114213257804, -9.159589141758145203 ) ) ;
#1319=CARTESIAN_POINT ( 'NONE',  ( -5.799656021750657521E-13, 8.953898637140671468, 3.324357723559535849 ) ) ;
#1323=FACE_OUTER_BOUND ( 'NONE', #23964, .T. ) ;
#1326=FACE_OUTER_BOUND ( 'NONE', #12184, .T. ) ;
#1340=CARTESIAN_POINT ( 'NONE',  ( -5.871322893124554021, 8.081182679343978492, -9.906742014460235168 ) ) ;
#1344=CARTESIAN_POINT ( 'NONE',  ( -2.935661446561384391, -9.035036904804158553, 12.60674201446023446 ) ) ;
#1345=CARTESIAN_POINT ( 'NONE',  ( -7.685661446561619314, -5.583959896779019161, 4.406742014460233392 ) ) ;
#1352=CARTESIAN_POINT ( 'NONE',  ( -5.871322893123449127, -8.081182679344781405, 3.359589141758143160 ) ) ;
#1367=VECTOR ( 'NONE', #191, 1000.000000000000000 ) ;
#1369=CARTESIAN_POINT ( 'NONE',  ( 8.680847955710813579, 2.820578480814259326, -8.733165578109185034 ) ) ;
#1372=VERTEX_POINT ( 'NONE', #23138 ) ;
#1381=CARTESIAN_POINT ( 'NONE',  ( -7.685661446561619314, -5.583959896779019161, -3.259589141758143516 ) ) ;
#1386=DIRECTION ( 'NONE',  ( 1.000000000000000000, 0.000000000000000000, 0.000000000000000000 ) ) ;
#1389=CARTESIAN_POINT ( 'NONE',  ( -7.685661446561619314, -5.583959896779019161, -6.406742014460233392 ) ) ;
#1391=CIRCLE ( 'NONE', #21637, 8.000000000000000000 ) ;
#1407=CARTESIAN_POINT ( 'NONE',  ( -9.499999999999790390, -3.086737114213257804, 3.159589141758143871 ) ) ;
#1437=CARTESIAN_POINT ( 'NONE',  ( -2.682529543899159208, -8.255977015246598327, -4.033165578109189298 ) ) ;
#1440=CARTESIAN_POINT ( 'NONE',  ( 2.682529543899157876, 8.255977015246598327, 9.033165578109187521 ) ) ;
#1450=CARTESIAN_POINT ( 'NONE',  ( 5.871322893124553133, -8.081182679343980269, -7.759589141758143072 ) ) ;
#1452=( BOUNDED_SURFACE ( )  B_SPLINE_SURFACE ( 1, 2, ( 
 ( #9852, #8268, #19403, #4763, #6331, #13654, #22943, #20985, #1105, #6099, #2563, #10095, #2926, #21355, #21091, #4391, #9976, #23185, #4274, #12046, #19518, #2797, #17435, #17679, #10353, #10218, #734, #8406, #23316, #17816, #1220, #23429, #6948, #14479, #10472, #20128, #19775, #5109, #8631, #1573, #16084, #12780, #12660, #3404, #10820, #10706, #18178, #18289, #8769, #8987, #3279, #14370, #22082, #1472, #16432, #17932, #21827, #15968, #14258, #23546, #12421, #7175, #5355, #21949, #8885, #6828, #21720, #16217, #23897, #19882, #14612, #23777, #12528, #5007, #7049, #6704, #20240, #12305, #16322, #3517, #3158, #5233, #10925, #18397, #8526, #20000, #3050, #14136, #1345, #10582, #4893, #340, #9459, #20350, #13882, #13997, #13625 ),
 ( #4731, #19010, #22914, #15562, #17644, #17520, #9819, #15319, #20959, #2651, #2284, #6299, #2530, #11775, #4243, #4617, #10185, #11905, #22789, #6071, #19251, #15824, #11652, #9702, #17413, #821, #19121, #12018, #13512, #23024, #17282, #19490, #582, #23288, #2765, #949, #8372, #21196, #4501, #6563, #708, #21441, #10067, #8117, #17155, #8232, #6191, #21065, #15687, #4361, #8602, #3023, #16051, #11113, #9288, #1751, #12833, #21565, #12274, #3128, #10550, #2896, #16733, #7237, #20291, #18463, #1310, #23516, #10443, #20406, #19743, #6797, #3697, #5520, #14226, #4981, #7343, #8498, #9179, #39, #21686, #8734, #10323, #12392, #15941, #16186, #1079, #23646, #14677, #18594, #14901, #22140, #5411, #3566, #16628, #22247, #17783 ) ),
 .UNSPECIFIED., .F., .F., .T. ) 
 B_SPLINE_SURFACE_WITH_KNOTS ( ( 2, 2 ),
 ( 3, 2, 2, 2, 2, 2, 2, 2, 2, 2, 2, 2, 2, 2, 2, 2, 2, 2, 2, 2, 2, 2, 2, 2, 2, 2, 2, 2, 2, 2, 2, 2, 2, 2, 2, 2, 2, 2, 2, 2, 2, 2, 2, 2, 2, 2, 2, 2, 3 ),
 ( 0.000000000000000000, 1.000000000000000000 ),
 ( 0.000000000000000000, 0.02000000000000000042, 0.04000000000000000083, 0.05999999999999999778, 0.08000000000000000167, 0.1000000000000000056, 0.1199999999999999956, 0.1400000000000000133, 0.1600000000000000033, 0.1799999999999999933, 0.2000000000000000111, 0.2200000000000000011, 0.2399999999999999911, 0.2600000000000000089, 0.2800000000000000266, 0.2999999999999999889, 0.3200000000000000067, 0.3400000000000000244, 0.3599999999999999867, 0.3800000000000000044, 0.4000000000000000222, 0.4199999999999999845, 0.4400000000000000022, 0.4600000000000000200, 0.4799999999999999822, 0.5000000000000000000, 0.5200000000000000178, 0.5400000000000000355, 0.5600000000000000533, 0.5799999999999999600, 0.5999999999999999778, 0.6199999999999999956, 0.6400000000000000133, 0.6600000000000000311, 0.6800000000000000488, 0.6999999999999999556, 0.7199999999999999734, 0.7399999999999999911, 0.7600000000000000089, 0.7800000000000000266, 0.8000000000000000444, 0.8199999999999999512, 0.8399999999999999689, 0.8599999999999999867, 0.8800000000000000044, 0.9000000000000000222, 0.9200000000000000400, 0.9399999999999999467, 0.9500000000000000666 ),
 .UNSPECIFIED. ) 
 GEOMETRIC_REPRESENTATION_ITEM ( )  RATIONAL_B_SPLINE_SURFACE ( (
 ( 1.000000000000000000, 0.9510565162951535312, 1.000000000000000000, 0.9510565162951535312, 1.000000000000000000, 0.9510565162951535312, 1.000000000000000000, 0.9510565162951535312, 1.000000000000000000, 0.9510565162951535312, 1.000000000000000000, 0.9510565162951535312, 1.000000000000000000, 0.9510565162951535312, 1.000000000000000000, 0.9510565162951535312, 1.000000000000000000, 0.9510565162951535312, 1.000000000000000000, 0.9510565162951535312, 1.000000000000000000, 0.9510565162951535312, 1.000000000000000000, 0.9510565162951535312, 1.000000000000000000, 0.9510565162951535312, 1.000000000000000000, 0.9510565162951535312, 1.000000000000000000, 0.9510565162951535312, 1.000000000000000000, 0.9510565162951535312, 1.000000000000000000, 0.9510565162951535312, 1.000000000000000000, 0.9510565162951535312, 1.000000000000000000, 0.9510565162951535312, 1.000000000000000000, 0.9510565162951535312, 1.000000000000000000, 0.9510565162951535312, 1.000000000000000000, 0.9510565162951535312, 1.000000000000000000, 0.9510565162951535312, 1.000000000000000000, 0.9510565162951535312, 1.000000000000000000, 0.9510565162951535312, 1.000000000000000000, 0.9510565162951535312, 1.000000000000000000, 0.9510565162951535312, 1.000000000000000000, 0.9510565162951535312, 1.000000000000000000, 0.9510565162951535312, 1.000000000000000000, 0.9510565162951535312, 1.000000000000000000, 0.9510565162951535312, 1.000000000000000000, 0.9510565162951535312, 1.000000000000000000, 0.9510565162951535312, 1.000000000000000000, 0.9510565162951535312, 1.000000000000000000, 0.9510565162951535312, 1.000000000000000000, 0.9510565162951535312, 1.000000000000000000, 0.9510565162951535312, 1.000000000000000000, 0.9510565162951535312, 1.000000000000000000, 0.9510565162951535312, 1.000000000000000000, 0.9510565162951535312, 1.000000000000000000, 0.9510565162951535312, 1.000000000000000000, 0.9510565162951535312, 1.000000000000000000, 0.9510565162951535312, 1.000000000000000000, 0.9510565162951535312, 1.000000000000000000, 0.9510565162951535312, 1.000000000000000000, 0.9510565162951535312, 1.000000000000000000, 0.9510565162951535312, 1.000000000000000000, 0.9755282581475764880, 0.9755282581475768211),
 ( 1.000000000000000000, 0.9510565162951535312, 1.000000000000000000, 0.9510565162951535312, 1.000000000000000000, 0.9510565162951535312, 1.000000000000000000, 0.9510565162951535312, 1.000000000000000000, 0.9510565162951535312, 1.000000000000000000, 0.9510565162951535312, 1.000000000000000000, 0.9510565162951535312, 1.000000000000000000, 0.9510565162951535312, 1.000000000000000000, 0.9510565162951535312, 1.000000000000000000, 0.9510565162951535312, 1.000000000000000000, 0.9510565162951535312, 1.000000000000000000, 0.9510565162951535312, 1.000000000000000000, 0.9510565162951535312, 1.000000000000000000, 0.9510565162951535312, 1.000000000000000000, 0.9510565162951535312, 1.000000000000000000, 0.9510565162951535312, 1.000000000000000000, 0.9510565162951535312, 1.000000000000000000, 0.9510565162951535312, 1.000000000000000000, 0.9510565162951535312, 1.000000000000000000, 0.9510565162951535312, 1.000000000000000000, 0.9510565162951535312, 1.000000000000000000, 0.9510565162951535312, 1.000000000000000000, 0.9510565162951535312, 1.000000000000000000, 0.9510565162951535312, 1.000000000000000000, 0.9510565162951535312, 1.000000000000000000, 0.9510565162951535312, 1.000000000000000000, 0.9510565162951535312, 1.000000000000000000, 0.9510565162951535312, 1.000000000000000000, 0.9510565162951535312, 1.000000000000000000, 0.9510565162951535312, 1.000000000000000000, 0.9510565162951535312, 1.000000000000000000, 0.9510565162951535312, 1.000000000000000000, 0.9510565162951535312, 1.000000000000000000, 0.9510565162951535312, 1.000000000000000000, 0.9510565162951535312, 1.000000000000000000, 0.9510565162951535312, 1.000000000000000000, 0.9510565162951535312, 1.000000000000000000, 0.9510565162951535312, 1.000000000000000000, 0.9510565162951535312, 1.000000000000000000, 0.9510565162951535312, 1.000000000000000000, 0.9510565162951535312, 1.000000000000000000, 0.9510565162951535312, 1.000000000000000000, 0.9510565162951535312, 1.000000000000000000, 0.9510565162951535312, 1.000000000000000000, 0.9510565162951535312, 1.000000000000000000, 0.9510565162951535312, 1.000000000000000000, 0.9510565162951535312, 1.000000000000000000, 0.9755282581475764880, 0.9755282581475768211) ) ) 
 REPRESENTATION_ITEM ( '' )  SURFACE ( )  );
#1471=CARTESIAN_POINT ( 'NONE',  ( -2.935661446561384391, -9.035036904804158553, 10.60674201446023446 ) ) ;
#1472=CARTESIAN_POINT ( 'NONE',  ( -5.871322893124554021, 8.081182679343978492, 7.906742014460233392 ) ) ;
#1479=CARTESIAN_POINT ( 'NONE',  ( -9.500000000000211386, 3.086737114211961064, 2.959589141758143249 ) ) ;
#1486=DIRECTION ( 'NONE',  ( -1.000000000000000000, 0.000000000000000000, 0.000000000000000000 ) ) ;
#1488=CARTESIAN_POINT ( 'NONE',  ( -3.053836969424609471, 9.001008217452133309, -3.499964733571762299 ) ) ;
#1492=CARTESIAN_POINT ( 'NONE',  ( -5.365059087799947335, 7.384370330706355290, -9.333165578109190008 ) ) ;
#1497=CARTESIAN_POINT ( 'NONE',  ( 7.022953521755574080, -5.102474405759714671, 4.433165578109187877 ) ) ;
#1500=CARTESIAN_POINT ( 'NONE',  ( -2.935661446562617183, 9.035036904803758873, -2.659589141758143871 ) ) ;
#1506=CARTESIAN_POINT ( 'NONE',  ( 6.809999908187194197E-13, -9.988891130263535700, -11.55958914175814201 ) ) ;
#1508=CARTESIAN_POINT ( 'NONE',  ( -6.153822176767817416E-13, 9.500000000000000000, -3.637828009640159621 ) ) ;
#1510=EDGE_CURVE ( 'NONE', #22463, #3733, #23458, .T. ) ;
#1512=ORIENTED_EDGE ( 'NONE', *, *, #21726, .F. ) ;
#1522=ORIENTED_EDGE ( 'NONE', *, *, #21971, .T. ) ;
#1528=ORIENTED_EDGE ( 'NONE', *, *, #15175, .T. ) ;
#1533=CARTESIAN_POINT ( 'NONE',  ( -9.500000000000000000, -6.482511860946779655E-13, 6.206742014460234103 ) ) ;
#1541=DIRECTION ( 'NONE',  ( -1.000000000000000000, 0.000000000000000000, 0.000000000000000000 ) ) ;
#1545=CARTESIAN_POINT ( 'NONE',  ( -6.233975306307046963E-13, 9.127583699786111282, 9.133165578109188942 ) ) ;
#1551=CARTESIAN_POINT ( 'NONE',  ( 6.809999908187194197E-13, -9.988891130263535700, -9.559589141758145558 ) ) ;
#1554=PLANE ( 'NONE',  #19356 ) ;
#1572=CARTESIAN_POINT ( 'NONE',  ( 6.809999908187194197E-13, -9.988891130263535700, 10.70674201446023233 ) ) ;
#1573=CARTESIAN_POINT ( 'NONE',  ( 9.499999999999790390, 3.086737114213260025, 9.306742014460233747 ) ) ;
#1586=ADVANCED_FACE ( 'NONE', ( #6225, #7677 ), #22839, .T. ) ;
#1589=CARTESIAN_POINT ( 'NONE',  ( -0.6269384450604889025, 9.499999999999955591, -3.500543795355101295 ) ) ;
#1592=CARTESIAN_POINT ( 'NONE',  ( -7.022953521754877748, -5.102474405760673015, -7.833165578109188232 ) ) ;
#1607=CARTESIAN_POINT ( 'NONE',  ( -5.622572944242077574E-13, 8.680847955711007202, -3.133165578109187610 ) ) ;
#1609=CARTESIAN_POINT ( 'NONE',  ( -2.935661446561384391, -9.035036904804158553, -5.459589141758144137 ) ) ;
#1616=EDGE_CURVE ( 'NONE', #6271, #5371, #20891, .T. ) ;
#1628=ORIENTED_EDGE ( 'NONE', *, *, #1510, .T. ) ;
#1630=VERTEX_POINT ( 'NONE', #13288 ) ;
#1641=DIRECTION ( 'NONE',  ( -0.000000000000000000, -0.000000000000000000, -1.000000000000000000 ) ) ;
#1653=CARTESIAN_POINT ( 'NONE',  ( 6.222797240145152671E-13, -9.127583699786111282, 8.133165578109188942 ) ) ;
#1669=CARTESIAN_POINT ( 'NONE',  ( 8.680847955710813579, 2.820578480814259326, -8.733165578109185034 ) ) ;
#1671=DIRECTION ( 'NONE',  ( -0.000000000000000000, -0.000000000000000000, -1.000000000000000000 ) ) ;
#1691=CARTESIAN_POINT ( 'NONE',  ( -9.500000000000211386, 3.086737114211961064, 8.106742014460232681 ) ) ;
#1711=DIRECTION ( 'NONE',  ( 1.000000000000000000, 0.000000000000000000, 0.000000000000000000 ) ) ;
#1712=CARTESIAN_POINT ( 'NONE',  ( 5.365059087799946447, -7.384370330706356178, -10.33316557810919001 ) ) ;
#1715=( BOUNDED_CURVE ( )  B_SPLINE_CURVE ( 2, ( #15462, #7876, #15329, #22802, #22925, #6308, #6084, #11917, #13525, #19261, #4254 ),
 .UNSPECIFIED., .F., .T. ) 
 B_SPLINE_CURVE_WITH_KNOTS ( ( 3, 2, 2, 2, 2, 3 ),
 ( 0.6000000000000000888, 0.6200000000000001066, 0.6400000000000001243, 0.6600000000000001421, 0.6800000000000001599, 0.7000000000000000666 ),
 .UNSPECIFIED. ) 
 CURVE ( )  GEOMETRIC_REPRESENTATION_ITEM ( )  RATIONAL_B_SPLINE_CURVE ( ( 0.9999999999999997780, 0.9510565162951537532, 1.000000000000000000, 0.9510565162951535312, 1.000000000000000000, 0.9510565162951535312, 1.000000000000000000, 0.9510565162951535312, 1.000000000000000000, 0.9510565162951533091, 1.000000000000000222 ) ) 
 REPRESENTATION_ITEM ( '' )  );
#1724=CARTESIAN_POINT ( 'NONE',  ( 8.076302169966863786, -3.241261634297124772, -12.50000000000002309 ) ) ;
#1732=CARTESIAN_POINT ( 'NONE',  ( 2.935661446561383503, 9.035036904804158553, -10.45958914175814414 ) ) ;
#1735=ORIENTED_EDGE ( 'NONE', *, *, #1616, .T. ) ;
#1751=CARTESIAN_POINT ( 'NONE',  ( -6.233975306307046963E-13, 9.127583699786111282, 7.133165578109187166 ) ) ;
#1765=FACE_OUTER_BOUND ( 'NONE', #1911, .T. ) ;
#1775=FACE_OUTER_BOUND ( 'NONE', #16689, .T. ) ;
#1777=CARTESIAN_POINT ( 'NONE',  ( 9.301232020971131220, 6.335487896752478916E-13, -12.19876797902886700 ) ) ;
#1780=CARTESIAN_POINT ( 'NONE',  ( 6.222797240145152671E-13, -9.127583699786111282, 10.13316557810918894 ) ) ;
#1788=CARTESIAN_POINT ( 'NONE',  ( 8.680847955711007202, 5.912916378492122225E-13, -10.63316557810918894 ) ) ;
#1800=DIRECTION ( 'NONE',  ( -0.000000000000000000, -0.000000000000000000, -1.000000000000000000 ) ) ;
#1803=CARTESIAN_POINT ( 'NONE',  ( -5.871322893123449127, -8.081182679344781405, -7.359589141758142716 ) ) ;
#1808=EDGE_CURVE ( 'NONE', #11482, #23301, #22258, .T. ) ;
#1810=CARTESIAN_POINT ( 'NONE',  ( -6.822232771736903637E-13, 9.988891130263535700, -9.706742014460232326 ) ) ;
#1817=CARTESIAN_POINT ( 'NONE',  ( 9.500000000000000000, 6.470877716354879437E-13, 7.206742014460234103 ) ) ;
#1849=EDGE_CURVE ( 'NONE', #17696, #2680, #10324, .T. ) ;
#1850=CARTESIAN_POINT ( 'NONE',  ( -6.822232771736903637E-13, 9.988891130263535700, -6.559589141758143782 ) ) ;
#1874=CARTESIAN_POINT ( 'NONE',  ( -9.000000000000001776, 0.000000000000000000, 12.50000000000000000 ) ) ;
#1881=CARTESIAN_POINT ( 'NONE',  ( 6.250000000000000000, -10.82531754730548279, 2.500000000000000000 ) ) ;
#1885=AXIS2_PLACEMENT_3D ( 'NONE', #19979, #1671, #21810 ) ;
#1897=CARTESIAN_POINT ( 'NONE',  ( -6.822232771736903637E-13, 9.988891130263535700, 10.55958914175814378 ) ) ;
#1903=CARTESIAN_POINT ( 'NONE',  ( -2.682529543900285862, 8.255977015246234174, -9.233165578109188587 ) ) ;
#1911=EDGE_LOOP ( 'NONE', ( #23621, #12603, #7007, #9760, #11729 ) ) ;
#1915=CARTESIAN_POINT ( 'NONE',  ( -9.500000000000202505, 3.086737114211975275, -8.959589141758142361 ) ) ;
#1922=CARTESIAN_POINT ( 'NONE',  ( -7.685661446562381371, 5.583959896777970222, 12.00674201446023481 ) ) ;
#1923=EDGE_LOOP ( 'NONE', ( #1275, #20934, #20599, #20192 ) ) ;
#1925=CARTESIAN_POINT ( 'NONE',  ( 0.000000000000000000, 0.000000000000000000, 3.499999999999999556 ) ) ;
#1935=FACE_OUTER_BOUND ( 'NONE', #4016, .T. ) ;
#1948=FACE_OUTER_BOUND ( 'NONE', #16003, .T. ) ;
#1951=CARTESIAN_POINT ( 'NONE',  ( -5.871322893123450015, -8.081182679344781405, -5.359589141758144493 ) ) ;
#1969=DIRECTION ( 'NONE',  ( 0.7071067811865439090, 4.816422645750986228E-14, -0.7071067811865512365 ) ) ;
#1976=ORIENTED_EDGE ( 'NONE', *, *, #18143, .F. ) ;
#1988=VECTOR ( 'NONE', #18068, 1000.000000000000227 ) ;
#1990=CARTESIAN_POINT ( 'NONE',  ( 0.000000000000000000, 0.000000000000000000, -12.50000000000000000 ) ) ;
#1996=ORIENTED_EDGE ( 'NONE', *, *, #7805, .T. ) ;
#1997=CARTESIAN_POINT ( 'NONE',  ( 8.680847955710813579, 2.820578480814259326, 6.733165578109187699 ) ) ;
#2008=CARTESIAN_POINT ( 'NONE',  ( 6.222797240145152671E-13, -9.127583699786111282, -10.13316557810918894 ) ) ;
#2012=VERTEX_POINT ( 'NONE', #18451 ) ;
#2026=CIRCLE ( 'NONE', #18783, 1.000000000000000000 ) ;
#2027=CARTESIAN_POINT ( 'NONE',  ( 7.685661446562381371, -5.583959896777971110, -5.859589141758143604 ) ) ;
#2028=CARTESIAN_POINT ( 'NONE',  ( -7.022953521754877748, -5.102474405760673015, -11.83316557810918823 ) ) ;
#2031=VECTOR ( 'NONE', #2727, 1000.000000000000000 ) ;
#2038=ORIENTED_EDGE ( 'NONE', *, *, #10766, .T. ) ;
#2040=CARTESIAN_POINT ( 'NONE',  ( -5.871322893123449127, -8.081182679344781405, 9.359589141758144493 ) ) ;
#2067=CIRCLE ( 'NONE', #16488, 10.49999999999999822 ) ;
#2076=CARTESIAN_POINT ( 'NONE',  ( -5.871322893124554021, 8.081182679343978492, -10.75958914175814130 ) ) ;
#2113=EDGE_LOOP ( 'NONE', ( #9487, #2649, #20729, #14313 ) ) ;
#2132=CARTESIAN_POINT ( 'NONE',  ( -7.022953521754877748, -5.102474405760673015, 3.833165578109188676 ) ) ;
#2133=ORIENTED_EDGE ( 'NONE', *, *, #11929, .F. ) ;
#2140=CARTESIAN_POINT ( 'NONE',  ( -2.682529543900285862, 8.255977015246234174, -11.23316557810918859 ) ) ;
#2160=CARTESIAN_POINT ( 'NONE',  ( -2.935661446561384391, -9.035036904804158553, -5.459589141758144137 ) ) ;
#2172=LINE ( 'NONE', #17044, #5315 ) ;
#2178=DIRECTION ( 'NONE',  ( 0.000000000000000000, 0.000000000000000000, -1.000000000000000000 ) ) ;
#2189=EDGE_CURVE ( 'NONE', #16661, #17696, #10053, .T. ) ;
#2200=B_SPLINE_CURVE_WITH_KNOTS ( 'NONE', 3,
 ( #12990, #3605, #16298, #14584, #11027, #7148, #23757, #23867, #20102, #12502 ),
 .UNSPECIFIED., .F., .F.,
 ( 4, 2, 2, 2, 4 ),
 ( 1.433669752132626775E-14, 0.001535707958717136149, 0.003071415917419935675, 0.004607123876122735419, 0.006142831834825534729 ),
 .UNSPECIFIED. ) ;
#2206=( BOUNDED_CURVE ( )  B_SPLINE_CURVE ( 2, ( #6720, #20148, #17834, #21842, #6846, #5122, #23446, #3421, #12544, #5252, #10836 ),
 .UNSPECIFIED., .F., .F. ) 
 B_SPLINE_CURVE_WITH_KNOTS ( ( 3, 2, 2, 2, 2, 3 ),
 ( 0.09999999999999992228, 0.1199999999999999262, 0.1399999999999999578, 0.1599999999999999756, 0.1799999999999999656, 0.2000000000000000111 ),
 .UNSPECIFIED. ) 
 CURVE ( )  GEOMETRIC_REPRESENTATION_ITEM ( )  RATIONAL_B_SPLINE_CURVE ( ( 1.000000000000000222, 0.9510565162951533091, 1.000000000000000000, 0.9510565162951535312, 1.000000000000000000, 0.9510565162951535312, 1.000000000000000000, 0.9510565162951535312, 1.000000000000000000, 0.9510565162951535312, 1.000000000000000000 ) ) 
 REPRESENTATION_ITEM ( '' )  );
#2208=ORIENTED_EDGE ( 'NONE', *, *, #23098, .T. ) ;
#2217=VECTOR ( 'NONE', #21626, 1000.000000000000000 ) ;
#2224=CARTESIAN_POINT ( 'NONE',  ( -2.682529543900285862, 8.255977015246234174, 11.23316557810918859 ) ) ;
#2235=ADVANCED_FACE ( 'NONE', ( #8292 ), #17888, .T. ) ;
#2249=CARTESIAN_POINT ( 'NONE',  ( 2.935661446562616295, -9.035036904803758873, -8.806742014460233747 ) ) ;
#2254=CARTESIAN_POINT ( 'NONE',  ( 2.682529543900284974, -8.255977015246234174, 4.233165578109187699 ) ) ;
#2259=ORIENTED_EDGE ( 'NONE', *, *, #7805, .F. ) ;
#2262=CARTESIAN_POINT ( 'NONE',  ( -2.682529543899159208, -8.255977015246598327, -6.033165578109189298 ) ) ;
#2266=CYLINDRICAL_SURFACE ( 'NONE', #20902, 9.500000000000000000 ) ;
#2268=ADVANCED_FACE ( 'NONE', ( #15986 ), #11225, .T. ) ;
#2284=CARTESIAN_POINT ( 'NONE',  ( -8.680847955711007202, -5.923547351154968927E-13, 11.63316557810919072 ) ) ;
#2297=EDGE_CURVE ( 'NONE', #20703, #4215, #10886, .T. ) ;
#2308=CARTESIAN_POINT ( 'NONE',  ( -8.680847955711200825, 2.820578480813073607, -7.533165578109188409 ) ) ;
#2324=EDGE_CURVE ( 'NONE', #18928, #20510, #16234, .T. ) ;
#2328=CARTESIAN_POINT ( 'NONE',  ( -8.523217878158652283, -3.742469342540160060, 12.19934731935375538 ) ) ;
#2330=CARTESIAN_POINT ( 'NONE',  ( -9.345831411446008374, 1.026058333938473455, 12.10150359048600954 ) ) ;
#2334=FACE_OUTER_BOUND ( 'NONE', #2364, .T. ) ;
#2335=CARTESIAN_POINT ( 'NONE',  ( 7.685661446562381371, -5.583959896777971110, -7.006742014460233037 ) ) ;
#2338=CARTESIAN_POINT ( 'NONE',  ( -8.680847955711007202, -5.923547351154968927E-13, 9.633165578109188942 ) ) ;
#2347=CARTESIAN_POINT ( 'NONE',  ( -9.378401895172215674, 3.550564238312661509E-15, 12.12159810482778077 ) ) ;
#2349=CARTESIAN_POINT ( 'NONE',  ( -9.499999999999790390, -3.086737114213257804, -12.30674201446023197 ) ) ;
#2357=LINE ( 'NONE', #6148, #5599 ) ;
#2362=EDGE_CURVE ( 'NONE', #14734, #22998, #19952, .T. ) ;
#2364=EDGE_LOOP ( 'NONE', ( #21509, #16238, #21427, #20211, #16671, #7867 ) ) ;
#2365=CARTESIAN_POINT ( 'NONE',  ( 9.500000000000209610, -3.086737114211962396, 11.95958914175814591 ) ) ;
#2374=CARTESIAN_POINT ( 'NONE',  ( 2.682529543900284974, -8.255977015246234174, -6.233165578109188587 ) ) ;
#2387=CARTESIAN_POINT ( 'NONE',  ( 7.685661446562381371, -5.583959896777971110, 3.859589141758143604 ) ) ;
#2390=CARTESIAN_POINT ( 'NONE',  ( -7.685661446561619314, -5.583959896779019161, -5.259589141758143960 ) ) ;
#2391=CARTESIAN_POINT ( 'NONE',  ( 8.680847955711007202, 5.912916378492122225E-13, -8.633165578109188942 ) ) ;
#2393=ORIENTED_EDGE ( 'NONE', *, *, #2852, .F. ) ;
#2396=EDGE_CURVE ( 'NONE', #17583, #19174, #23397, .T. ) ;
#2405=CARTESIAN_POINT ( 'NONE',  ( -6.822232771736903637E-13, 9.988891130263535700, -10.55958914175814378 ) ) ;
#2420=CARTESIAN_POINT ( 'NONE',  ( 2.935661446562616295, -9.035036904803758873, 4.806742014460232859 ) ) ;
#2422=CARTESIAN_POINT ( 'NONE',  ( 8.680847955710813579, 2.820578480814259326, -6.733165578109187699 ) ) ;
#2424=ORIENTED_EDGE ( 'NONE', *, *, #15034, .F. ) ;
#2425=CARTESIAN_POINT ( 'NONE',  ( 7.685661446561619314, 5.583959896779020049, 8.259589141758144848 ) ) ;
#2441=CARTESIAN_POINT ( 'NONE',  ( -7.685661446561619314, -5.583959896779019161, -3.259589141758143516 ) ) ;
#2446=CARTESIAN_POINT ( 'NONE',  ( -8.133009343831700377, 4.898054503500675949, 12.01970453032984487 ) ) ;
#2458=CARTESIAN_POINT ( 'NONE',  ( -7.685661446562381371, 5.583959896777970222, -4.006742014460233925 ) ) ;
#2461=CARTESIAN_POINT ( 'NONE',  ( 8.680847955710813579, 2.820578480814259326, 8.733165578109186811 ) ) ;
#2474=CARTESIAN_POINT ( 'NONE',  ( -5.871322893123450015, -8.081182679344781405, -8.506742014460233037 ) ) ;
#2490=CARTESIAN_POINT ( 'NONE',  ( 9.330908268522616567, -1.784418920661929642, -11.99999999999998934 ) ) ;
#2497=CARTESIAN_POINT ( 'NONE',  ( 5.871322893123449127, 8.081182679344781405, 4.359589141758143604 ) ) ;
#2507=CARTESIAN_POINT ( 'NONE',  ( -7.022953521754877748, -5.102474405760673015, -5.833165578109188232 ) ) ;
#2508=CARTESIAN_POINT ( 'NONE',  ( 2.935661446561383503, 9.035036904804158553, 7.606742014460233570 ) ) ;
#2510=LINE ( 'NONE', #21784, #18102 ) ;
#2520=CARTESIAN_POINT ( 'NONE',  ( 7.685661446561619314, 5.583959896779020049, -8.259589141758144848 ) ) ;
#2524=CARTESIAN_POINT ( 'NONE',  ( -8.680847955711200825, 2.820578480813073607, -5.533165578109187521 ) ) ;
#2529=CARTESIAN_POINT ( 'NONE',  ( -2.682529543900285862, 8.255977015246234174, -11.23316557810918859 ) ) ;
#2530=CARTESIAN_POINT ( 'NONE',  ( -7.022953521755574080, 5.102474405759713783, 11.43316557810918965 ) ) ;
#2534=VECTOR ( 'NONE', #13156, 1000.000000000000000 ) ;
#2538=UNCERTAINTY_MEASURE_WITH_UNIT (LENGTH_MEASURE( 1.000000000000000082E-05 ), #11166, 'distance_accuracy_value', 'NONE');
#2541=CARTESIAN_POINT ( 'NONE',  ( 5.626939011991881401, -6.906580693685397954, 12.50000000000000000 ) ) ;
#2547=CIRCLE ( 'NONE', #16181, 9.500000000000000000 ) ;
#2558=ORIENTED_EDGE ( 'NONE', *, *, #2324, .F. ) ;
#2559=CARTESIAN_POINT ( 'NONE',  ( -8.680847955711007202, -5.923547351154968927E-13, -3.633165578109188054 ) ) ;
#2562=CARTESIAN_POINT ( 'NONE',  ( -9.499999999999790390, -3.086737114213257804, 9.159589141758145203 ) ) ;
#2563=CARTESIAN_POINT ( 'NONE',  ( -9.500000000000000000, -6.482511860946779655E-13, 12.20674201446023410 ) ) ;
#2567=CARTESIAN_POINT ( 'NONE',  ( 8.680847955711007202, 5.912916378492122225E-13, -12.63316557810918894 ) ) ;
#2576=CARTESIAN_POINT ( 'NONE',  ( 10.49999999999999822, 0.000000000000000000, -3.499999999999999556 ) ) ;
#2584=CARTESIAN_POINT ( 'NONE',  ( 0.000000000000000000, 0.000000000000000000, -12.50000000000000000 ) ) ;
#2585=CARTESIAN_POINT ( 'NONE',  ( 9.301232020971131220, 6.335487896752478916E-13, -12.19876797902886700 ) ) ;
#2592=CARTESIAN_POINT ( 'NONE',  ( -7.685661446562381371, 5.583959896777970222, -8.006742014460233037 ) ) ;
#2595=CARTESIAN_POINT ( 'NONE',  ( -2.682529543899159208, -8.255977015246598327, 6.033165578109189298 ) ) ;
#2597=PRODUCT_DEFINITION_FORMATION_WITH_SPECIFIED_SOURCE ( 'ANY', '', #10186, .NOT_KNOWN. ) ;
#2603=ORIENTED_EDGE ( 'NONE', *, *, #23259, .F. ) ;
#2618=CARTESIAN_POINT ( 'NONE',  ( 9.500000000000000000, 1.163414459189985485E-15, 12.50000000000000000 ) ) ;
#2622=CARTESIAN_POINT ( 'NONE',  ( -5.871322893124554021, 8.081182679343978492, -4.759589141758143960 ) ) ;
#2625=CARTESIAN_POINT ( 'NONE',  ( 5.871322893124553133, -8.081182679343980269, 9.759589141758143072 ) ) ;
#2627=ORIENTED_EDGE ( 'NONE', *, *, #16032, .F. ) ;
#2631=CARTESIAN_POINT ( 'NONE',  ( 8.680847955710813579, 2.820578480814259326, -4.733165578109188587 ) ) ;
#2632=CARTESIAN_POINT ( 'NONE',  ( -6.822232771736904647E-13, 9.988891130263535700, 7.706742014460232326 ) ) ;
#2635=DIRECTION ( 'NONE',  ( -0.5000000000000001110, -0.8660254037844384856, 0.000000000000000000 ) ) ;
#2648=CARTESIAN_POINT ( 'NONE',  ( 2.682529543900284974, -8.255977015246234174, -6.233165578109188587 ) ) ;
#2649=ORIENTED_EDGE ( 'NONE', *, *, #9525, .T. ) ;
#2651=CARTESIAN_POINT ( 'NONE',  ( -8.680847955710813579, -2.820578480814258437, 11.73316557810918859 ) ) ;
#2660=CARTESIAN_POINT ( 'NONE',  ( 0.000000000000000000, 0.000000000000000000, -12.00000000000000000 ) ) ;
#2674=CARTESIAN_POINT ( 'NONE',  ( -8.680847955711007202, -5.923547351154968927E-13, -5.633165578109188942 ) ) ;
#2680=VERTEX_POINT ( 'NONE', #8416 ) ;
#2696=CARTESIAN_POINT ( 'NONE',  ( -9.363437198784961168, -0.7753088219917839696, 12.13656280121503883 ) ) ;
#2697=CARTESIAN_POINT ( 'NONE',  ( -9.500000000000000000, -6.482511860946779655E-13, 11.05958914175814556 ) ) ;
#2702=CARTESIAN_POINT ( 'NONE',  ( -5.871322893124554021, 8.081182679343978492, -7.906742014460233392 ) ) ;
#2705=CARTESIAN_POINT ( 'NONE',  ( -9.500000000000211386, 3.086737114211961064, -8.106742014460232681 ) ) ;
#2708=CARTESIAN_POINT ( 'NONE',  ( -8.680847955710813579, -2.820578480814257549, 9.733165578109186811 ) ) ;
#2719=CARTESIAN_POINT ( 'NONE',  ( -2.935661446561384391, -9.035036904804158553, -10.60674201446023446 ) ) ;
#2727=DIRECTION ( 'NONE',  ( -0.000000000000000000, -0.000000000000000000, -1.000000000000000000 ) ) ;
#2729=CYLINDRICAL_SURFACE ( 'NONE', #7901, 9.500000000000000000 ) ;
#2731=DIRECTION ( 'NONE',  ( 0.8660254037844385966, 0.5000000000000003331, -0.000000000000000000 ) ) ;
#2736=CARTESIAN_POINT ( 'NONE',  ( 7.685661446561619314, 5.583959896779020049, 6.259589141758143960 ) ) ;
#2744=CARTESIAN_POINT ( 'NONE',  ( 5.365059087799946447, -7.384370330706356178, -4.333165578109189120 ) ) ;
#2759=CARTESIAN_POINT ( 'NONE',  ( -5.365059087798940141, -7.384370330707086261, -9.933165578109189653 ) ) ;
#2763=ORIENTED_EDGE ( 'NONE', *, *, #9897, .F. ) ;
#2765=CARTESIAN_POINT ( 'NONE',  ( -2.682529543900285862, 8.255977015246234174, 9.233165578109188587 ) ) ;
#2774=CARTESIAN_POINT ( 'NONE',  ( -9.500000000000000000, -6.482511860946779655E-13, -11.05958914175814556 ) ) ;
#2777=CARTESIAN_POINT ( 'NONE',  ( 8.511897654723208362, -2.099402067127519533, 12.50000000000000000 ) ) ;
#2792=CARTESIAN_POINT ( 'NONE',  ( 5.871322893123449127, 8.081182679344781405, -11.50674201446023126 ) ) ;
#2796=CARTESIAN_POINT ( 'NONE',  ( -9.500000000000211386, 3.086737114211961064, 4.959589141758145026 ) ) ;
#2797=CARTESIAN_POINT ( 'NONE',  ( 9.500000000000209610, -3.086737114211962396, 11.10674201446023446 ) ) ;
#2802=CARTESIAN_POINT ( 'NONE',  ( -7.685661446562381371, 5.583959896777970222, 2.859589141758144493 ) ) ;
#2811=CARTESIAN_POINT ( 'NONE',  ( -1.332035614406995583, -9.022543824230414344, 12.38784953505801667 ) ) ;
#2813=CARTESIAN_POINT ( 'NONE',  ( 9.376681730866069486, -1.188761456322952936, 12.06692573382530931 ) ) ;
#2832=CARTESIAN_POINT ( 'NONE',  ( 5.871322893124553133, -8.081182679343980269, -8.906742014460233392 ) ) ;
#2833=EDGE_LOOP ( 'NONE', ( #16684, #17161, #15626, #13597 ) ) ;
#2846=ORIENTED_EDGE ( 'NONE', *, *, #17652, .T. ) ;
#2852=EDGE_CURVE ( 'NONE', #14927, #13793, #18060, .T. ) ;
#2858=CARTESIAN_POINT ( 'NONE',  ( 7.685661446561619314, 5.583959896779020049, 8.259589141758144848 ) ) ;
#2865=AXIS2_PLACEMENT_3D ( 'NONE', #9047, #14185, #5053 ) ;
#2871=ORIENTED_EDGE ( 'NONE', *, *, #13640, .F. ) ;
#2877=CARTESIAN_POINT ( 'NONE',  ( 5.871322893123449127, 8.081182679344781405, 5.506742014460233925 ) ) ;
#2889=CARTESIAN_POINT ( 'NONE',  ( -8.680847955711007202, -5.923547351154968927E-13, -7.633165578109188942 ) ) ;
#2896=CARTESIAN_POINT ( 'NONE',  ( 8.680847955711199049, -2.820578480813074496, 6.533165578109188409 ) ) ;
#2906=CARTESIAN_POINT ( 'NONE',  ( 8.076302169966853128, -3.241261634297146088, 12.50000000000002665 ) ) ;
#2907=CARTESIAN_POINT ( 'NONE',  ( -9.500000000000000000, -6.482511860946779655E-13, -6.206742014460234103 ) ) ;
#2913=DIRECTION ( 'NONE',  ( -6.485355633664481337E-14, 1.000000000000000000, 0.000000000000000000 ) ) ;
#2914=ADVANCED_FACE ( 'NONE', ( #13143 ), #16605, .F. ) ;
#2925=CARTESIAN_POINT ( 'NONE',  ( 9.499999999999790390, 3.086737114213260025, 6.159589141758145203 ) ) ;
#2926=CARTESIAN_POINT ( 'NONE',  ( -7.685661446562381371, 5.583959896777970222, 12.00674201446023481 ) ) ;
#2971=CARTESIAN_POINT ( 'NONE',  ( -5.871322893123450015, -8.081182679344781405, -6.506742014460233925 ) ) ;
#2983=DIRECTION ( 'NONE',  ( -0.000000000000000000, -0.000000000000000000, -1.000000000000000000 ) ) ;
#2988=CARTESIAN_POINT ( 'NONE',  ( -9.500000000000000000, -6.482511860946779655E-13, -10.20674201446023233 ) ) ;
#2992=CARTESIAN_POINT ( 'NONE',  ( -9.500000000000211386, 3.086737114211961064, 8.959589141758140585 ) ) ;
#3010=( BOUNDED_CURVE ( )  B_SPLINE_CURVE ( 2, ( #23145, #10432, #15931, #1067, #17631, #10541, #23636, #1181, #21317, #13872, #8488 ),
 .UNSPECIFIED., .F., .T. ) 
 B_SPLINE_CURVE_WITH_KNOTS ( ( 3, 2, 2, 2, 2, 3 ),
 ( 0.7000000000000000666, 0.7200000000000000844, 0.7400000000000001021, 0.7600000000000000089, 0.7800000000000000266, 0.8000000000000000444 ),
 .UNSPECIFIED. ) 
 CURVE ( )  GEOMETRIC_REPRESENTATION_ITEM ( )  RATIONAL_B_SPLINE_CURVE ( ( 0.9999999999999997780, 0.9510565162951537532, 1.000000000000000000, 0.9510565162951535312, 1.000000000000000000, 0.9510565162951535312, 1.000000000000000000, 0.9510565162951535312, 1.000000000000000000, 0.9510565162951535312, 1.000000000000000000 ) ) 
 REPRESENTATION_ITEM ( '' )  );
#3012=CARTESIAN_POINT ( 'NONE',  ( -9.499999999999790390, -3.086737114213257804, 6.306742014460231971 ) ) ;
#3017=CARTESIAN_POINT ( 'NONE',  ( 0.000000000000000000, 0.000000000000000000, 12.50000000000000000 ) ) ;
#3018=CARTESIAN_POINT ( 'NONE',  ( 5.365059087799947335, -7.384370330706356178, -4.333165578109189120 ) ) ;
#3023=CARTESIAN_POINT ( 'NONE',  ( -8.680847955711200825, 2.820578480813073607, 7.533165578109188409 ) ) ;
#3025=ORIENTED_EDGE ( 'NONE', *, *, #18761, .T. ) ;
#3032=CARTESIAN_POINT ( 'NONE',  ( -9.499999999999790390, -3.086737114213257804, -7.159589141758144315 ) ) ;
#3046=CARTESIAN_POINT ( 'NONE',  ( -8.680847955710813579, -2.820578480814258437, -5.733165578109188587 ) ) ;
#3049=CARTESIAN_POINT ( 'NONE',  ( -2.935661446561384391, -9.035036904804158553, 5.459589141758144137 ) ) ;
#3050=CARTESIAN_POINT ( 'NONE',  ( -2.935661446561384391, -9.035036904804158553, 4.606742014460233570 ) ) ;
#3067=CARTESIAN_POINT ( 'NONE',  ( -9.014529360237583333, 3.062692055659724133, -3.500237789100161923 ) ) ;
#3081=EDGE_CURVE ( 'NONE', #5584, #10554, #1715, .T. ) ;
#3084=EDGE_LOOP ( 'NONE', ( #18596, #12114, #22270, #8230 ) ) ;
#3086=CARTESIAN_POINT ( 'NONE',  ( -9.499999999999790390, -3.086737114213257804, -6.306742014460231971 ) ) ;
#3097=CARTESIAN_POINT ( 'NONE',  ( -6.822232771736904647E-13, 9.988891130263535700, -9.706742014460232326 ) ) ;
#3099=CARTESIAN_POINT ( 'NONE',  ( -2.935661446562617183, 9.035036904803758873, -4.659589141758143427 ) ) ;
#3100=CARTESIAN_POINT ( 'NONE',  ( -9.500000000000000000, 1.163414459189985485E-15, -12.00000000000000000 ) ) ;
#3114=CARTESIAN_POINT ( 'NONE',  ( -5.871322893123450015, -8.081182679344781405, 6.506742014460233925 ) ) ;
#3116=VERTEX_POINT ( 'NONE', #2907 ) ;
#3127=EDGE_CURVE ( 'NONE', #21315, #9633, #20767, .T. ) ;
#3128=CARTESIAN_POINT ( 'NONE',  ( 8.680847955710813579, 2.820578480814259326, 6.733165578109187699 ) ) ;
#3134=CARTESIAN_POINT ( 'NONE',  ( -9.500000000000000000, -6.482511860946779655E-13, -9.059589141758143782 ) ) ;
#3138=LINE ( 'NONE', #23299, #16952 ) ;
#3152=CARTESIAN_POINT ( 'NONE',  ( 7.685661446561619314, 5.583959896779020049, -9.406742014460235168 ) ) ;
#3154=EDGE_CURVE ( 'NONE', #7449, #5584, #3138, .T. ) ;
#3157=CARTESIAN_POINT ( 'NONE',  ( 9.500000000000209610, -3.086737114211962396, 5.959589141758143249 ) ) ;
#3158=CARTESIAN_POINT ( 'NONE',  ( 9.500000000000000000, 6.470877716354879437E-13, 5.206742014460234103 ) ) ;
#3171=CARTESIAN_POINT ( 'NONE',  ( -4.754193646886300861, 8.248659687480364155, -3.499363352907163272 ) ) ;
#3192=CARTESIAN_POINT ( 'NONE',  ( 5.871322893124553133, -8.081182679343980269, -4.906742014460232504 ) ) ;
#3212=CARTESIAN_POINT ( 'NONE',  ( -10.49999999999999822, 1.285879139104720633E-15, 2.499999999999999556 ) ) ;
#3215=CARTESIAN_POINT ( 'NONE',  ( 5.871322893124553133, -8.081182679343980269, 3.759589141758144404 ) ) ;
#3227=CIRCLE ( 'NONE', #15284, 10.49999999999999822 ) ;
#3231=CARTESIAN_POINT ( 'NONE',  ( 9.500000000000000000, 6.470877716354879437E-13, -9.206742014460234103 ) ) ;
#3232=CARTESIAN_POINT ( 'NONE',  ( 9.500000000000000000, 6.470877716354879437E-13, 5.206742014460234103 ) ) ;
#3233=CARTESIAN_POINT ( 'NONE',  ( -6.822232771736903637E-13, 9.988891130263535700, 5.706742014460234103 ) ) ;
#3245=CARTESIAN_POINT ( 'NONE',  ( 8.680847955710813579, 2.820578480814259326, 10.73316557810918503 ) ) ;
#3254=CARTESIAN_POINT ( 'NONE',  ( 2.935661446561383503, 9.035036904804158553, -6.459589141758144137 ) ) ;
#3278=CARTESIAN_POINT ( 'NONE',  ( 2.935661446561383503, 9.035036904804158553, 6.459589141758144137 ) ) ;
#3279=CARTESIAN_POINT ( 'NONE',  ( -9.500000000000000000, -6.482511860946779655E-13, 8.206742014460234103 ) ) ;
#3287=CARTESIAN_POINT ( 'NONE',  ( -2.935661446561384391, -9.035036904804158553, 3.459589141758144137 ) ) ;
#3300=CARTESIAN_POINT ( 'NONE',  ( -6.283940952339894359, 7.151940571226186094, -3.501042821985360654 ) ) ;
#3306=CARTESIAN_POINT ( 'NONE',  ( 2.682529543900284974, -8.255977015246234174, -8.233165578109190363 ) ) ;
#3310=CARTESIAN_POINT ( 'NONE',  ( -9.378401895172221003, -4.713374146359802882E-16, -12.12159810482778788 ) ) ;
#3318=LINE ( 'NONE', #7080, #4793 ) ;
#3325=CARTESIAN_POINT ( 'NONE',  ( 9.500000000000209610, -3.086737114211962396, -11.95958914175814591 ) ) ;
#3337=CARTESIAN_POINT ( 'NONE',  ( -2.935661446562617183, 9.035036904803758873, -9.806742014460233747 ) ) ;
#3340=VERTEX_POINT ( 'NONE', #23872 ) ;
#3359=CARTESIAN_POINT ( 'NONE',  ( -2.935661446562617183, 9.035036904803758873, 3.806742014460233303 ) ) ;
#3365=CARTESIAN_POINT ( 'NONE',  ( -8.680847955710813579, -2.820578480814257549, -3.733165578109188587 ) ) ;
#3368=CARTESIAN_POINT ( 'NONE',  ( 6.222797240145152671E-13, -9.127583699786111282, 12.13316557810918717 ) ) ;
#3379=CARTESIAN_POINT ( 'NONE',  ( 5.871322893124553133, -8.081182679343980269, -5.759589141758144848 ) ) ;
#3403=CARTESIAN_POINT ( 'NONE',  ( 2.935661446562616295, -9.035036904803758873, 8.806742014460233747 ) ) ;
#3404=CARTESIAN_POINT ( 'NONE',  ( 5.871322893124553133, -8.081182679343980269, 8.906742014460233392 ) ) ;
#3406=ORIENTED_EDGE ( 'NONE', *, *, #24004, .T. ) ;
#3410=CARTESIAN_POINT ( 'NONE',  ( 9.500000000000209610, -3.086737114211962396, -5.106742014460234458 ) ) ;
#3421=CARTESIAN_POINT ( 'NONE',  ( 5.871322893123448239, 8.081182679344781405, 10.35958914175814449 ) ) ;
#3425=VERTEX_POINT ( 'NONE', #20111 ) ;
#3431=EDGE_CURVE ( 'NONE', #23486, #3340, #9223, .T. ) ;
#3437=CARTESIAN_POINT ( 'NONE',  ( 5.365059087798938364, 7.384370330707087149, -10.93316557810918788 ) ) ;
#3442=FACE_OUTER_BOUND ( 'NONE', #10710, .T. ) ;
#3445=CARTESIAN_POINT ( 'NONE',  ( 2.935661446562616295, -9.035036904803758873, -5.659589141758144315 ) ) ;
#3458=CARTESIAN_POINT ( 'NONE',  ( 9.499999999999790390, 3.086737114213260025, -9.306742014460233747 ) ) ;
#3460=CARTESIAN_POINT ( 'NONE',  ( 9.500000000000000000, 6.470877716354879437E-13, 8.059589141758143782 ) ) ;
#3465=DIRECTION ( 'NONE',  ( 0.5000000000000002220, 0.8660254037844384856, 0.000000000000000000 ) ) ;
#3468=ORIENTED_EDGE ( 'NONE', *, *, #3431, .T. ) ;
#3478=CYLINDRICAL_SURFACE ( 'NONE', #15728, 9.500000000000000000 ) ;
#3484=CARTESIAN_POINT ( 'NONE',  ( 5.365059087799946447, -7.384370330706356178, 8.333165578109190008 ) ) ;
#3487=CARTESIAN_POINT ( 'NONE',  ( 0.000000000000000000, 0.000000000000000000, -2.500000000000000000 ) ) ;
#3488=ORIENTED_EDGE ( 'NONE', *, *, #8278, .F. ) ;
#3491=CARTESIAN_POINT ( 'NONE',  ( 5.871322893123449127, 8.081182679344781405, -8.359589141758144493 ) ) ;
#3512=ADVANCED_FACE ( 'NONE', ( #1323 ), #14352, .T. ) ;
#3516=CARTESIAN_POINT ( 'NONE',  ( -2.935661446561384391, -9.035036904804158553, 8.606742014460234458 ) ) ;
#3517=CARTESIAN_POINT ( 'NONE',  ( 9.499999999999790390, 3.086737114213260025, 5.306742014460231971 ) ) ;
#3534=DIRECTION ( 'NONE',  ( -0.000000000000000000, -0.000000000000000000, -1.000000000000000000 ) ) ;
#3543=CARTESIAN_POINT ( 'NONE',  ( 6.809999908187194197E-13, -9.988891130263535700, -9.559589141758145558 ) ) ;
#3548=APPLICATION_CONTEXT ( 'automotive_design' ) ;
#3549=CARTESIAN_POINT ( 'NONE',  ( 6.809999908187194197E-13, -9.988891130263535700, -7.559589141758143782 ) ) ;
#3563=AXIS2_PLACEMENT_3D ( 'NONE', #9163, #23713, #16486 ) ;
#3566=CARTESIAN_POINT ( 'NONE',  ( -5.365059087799947335, 7.384370330706355290, 3.333165578109187344 ) ) ;
#3595=CARTESIAN_POINT ( 'NONE',  ( 8.680847955711199049, -2.820578480813074496, 10.53316557810918752 ) ) ;
#3602=CONICAL_SURFACE ( 'NONE', #22324, 9.000000000000001776, 0.7853981633974431720 ) ;
#3605=CARTESIAN_POINT ( 'NONE',  ( -7.865713094527578164, 5.334608486671521099, -12.00987729971068774 ) ) ;
#3606=CARTESIAN_POINT ( 'NONE',  ( -6.233975306307046963E-13, 9.127583699786111282, -9.133165578109188942 ) ) ;
#3624=VECTOR ( 'NONE', #22848, 999.9999999999998863 ) ;
#3628=CARTESIAN_POINT ( 'NONE',  ( -9.500000000000211386, 3.086737114211961064, -10.10674201446023446 ) ) ;
#3629=( BOUNDED_CURVE ( )  B_SPLINE_CURVE ( 2, ( #7497, #22778, #7853, #22648, #6062, #20950, #5928, #1803, #14951, #9228, #5711 ),
 .UNSPECIFIED., .F., .T. ) 
 B_SPLINE_CURVE_WITH_KNOTS ( ( 3, 2, 2, 2, 2, 3 ),
 ( 0.4000000000000000222, 0.4199999999999999845, 0.4400000000000000022, 0.4600000000000000200, 0.4799999999999999822, 0.5000000000000000000 ),
 .UNSPECIFIED. ) 
 CURVE ( )  GEOMETRIC_REPRESENTATION_ITEM ( )  RATIONAL_B_SPLINE_CURVE ( ( 1.000000000000000000, 0.9510565162951535312, 1.000000000000000000, 0.9510565162951535312, 1.000000000000000000, 0.9510565162951535312, 1.000000000000000000, 0.9510565162951535312, 1.000000000000000000, 0.9510565162951535312, 1.000000000000000000 ) ) 
 REPRESENTATION_ITEM ( '' )  );
#3633=CARTESIAN_POINT ( 'NONE',  ( 9.500000000000209610, -3.086737114211962396, 7.106742014460232681 ) ) ;
#3635=ORIENTED_EDGE ( 'NONE', *, *, #8061, .F. ) ;
#3650=CARTESIAN_POINT ( 'NONE',  ( 9.499999999999790390, 3.086737114213260025, -10.15958914175814343 ) ) ;
#3657=CARTESIAN_POINT ( 'NONE',  ( 2.682529543899157876, 8.255977015246598327, -9.033165578109187521 ) ) ;
#3662=ORIENTED_EDGE ( 'NONE', *, *, #10766, .F. ) ;
#3670=CARTESIAN_POINT ( 'NONE',  ( -9.500000000000000000, -6.482511860946779655E-13, -3.059589141758143338 ) ) ;
#3678=CARTESIAN_POINT ( 'NONE',  ( -6.822232771736903637E-13, 9.988891130263535700, -8.559589141758145558 ) ) ;
#3683=ORIENTED_EDGE ( 'NONE', *, *, #15336, .F. ) ;
#3684=AXIS2_PLACEMENT_3D ( 'NONE', #17884, #10533, #8212 ) ;
#3697=CARTESIAN_POINT ( 'NONE',  ( -7.022953521755574080, 5.102474405759713783, 5.433165578109188765 ) ) ;
#3711=CARTESIAN_POINT ( 'NONE',  ( -9.500000000000000000, -6.482511860946779655E-13, 10.20674201446023233 ) ) ;
#3717=CARTESIAN_POINT ( 'NONE',  ( -6.153822176767817416E-13, 9.500000000000000000, -2.559589141758142894 ) ) ;
#3729=CARTESIAN_POINT ( 'NONE',  ( -5.622572944242076564E-13, 8.680847955711007202, 3.133165578109187166 ) ) ;
#3733=VERTEX_POINT ( 'NONE', #23010 ) ;
#3737=CARTESIAN_POINT ( 'NONE',  ( 5.365059087799946447, -7.384370330706356178, -12.33316557810918646 ) ) ;
#3746=EDGE_LOOP ( 'NONE', ( #12459, #17177, #4349 ) ) ;
#3753=CARTESIAN_POINT ( 'NONE',  ( 9.500000000000000000, 1.163414459189985485E-15, 3.499999999999999556 ) ) ;
#3763=CARTESIAN_POINT ( 'NONE',  ( -6.822232771736903637E-13, 9.988891130263535700, 11.70674201446023410 ) ) ;
#3782=( BOUNDED_CURVE ( )  B_SPLINE_CURVE ( 2, ( #24024, #3410, #1226, #5363, #23784, #6836, #16438, #21724, #12667, #20247, #5016 ),
 .UNSPECIFIED., .F., .T. ) 
 B_SPLINE_CURVE_WITH_KNOTS ( ( 3, 2, 2, 2, 2, 3 ),
 ( 0.8000000000000000444, 0.8199999999999999512, 0.8399999999999999689, 0.8599999999999999867, 0.8800000000000000044, 0.9000000000000000222 ),
 .UNSPECIFIED. ) 
 CURVE ( )  GEOMETRIC_REPRESENTATION_ITEM ( )  RATIONAL_B_SPLINE_CURVE ( ( 1.000000000000000000, 0.9510565162951535312, 1.000000000000000000, 0.9510565162951535312, 1.000000000000000000, 0.9510565162951535312, 1.000000000000000000, 0.9510565162951535312, 1.000000000000000000, 0.9510565162951535312, 1.000000000000000000 ) ) 
 REPRESENTATION_ITEM ( '' )  );
#3784=CARTESIAN_POINT ( 'NONE',  ( 2.682529543900284974, -8.255977015246234174, -10.23316557810918859 ) ) ;
#3798=CARTESIAN_POINT ( 'NONE',  ( 5.871322893123449127, 8.081182679344781405, -6.359589141758142716 ) ) ;
#3802=VERTEX_POINT ( 'NONE', #21177 ) ;
#3803=CARTESIAN_POINT ( 'NONE',  ( -6.822232771736904647E-13, 9.988891130263535700, 5.706742014460233214 ) ) ;
#3811=PLANE ( 'NONE',  #21056 ) ;
#3815=ADVANCED_FACE ( 'NONE', ( #23386 ), #23140, .T. ) ;
#3825=CARTESIAN_POINT ( 'NONE',  ( -2.935661446562617183, 9.035036904803758873, 9.806742014460233747 ) ) ;
#3840=DIRECTION ( 'NONE',  ( 0.000000000000000000, 0.000000000000000000, 1.000000000000000000 ) ) ;
#3841=CARTESIAN_POINT ( 'NONE',  ( 5.871322893124553133, -8.081182679343980269, -8.906742014460233392 ) ) ;
#3845=CARTESIAN_POINT ( 'NONE',  ( -8.680847955711200825, 2.820578480813073607, 3.533165578109187965 ) ) ;
#3852=CARTESIAN_POINT ( 'NONE',  ( -8.680847955710813579, -2.820578480814258437, -7.733165578109187699 ) ) ;
#3860=FACE_OUTER_BOUND ( 'NONE', #2113, .T. ) ;
#3871=CARTESIAN_POINT ( 'NONE',  ( 5.871322893124551356, -8.081182679343980269, 8.906742014460233392 ) ) ;
#3880=CARTESIAN_POINT ( 'NONE',  ( 6.809999908187194197E-13, -9.988891130263535700, 9.559589141758145558 ) ) ;
#3889=DIRECTION ( 'NONE',  ( -1.000000000000000000, 0.000000000000000000, 0.000000000000000000 ) ) ;
#3895=CARTESIAN_POINT ( 'NONE',  ( 8.680847955711199049, -2.820578480813074496, -6.533165578109188409 ) ) ;
#3898=CYLINDRICAL_SURFACE ( 'NONE', #11849, 9.500000000000000000 ) ;
#3909=CARTESIAN_POINT ( 'NONE',  ( 7.685661446561619314, 5.583959896779020049, -10.25958914175814485 ) ) ;
#3916=CARTESIAN_POINT ( 'NONE',  ( 9.499999999999790390, 3.086737114213260025, 5.306742014460231971 ) ) ;
#3917=CARTESIAN_POINT ( 'NONE',  ( -7.561939491010504000, 5.750397476200735269, 11.99999999999999822 ) ) ;
#3919=DIRECTION ( 'NONE',  ( -0.000000000000000000, -0.000000000000000000, -1.000000000000000000 ) ) ;
#3931=ADVANCED_FACE ( 'NONE', ( #1765 ), #18350, .T. ) ;
#3946=CARTESIAN_POINT ( 'NONE',  ( -9.499999999999799272, -3.086737114213243593, 10.30674201446023019 ) ) ;
#3957=CARTESIAN_POINT ( 'NONE',  ( 7.022953521755574080, -5.102474405759714671, 4.433165578109187877 ) ) ;
#3965=CARTESIAN_POINT ( 'NONE',  ( -5.365059087799947335, 7.384370330706355290, -7.333165578109188232 ) ) ;
#3970=CARTESIAN_POINT ( 'NONE',  ( 9.500000000000000000, 1.163414459189985485E-15, 12.50000000000000000 ) ) ;
#3975=B_SPLINE_CURVE_WITH_KNOTS ( 'NONE', 3,
 ( #2585, #23335, #16581, #12909 ),
 .UNSPECIFIED., .F., .F.,
 ( 4, 4 ),
 ( 0.000000000000000000, 0.001795700496623673509 ),
 .UNSPECIFIED. ) ;
#3978=CARTESIAN_POINT ( 'NONE',  ( 9.500000000000000000, 1.163414459189985485E-15, 12.50000000000000000 ) ) ;
#3989=ORIENTED_EDGE ( 'NONE', *, *, #18579, .F. ) ;
#3990=ORIENTED_EDGE ( 'NONE', *, *, #22025, .F. ) ;
#3993=VERTEX_POINT ( 'NONE', #18131 ) ;
#3997=CARTESIAN_POINT ( 'NONE',  ( 9.500000000000000000, 6.470877716354879437E-13, -11.20674201446023410 ) ) ;
#4000=CARTESIAN_POINT ( 'NONE',  ( 7.685661446561619314, 5.583959896779020049, -5.406742014460233392 ) ) ;
#4015=CARTESIAN_POINT ( 'NONE',  ( 6.809999908187194197E-13, -9.988891130263535700, 4.706742014460233214 ) ) ;
#4016=EDGE_LOOP ( 'NONE', ( #12419, #5534, #5554, #11475 ) ) ;
#4021=CARTESIAN_POINT ( 'NONE',  ( 9.499999999999790390, 3.086737114213260025, 8.159589141758143427 ) ) ;
#4029=TOROIDAL_SURFACE ( 'NONE', #2865, 10.49999999999999822, 1.000000000000000000 ) ;
#4032=CARTESIAN_POINT ( 'NONE',  ( 10.49999999999999822, 0.000000000000000000, 2.499999999999999556 ) ) ;
#4059=DIRECTION ( 'NONE',  ( -0.000000000000000000, -0.000000000000000000, -1.000000000000000000 ) ) ;
#4068=ORIENTED_EDGE ( 'NONE', *, *, #5566, .F. ) ;
#4078=CARTESIAN_POINT ( 'NONE',  ( -6.575584573473629568, -6.878740310043753858, -3.499821620521013976 ) ) ;
#4091=CARTESIAN_POINT ( 'NONE',  ( 8.680847955711199049, -2.820578480813074496, 4.533165578109188409 ) ) ;
#4100=ORIENTED_EDGE ( 'NONE', *, *, #15980, .T. ) ;
#4102=CARTESIAN_POINT ( 'NONE',  ( 7.022953521755574080, -5.102474405759714671, -10.43316557810918788 ) ) ;
#4109=AXIS2_PLACEMENT_3D ( 'NONE', #24073, #16635, #3465 ) ;
#4133=CARTESIAN_POINT ( 'NONE',  ( 7.685661446562381371, -5.583959896777971110, 9.859589141758144493 ) ) ;
#4154=CARTESIAN_POINT ( 'NONE',  ( -8.680847955710813579, -2.820578480814258437, -7.733165578109187699 ) ) ;
#4160=CARTESIAN_POINT ( 'NONE',  ( 9.500000000000000000, 6.470877716354879437E-13, 8.059589141758143782 ) ) ;
#4164=FACE_OUTER_BOUND ( 'NONE', #199, .T. ) ;
#4172=CARTESIAN_POINT ( 'NONE',  ( -9.499999999999790390, -3.086737114213257804, -3.159589141758143871 ) ) ;
#4176=EDGE_LOOP ( 'NONE', ( #23806, #10276, #657, #4956 ) ) ;
#4190=CARTESIAN_POINT ( 'NONE',  ( -2.682529543899159208, -8.255977015246598327, 8.033165578109189298 ) ) ;
#4192=DIRECTION ( 'NONE',  ( -0.000000000000000000, -0.000000000000000000, -1.000000000000000000 ) ) ;
#4196=CARTESIAN_POINT ( 'NONE',  ( 9.500000000000000000, 6.470877716354879437E-13, -9.206742014460234103 ) ) ;
#4212=CARTESIAN_POINT ( 'NONE',  ( -7.022953521755574080, 5.102474405759713783, 7.433165578109188765 ) ) ;
#4215=VERTEX_POINT ( 'NONE', #12224 ) ;
#4220=CARTESIAN_POINT ( 'NONE',  ( 8.680847955711199049, -2.820578480813074496, -4.533165578109188409 ) ) ;
#4225=LINE ( 'NONE', #6054, #13883 ) ;
#4234=CARTESIAN_POINT ( 'NONE',  ( 9.500000000000000000, 6.470877716354879437E-13, -8.059589141758143782 ) ) ;
#4238=CARTESIAN_POINT ( 'NONE',  ( -8.680847955711200825, 2.820578480813073607, -9.533165578109189298 ) ) ;
#4240=CARTESIAN_POINT ( 'NONE',  ( -7.685661446561619314, -5.583959896779019161, 8.406742014460233392 ) ) ;
#4243=CARTESIAN_POINT ( 'NONE',  ( -2.682529543900285862, 8.255977015246234174, 11.23316557810918859 ) ) ;
#4249=CARTESIAN_POINT ( 'NONE',  ( 2.935661446561383503, 9.035036904804158553, -10.45958914175814414 ) ) ;
#4254=CARTESIAN_POINT ( 'NONE',  ( -9.500000000000000000, -6.482511860946779655E-13, 6.206742014460234103 ) ) ;
#4263=ORIENTED_EDGE ( 'NONE', *, *, #787, .T. ) ;
#4270=CARTESIAN_POINT ( 'NONE',  ( -2.682529543900285862, 8.255977015246234174, -7.233165578109188587 ) ) ;
#4273=CARTESIAN_POINT ( 'NONE',  ( 2.935661446561383503, 9.035036904804158553, 10.45958914175814414 ) ) ;
#4274=CARTESIAN_POINT ( 'NONE',  ( 7.685661446561619314, 5.583959896779020049, 11.40674201446023517 ) ) ;
#4290=CARTESIAN_POINT ( 'NONE',  ( 3.586653933227395008, -8.272513638839596339, 12.49187530341550278 ) ) ;
#4292=CARTESIAN_POINT ( 'NONE',  ( -9.210377633962220756, 2.035213337404456535, 12.08117117427555165 ) ) ;
#4298=FACE_OUTER_BOUND ( 'NONE', #12334, .T. ) ;
#4299=CARTESIAN_POINT ( 'NONE',  ( -5.871322893123450015, -8.081182679344781405, -6.506742014460233925 ) ) ;
#4302=CARTESIAN_POINT ( 'NONE',  ( -8.680847955711200825, 2.820578480813073607, 11.53316557810918752 ) ) ;
#4305=CARTESIAN_POINT ( 'NONE',  ( 4.029965094393306726E-41, -5.916456789157588541E-28, 21.50000000000009592 ) ) ;
#4310=CARTESIAN_POINT ( 'NONE',  ( 7.685661446562381371, -5.583959896777971110, -9.006742014460233037 ) ) ;
#4311=ORIENTED_EDGE ( 'NONE', *, *, #2396, .T. ) ;
#4315=CARTESIAN_POINT ( 'NONE',  ( -9.499999952843596773, -0.5398784843733258620, -3.499626879768900523 ) ) ;
#4323=FACE_OUTER_BOUND ( 'NONE', #21327, .T. ) ;
#4328=CARTESIAN_POINT ( 'NONE',  ( 5.871322893124553133, -8.081182679343980269, 7.759589141758143072 ) ) ;
#4336=CARTESIAN_POINT ( 'NONE',  ( 7.022953521755574080, -5.102474405759714671, -4.433165578109187877 ) ) ;
#4337=CARTESIAN_POINT ( 'NONE',  ( 7.685661446561619314, 5.583959896779020049, 7.406742014460233392 ) ) ;
#4340=ORIENTED_EDGE ( 'NONE', *, *, #5537, .F. ) ;
#4349=ORIENTED_EDGE ( 'NONE', *, *, #14997, .T. ) ;
#4352=ORIENTED_EDGE ( 'NONE', *, *, #20070, .F. ) ;
#4353=CARTESIAN_POINT ( 'NONE',  ( -1.749335460929532182, -9.337549220493269075, 3.500000000000028866 ) ) ;
#4356=CARTESIAN_POINT ( 'NONE',  ( -9.500000000000000000, -6.482511860946779655E-13, 5.059589141758143782 ) ) ;
#4357=CARTESIAN_POINT ( 'NONE',  ( -5.365059087799948223, 7.384370330706355290, -7.333165578109188232 ) ) ;
#4361=CARTESIAN_POINT ( 'NONE',  ( -8.680847955710813579, -2.820578480814258437, 7.733165578109187699 ) ) ;
#4363=ORIENTED_EDGE ( 'NONE', *, *, #9525, .F. ) ;
#4390=CARTESIAN_POINT ( 'NONE',  ( 9.500000000000000000, 6.470877716354879437E-13, 10.05958914175814378 ) ) ;
#4391=CARTESIAN_POINT ( 'NONE',  ( -6.822232771736903637E-13, 9.988891130263535700, 11.70674201446023410 ) ) ;
#4396=DIRECTION ( 'NONE',  ( 1.000000000000000000, 0.000000000000000000, 0.000000000000000000 ) ) ;
#4410=CARTESIAN_POINT ( 'NONE',  ( -9.500000000000211386, 3.086737114211961064, -2.959589141758143249 ) ) ;
#4413=CARTESIAN_POINT ( 'NONE',  ( -4.277975316535544970, -8.125595891023657202, 12.32532379220425867 ) ) ;
#4425=CARTESIAN_POINT ( 'NONE',  ( -2.935661446562617183, 9.035036904803758873, -3.806742014460233303 ) ) ;
#4428=CARTESIAN_POINT ( 'NONE',  ( 6.222797240145152671E-13, -9.127583699786111282, 6.133165578109188054 ) ) ;
#4432=EDGE_CURVE ( 'NONE', #1630, #5584, #7193, .T. ) ;
#4439=CARTESIAN_POINT ( 'NONE',  ( -2.935661446562617183, 9.035036904803758873, -11.80674201446023375 ) ) ;
#4445=AXIS2_PLACEMENT_3D ( 'NONE', #193, #11247, #20672 ) ;
#4456=CARTESIAN_POINT ( 'NONE',  ( -9.500000000000000000, -6.482511860946779655E-13, 10.20674201446023233 ) ) ;
#4460=CARTESIAN_POINT ( 'NONE',  ( -9.500000000000211386, 3.086737114211961064, 4.959589141758145026 ) ) ;
#4473=CARTESIAN_POINT ( 'NONE',  ( -8.680847955711007202, -5.923547351154968927E-13, -5.633165578109188942 ) ) ;
#4485=EDGE_CURVE ( 'NONE', #17850, #9263, #7923, .T. ) ;
#4494=CARTESIAN_POINT ( 'NONE',  ( 5.365059087798939252, 7.384370330707087149, -10.93316557810918965 ) ) ;
#4501=CARTESIAN_POINT ( 'NONE',  ( 7.022953521754877748, 5.102474405760673903, 8.833165578109190008 ) ) ;
#4505=CARTESIAN_POINT ( 'NONE',  ( 9.499999999999790390, 3.086737114213260025, -11.30674201446023197 ) ) ;
#4527=CARTESIAN_POINT ( 'NONE',  ( -1.374911245008260563, 8.680847955710920161, -3.184419859656034024 ) ) ;
#4530=CARTESIAN_POINT ( 'NONE',  ( -9.500000000000000000, -6.482511860946779655E-13, 11.05958914175814556 ) ) ;
#4534=CARTESIAN_POINT ( 'NONE',  ( -2.682529543899159208, -8.255977015246598327, -12.03316557810918930 ) ) ;
#4551=ORIENTED_EDGE ( 'NONE', *, *, #10744, .F. ) ;
#4556=CARTESIAN_POINT ( 'NONE',  ( -9.499999999999790390, -3.086737114213257804, -8.306742014460233747 ) ) ;
#4559=CARTESIAN_POINT ( 'NONE',  ( -8.680847955710813579, -2.820578480814257549, 11.73316557810918859 ) ) ;
#4573=CARTESIAN_POINT ( 'NONE',  ( -2.808756108234559346, -9.079354608113304081, -3.500655287669418136 ) ) ;
#4576=ORIENTED_EDGE ( 'NONE', *, *, #17794, .T. ) ;
#4578=CARTESIAN_POINT ( 'NONE',  ( -9.500000000000000000, 0.000000000000000000, 12.50000000000000000 ) ) ;
#4591=CARTESIAN_POINT ( 'NONE',  ( 7.685661446561619314, 5.583959896779020049, 10.25958914175814485 ) ) ;
#4595=CARTESIAN_POINT ( 'NONE',  ( -8.680847955711200825, 2.820578480813073607, -5.533165578109187521 ) ) ;
#4612=CARTESIAN_POINT ( 'NONE',  ( 5.365059087799947335, -7.384370330706356178, -8.333165578109188232 ) ) ;
#4616=CARTESIAN_POINT ( 'NONE',  ( -8.680847955710813579, -2.820578480814258437, -11.73316557810918859 ) ) ;
#4617=CARTESIAN_POINT ( 'NONE',  ( -6.233975306307046963E-13, 9.127583699786111282, 11.13316557810918894 ) ) ;
#4622=DIRECTION ( 'NONE',  ( -0.000000000000000000, -0.000000000000000000, 1.000000000000000000 ) ) ;
#4640=CARTESIAN_POINT ( 'NONE',  ( -6.822232771736903637E-13, 9.988891130263535700, -11.70674201446023410 ) ) ;
#4644=CARTESIAN_POINT ( 'NONE',  ( -9.500000000000000000, -6.482511860946779655E-13, 7.059589141758143782 ) ) ;
#4649=FACE_OUTER_BOUND ( 'NONE', #22896, .T. ) ;
#4661=CARTESIAN_POINT ( 'NONE',  ( -5.622572944242077574E-13, 8.680847955711007202, 3.133165578109187610 ) ) ;
#4667=CARTESIAN_POINT ( 'NONE',  ( -7.685661446561619314, -5.583959896779019161, -8.406742014460233392 ) ) ;
#4674=LINE ( 'NONE', #12079, #18912 ) ;
#4681=CARTESIAN_POINT ( 'NONE',  ( -7.685661446561619314, -5.583959896779019161, -12.40674201446023339 ) ) ;
#4696=CARTESIAN_POINT ( 'NONE',  ( -9.500000000000000000, -6.482511860946779655E-13, -5.059589141758143782 ) ) ;
#4699=CARTESIAN_POINT ( 'NONE',  ( 9.500000000000209610, -3.086737114211962396, 7.959589141758143249 ) ) ;
#4718=( BOUNDED_CURVE ( )  B_SPLINE_CURVE ( 2, ( #4696, #16146, #912, #2622, #3099, #15645, #21411, #790, #5057, #21772, #4950 ),
 .UNSPECIFIED., .F., .T. ) 
 B_SPLINE_CURVE_WITH_KNOTS ( ( 3, 2, 2, 2, 2, 3 ),
 ( 0.7000000000000000666, 0.7200000000000000844, 0.7400000000000001021, 0.7600000000000000089, 0.7800000000000000266, 0.8000000000000000444 ),
 .UNSPECIFIED. ) 
 CURVE ( )  GEOMETRIC_REPRESENTATION_ITEM ( )  RATIONAL_B_SPLINE_CURVE ( ( 0.9999999999999997780, 0.9510565162951537532, 1.000000000000000000, 0.9510565162951535312, 1.000000000000000000, 0.9510565162951535312, 1.000000000000000000, 0.9510565162951535312, 1.000000000000000000, 0.9510565162951535312, 1.000000000000000000 ) ) 
 REPRESENTATION_ITEM ( '' )  );
#4726=CARTESIAN_POINT ( 'NONE',  ( -6.233975306307045953E-13, 9.127583699786111282, -9.133165578109188942 ) ) ;
#4730=ORIENTED_EDGE ( 'NONE', *, *, #5566, .T. ) ;
#4731=CARTESIAN_POINT ( 'NONE',  ( 8.680847955711007202, 5.912916378492122225E-13, 12.63316557810918894 ) ) ;
#4734=CARTESIAN_POINT ( 'NONE',  ( -7.561939491010498671, 5.750397476200742375, -11.99999999999999822 ) ) ;
#4736=ORIENTED_EDGE ( 'NONE', *, *, #6012, .T. ) ;
#4762=CARTESIAN_POINT ( 'NONE',  ( 2.935661446562616295, -9.035036904803758873, 12.80674201446023375 ) ) ;
#4763=CARTESIAN_POINT ( 'NONE',  ( 5.871322893124553133, -8.081182679343980269, 12.90674201446023517 ) ) ;
#4773=CARTESIAN_POINT ( 'NONE',  ( 0.000000000000000000, 0.000000000000000000, 12.50000000000000000 ) ) ;
#4780=DIRECTION ( 'NONE',  ( -0.000000000000000000, -0.000000000000000000, -1.000000000000000000 ) ) ;
#4786=CARTESIAN_POINT ( 'NONE',  ( -9.500000000000202505, 3.086737114211975275, 8.959589141758142361 ) ) ;
#4793=VECTOR ( 'NONE', #14520, 1000.000000000000000 ) ;
#4803=CARTESIAN_POINT ( 'NONE',  ( -9.500000000000000000, -6.482511860946779655E-13, 5.059589141758143782 ) ) ;
#4804=EDGE_LOOP ( 'NONE', ( #19717, #368, #1032, #6560 ) ) ;
#4809=AXIS2_PLACEMENT_3D ( 'NONE', #21341, #8752, #19980 ) ;
#4813=VERTEX_POINT ( 'NONE', #9154 ) ;
#4822=CARTESIAN_POINT ( 'NONE',  ( 0.000000000000000000, 0.000000000000000000, 12.50000000000000000 ) ) ;
#4831=CARTESIAN_POINT ( 'NONE',  ( -2.935661446562617183, 9.035036904803758873, 8.659589141758143427 ) ) ;
#4846=CARTESIAN_POINT ( 'NONE',  ( 9.500000000000209610, -3.086737114211962396, 7.959589141758143249 ) ) ;
#4847=CARTESIAN_POINT ( 'NONE',  ( -9.500000000000211386, 3.086737114211961064, 6.106742014460234458 ) ) ;
#4862=CARTESIAN_POINT ( 'NONE',  ( -8.680847955711200825, 2.820578480813073607, -11.53316557810918574 ) ) ;
#4868=CARTESIAN_POINT ( 'NONE',  ( 9.500000000000209610, -3.086737114211962396, -7.959589141758143249 ) ) ;
#4873=CARTESIAN_POINT ( 'NONE',  ( -6.153822176767817416E-13, 9.500000000000000000, 3.499999999999999556 ) ) ;
#4878=CARTESIAN_POINT ( 'NONE',  ( 9.330908268522556170, -1.784418920662232289, 11.99999999999997691 ) ) ;
#4880=EDGE_LOOP ( 'NONE', ( #12878, #6273 ) ) ;
#4886=CARTESIAN_POINT ( 'NONE',  ( 7.022953521755574080, -5.102474405759714671, -4.433165578109187877 ) ) ;
#4892=CARTESIAN_POINT ( 'NONE',  ( 7.685661446562381371, -5.583959896777971110, 3.859589141758143604 ) ) ;
#4893=CARTESIAN_POINT ( 'NONE',  ( -9.500000000000000000, -6.482511860946779655E-13, 4.206742014460233214 ) ) ;
#4894=AXIS2_PLACEMENT_3D ( 'NONE', #3017, #15817, #21188 ) ;
#4896=CIRCLE ( 'NONE', #215, 9.500000000000000000 ) ;
#4908=CARTESIAN_POINT ( 'NONE',  ( 9.500000000000000000, 6.470877716354879437E-13, -10.05958914175814378 ) ) ;
#4911=CARTESIAN_POINT ( 'NONE',  ( -7.685661446561619314, -5.583959896779019161, 11.25958914175814307 ) ) ;
#4921=CARTESIAN_POINT ( 'NONE',  ( 2.935661446561383503, 9.035036904804158553, -6.459589141758144137 ) ) ;
#4923=CARTESIAN_POINT ( 'NONE',  ( -2.682529543900285862, 8.255977015246234174, 3.233165578109188587 ) ) ;
#4928=CIRCLE ( 'NONE', #20491, 9.500000000000000000 ) ;
#4931=CARTESIAN_POINT ( 'NONE',  ( 9.500000000000209610, -3.086737114211962396, -7.106742014460232681 ) ) ;
#4934=CARTESIAN_POINT ( 'NONE',  ( -8.539523583899518044, -3.764097148612461474, -12.19964644692132438 ) ) ;
#4950=CARTESIAN_POINT ( 'NONE',  ( 9.500000000000000000, 6.470877716354879437E-13, -4.059589141758143782 ) ) ;
#4955=EDGE_LOOP ( 'NONE', ( #7820, #6022, #23962, #17042, #4736 ) ) ;
#4956=ORIENTED_EDGE ( 'NONE', *, *, #16147, .F. ) ;
#4972=B_SPLINE_CURVE_WITH_KNOTS ( 'NONE', 3,
 ( #16990, #8559, #21135, #17475, #4934, #10403, #15627, #15774, #14064, #8320, #6386, #892, #21276, #13690, #1257, #13829, #17858, #6514, #23238, #11972, #8678, #10509, #6745, #12086, #21510, #19443 ),
 .UNSPECIFIED., .F., .F.,
 ( 4, 2, 2, 2, 2, 2, 2, 2, 2, 2, 2, 2, 4 ),
 ( 0.006142831834825534729, 0.008468238795519878598, 0.01079364575621422247, 0.01195634923656139527, 0.01311905271690856807, 0.01428175619725574087, 0.01544445967760291367, 0.01660716315795008474, 0.01776986663829725754, 0.01893257011864443035, 0.02009527359899160315, 0.02242068055968594181, 0.02474608752038028742 ),
 .UNSPECIFIED. ) ;
#4977=CARTESIAN_POINT ( 'NONE',  ( -5.622572944242077574E-13, 8.680847955711007202, -3.133165578109187610 ) ) ;
#4981=CARTESIAN_POINT ( 'NONE',  ( -6.233975306307046963E-13, 9.127583699786111282, 5.133165578109188054 ) ) ;
#4986=CARTESIAN_POINT ( 'NONE',  ( -6.249999999999999112, -10.82531754730548279, 2.500000000000000000 ) ) ;
#4987=CARTESIAN_POINT ( 'NONE',  ( -7.685661446562381371, 5.583959896777970222, -4.859589141758143604 ) ) ;
#4988=CARTESIAN_POINT ( 'NONE',  ( -6.153822176767817416E-13, 9.500000000000000000, 3.186529713919380669 ) ) ;
#5006=CARTESIAN_POINT ( 'NONE',  ( 9.500000000000000000, 6.470877716354879437E-13, 6.059589141758143782 ) ) ;
#5007=CARTESIAN_POINT ( 'NONE',  ( -5.871322893124554021, 8.081182679343978492, 5.906742014460233392 ) ) ;
#5016=CARTESIAN_POINT ( 'NONE',  ( -9.500000000000000000, -6.482511860946779655E-13, -4.206742014460233214 ) ) ;
#5017=ADVANCED_FACE ( 'NONE', ( #4164 ), #12952, .F. ) ;
#5034=CARTESIAN_POINT ( 'NONE',  ( -8.680847955711200825, 2.820578480813073607, 3.533165578109187965 ) ) ;
#5038=CARTESIAN_POINT ( 'NONE',  ( 8.840695694414906214, -0.6121865488562178159, -12.50000000000000000 ) ) ;
#5046=CARTESIAN_POINT ( 'NONE',  ( -6.822232771736903637E-13, 9.988891130263535700, -7.706742014460232326 ) ) ;
#5048=ORIENTED_EDGE ( 'NONE', *, *, #18882, .T. ) ;
#5053=DIRECTION ( 'NONE',  ( 1.000000000000000000, 0.000000000000000000, 0.000000000000000000 ) ) ;
#5057=CARTESIAN_POINT ( 'NONE',  ( 7.685661446561619314, 5.583959896779020049, -4.259589141758143960 ) ) ;
#5066=VERTEX_POINT ( 'NONE', #23452 ) ;
#5070=CARTESIAN_POINT ( 'NONE',  ( 7.685661446562381371, -5.583959896777971110, -9.006742014460233037 ) ) ;
#5071=CARTESIAN_POINT ( 'NONE',  ( 7.685661446561619314, 5.583959896779020049, 5.406742014460233392 ) ) ;
#5072=CARTESIAN_POINT ( 'NONE',  ( -2.935661446561384391, -9.035036904804158553, 4.606742014460233570 ) ) ;
#5077=CARTESIAN_POINT ( 'NONE',  ( 8.680847955711007202, 5.912916378492122225E-13, -4.633165578109188942 ) ) ;
#5082=DIRECTION ( 'NONE',  ( 1.000000000000000000, 0.000000000000000000, -0.000000000000000000 ) ) ;
#5087=CARTESIAN_POINT ( 'NONE',  ( -7.685661446562381371, 5.583959896777970222, -6.859589141758143604 ) ) ;
#5096=VERTEX_POINT ( 'NONE', #17956 ) ;
#5101=VERTEX_POINT ( 'NONE', #3310 ) ;
#5107=CARTESIAN_POINT ( 'NONE',  ( 5.871322893124553133, -8.081182679343980269, 5.759589141758144848 ) ) ;
#5109=CARTESIAN_POINT ( 'NONE',  ( 5.871322893123449127, 8.081182679344781405, 9.506742014460231260 ) ) ;
#5122=CARTESIAN_POINT ( 'NONE',  ( -6.822232771736904647E-13, 9.988891130263535700, 10.55958914175814201 ) ) ;
#5124=CARTESIAN_POINT ( 'NONE',  ( -10.49999999999999822, 1.285879139104720633E-15, -3.499999999999999556 ) ) ;
#5125=CARTESIAN_POINT ( 'NONE',  ( -5.976739099259236459E-13, 9.226949318570335734, -3.515549869009883643 ) ) ;
#5135=EDGE_CURVE ( 'NONE', #9659, #18218, #14676, .T. ) ;
#5137=CARTESIAN_POINT ( 'NONE',  ( 8.511897654723162177, -2.099402067127676297, -12.50000000000000000 ) ) ;
#5146=CARTESIAN_POINT ( 'NONE',  ( -6.153822176767817416E-13, 9.500000000000000000, -3.706742014460232326 ) ) ;
#5165=CARTESIAN_POINT ( 'NONE',  ( -1.504652183083727168, 9.499999999999904077, -3.757996296007079184 ) ) ;
#5183=CARTESIAN_POINT ( 'NONE',  ( -5.871322893124554021, 8.081182679343978492, 3.906742014460231616 ) ) ;
#5191=ADVANCED_FACE ( 'NONE', ( #14756 ), #3898, .T. ) ;
#5194=CARTESIAN_POINT ( 'NONE',  ( 8.680847955711007202, 5.912916378492122225E-13, 10.63316557810918894 ) ) ;
#5195=VERTEX_POINT ( 'NONE', #22565 ) ;
#5203=CARTESIAN_POINT ( 'NONE',  ( -6.822232771736903637E-13, 9.988891130263535700, -8.559589141758145558 ) ) ;
#5232=CARTESIAN_POINT ( 'NONE',  ( 9.500000000000209610, -3.086737114211962396, 9.106742014460232681 ) ) ;
#5233=CARTESIAN_POINT ( 'NONE',  ( 9.500000000000209610, -3.086737114211962396, 5.106742014460234458 ) ) ;
#5252=CARTESIAN_POINT ( 'NONE',  ( 9.499999999999790390, 3.086737114213260025, 10.15958914175814343 ) ) ;
#5253=CARTESIAN_POINT ( 'NONE',  ( -1.253758815873204258, 9.437348638249524413, -3.501083568643978960 ) ) ;
#5254=CARTESIAN_POINT ( 'NONE',  ( 7.685661446562381371, -5.583959896777971110, -11.85958914175814449 ) ) ;
#5257=CARTESIAN_POINT ( 'NONE',  ( -2.682529543900285862, 8.255977015246234174, -9.233165578109188587 ) ) ;
#5266=CARTESIAN_POINT ( 'NONE',  ( 8.871028110654306076, 6.042456644462176420E-13, -12.50000000000000000 ) ) ;
#5267=CIRCLE ( 'NONE', #6437, 9.500000000000000000 ) ;
#5275=CARTESIAN_POINT ( 'NONE',  ( 9.500000000000000000, 6.470877716354879437E-13, -5.206742014460234103 ) ) ;
#5279=CARTESIAN_POINT ( 'NONE',  ( -6.153822176767817416E-13, 9.500000000000000000, -3.706742014460231882 ) ) ;
#5280=ADVANCED_FACE ( 'NONE', ( #5743 ), #18560, .F. ) ;
#5308=EDGE_CURVE ( 'NONE', #5096, #3802, #24042, .T. ) ;
#5315=VECTOR ( 'NONE', #112, 1000.000000000000000 ) ;
#5316=CARTESIAN_POINT ( 'NONE',  ( -8.585126421212056158, 3.981676010260311482, 12.03996617712741646 ) ) ;
#5317=DIRECTION ( 'NONE',  ( -0.000000000000000000, -0.000000000000000000, 1.000000000000000000 ) ) ;
#5320=VECTOR ( 'NONE', #20138, 1000.000000000000227 ) ;
#5325=CARTESIAN_POINT ( 'NONE',  ( -8.680847955710813579, -2.820578480814258437, 11.73316557810918859 ) ) ;
#5333=CARTESIAN_POINT ( 'NONE',  ( 2.935661446561383503, 9.035036904804158553, -8.459589141758144137 ) ) ;
#5354=CARTESIAN_POINT ( 'NONE',  ( 5.871322893124553133, -8.081182679343980269, 10.90674201446023339 ) ) ;
#5355=CARTESIAN_POINT ( 'NONE',  ( 7.685661446562381371, -5.583959896777971110, 7.006742014460233037 ) ) ;
#5363=CARTESIAN_POINT ( 'NONE',  ( 5.871322893124551356, -8.081182679343980269, -4.906742014460232504 ) ) ;
#5371=VERTEX_POINT ( 'NONE', #18839 ) ;
#5378=CARTESIAN_POINT ( 'NONE',  ( 6.222797240145152671E-13, -9.127583699786111282, -10.13316557810918894 ) ) ;
#5380=CARTESIAN_POINT ( 'NONE',  ( 0.000000000000000000, 0.000000000000000000, 3.499999999999999556 ) ) ;
#5383=CARTESIAN_POINT ( 'NONE',  ( 6.250000000000000000, 10.82531754730548279, 2.500000000000000000 ) ) ;
#5388=CARTESIAN_POINT ( 'NONE',  ( -9.500000000000000000, 0.000000000000000000, 12.50000000000000000 ) ) ;
#5395=CARTESIAN_POINT ( 'NONE',  ( 9.500000000000209610, -3.086737114211962396, -7.959589141758143249 ) ) ;
#5407=ORIENTED_EDGE ( 'NONE', *, *, #3127, .T. ) ;
#5411=CARTESIAN_POINT ( 'NONE',  ( -7.022953521755574080, 5.102474405759713783, 3.433165578109189209 ) ) ;
#5428=CARTESIAN_POINT ( 'NONE',  ( 5.871322893124551356, -8.081182679343980269, 10.90674201446023339 ) ) ;
#5437=CARTESIAN_POINT ( 'NONE',  ( 8.680847955711199049, -2.820578480813074496, 8.533165578109187521 ) ) ;
#5447=CARTESIAN_POINT ( 'NONE',  ( -8.680847955711007202, -5.923547351154968927E-13, -11.63316557810919072 ) ) ;
#5449=CARTESIAN_POINT ( 'NONE',  ( -6.153822176767817416E-13, 9.500000000000000000, 3.706742014460231882 ) ) ;
#5459=LINE ( 'NONE', #12880, #7810 ) ;
#5462=EDGE_CURVE ( 'NONE', #19051, #17352, #22619, .T. ) ;
#5469=CARTESIAN_POINT ( 'NONE',  ( 7.685661446561619314, 5.583959896779020049, 7.406742014460233392 ) ) ;
#5470=EDGE_CURVE ( 'NONE', #17358, #11482, #15043, .T. ) ;
#5478=DIRECTION ( 'NONE',  ( 1.000000000000000000, 0.000000000000000000, 0.000000000000000000 ) ) ;
#5481=LINE ( 'NONE', #16701, #9005 ) ;
#5483=CARTESIAN_POINT ( 'NONE',  ( -9.499999999999962697, -8.297908579805900909E-07, -3.500254135480583617 ) ) ;
#5485=( BOUNDED_CURVE ( )  B_SPLINE_CURVE ( 2, ( #17308, #13647, #7894, #16805, #2420, #4015, #21085, #9845, #19033, #17173, #609 ),
 .UNSPECIFIED., .F., .T. ) 
 B_SPLINE_CURVE_WITH_KNOTS ( ( 3, 2, 2, 2, 2, 3 ),
 ( 0.8000000000000000444, 0.8199999999999999512, 0.8399999999999999689, 0.8599999999999999867, 0.8800000000000000044, 0.9000000000000000222 ),
 .UNSPECIFIED. ) 
 CURVE ( )  GEOMETRIC_REPRESENTATION_ITEM ( )  RATIONAL_B_SPLINE_CURVE ( ( 1.000000000000000000, 0.9510565162951535312, 1.000000000000000000, 0.9510565162951535312, 1.000000000000000000, 0.9510565162951535312, 1.000000000000000000, 0.9510565162951535312, 1.000000000000000000, 0.9510565162951535312, 1.000000000000000000 ) ) 
 REPRESENTATION_ITEM ( '' )  );
#5500=CARTESIAN_POINT ( 'NONE',  ( 9.500000000000000000, 6.470877716354879437E-13, -10.05958914175814378 ) ) ;
#5514=CARTESIAN_POINT ( 'NONE',  ( 0.000000000000000000, 0.000000000000000000, 12.50000000000000000 ) ) ;
#5516=CARTESIAN_POINT ( 'NONE',  ( 7.022953521755574080, -5.102474405759714671, 12.43316557810918788 ) ) ;
#5520=CARTESIAN_POINT ( 'NONE',  ( -5.365059087799947335, 7.384370330706355290, 5.333165578109189120 ) ) ;
#5526=CARTESIAN_POINT ( 'NONE',  ( 7.685661446561619314, 5.583959896779020049, 9.406742014460235168 ) ) ;
#5528=CONICAL_SURFACE ( 'NONE', #14105, 9.500000000000000000, 0.7853981633974500554 ) ;
#5534=ORIENTED_EDGE ( 'NONE', *, *, #1808, .F. ) ;
#5537=EDGE_CURVE ( 'NONE', #6271, #19427, #16169, .T. ) ;
#5545=ORIENTED_EDGE ( 'NONE', *, *, #988, .F. ) ;
#5546=CARTESIAN_POINT ( 'NONE',  ( -2.682529543899159208, -8.255977015246598327, 10.03316557810918930 ) ) ;
#5554=ORIENTED_EDGE ( 'NONE', *, *, #5470, .F. ) ;
#5558=CARTESIAN_POINT ( 'NONE',  ( -5.365059087799947335, 7.384370330706355290, -9.333165578109190008 ) ) ;
#5566=EDGE_CURVE ( 'NONE', #5066, #8782, #8464, .T. ) ;
#5584=VERTEX_POINT ( 'NONE', #8193 ) ;
#5587=CARTESIAN_POINT ( 'NONE',  ( 7.685661446562381371, -5.583959896777971110, 11.00674201446023304 ) ) ;
#5599=VECTOR ( 'NONE', #9773, 1000.000000000000114 ) ;
#5629=EDGE_CURVE ( 'NONE', #5195, #9278, #2357, .T. ) ;
#5632=CARTESIAN_POINT ( 'NONE',  ( -7.685661446562381371, 5.583959896777970222, -6.859589141758143604 ) ) ;
#5639=ORIENTED_EDGE ( 'NONE', *, *, #17052, .F. ) ;
#5652=VECTOR ( 'NONE', #15907, 1000.000000000000000 ) ;
#5674=CARTESIAN_POINT ( 'NONE',  ( -5.622572944242077574E-13, 8.680847955711007202, -3.133165578109187610 ) ) ;
#5682=CIRCLE ( 'NONE', #17354, 10.49999999999999822 ) ;
#5683=AXIS2_PLACEMENT_3D ( 'NONE', #6760, #14190, #16501 ) ;
#5685=CARTESIAN_POINT ( 'NONE',  ( -6.233975306307046963E-13, 9.127583699786111282, 7.133165578109187166 ) ) ;
#5693=CARTESIAN_POINT ( 'NONE',  ( -8.680847955711200825, 2.820578480813073607, -9.533165578109187521 ) ) ;
#5711=CARTESIAN_POINT ( 'NONE',  ( -9.500000000000000000, -6.482511860946779655E-13, -7.059589141758143782 ) ) ;
#5726=CARTESIAN_POINT ( 'NONE',  ( 7.937578510445358226, -3.514536757623690999, 12.49999999999999112 ) ) ;
#5742=ADVANCED_FACE ( 'NONE', ( #8689 ), #4029, .F. ) ;
#5743=FACE_OUTER_BOUND ( 'NONE', #21744, .T. ) ;
#5755=CARTESIAN_POINT ( 'NONE',  ( -9.500000000000000000, -6.482511860946779655E-13, -9.059589141758143782 ) ) ;
#5781=CARTESIAN_POINT ( 'NONE',  ( 9.500000000000000000, 6.470877716354879437E-13, 9.206742014460234103 ) ) ;
#5789=CARTESIAN_POINT ( 'NONE',  ( -6.249999999999999112, -10.82531754730548279, 2.500000000000000000 ) ) ;
#5795=CARTESIAN_POINT ( 'NONE',  ( -8.680847955711200825, 2.820578480813073607, 7.533165578109188409 ) ) ;
#5802=CARTESIAN_POINT ( 'NONE',  ( -7.685661446562381371, 5.583959896777970222, -2.859589141758144493 ) ) ;
#5817=CARTESIAN_POINT ( 'NONE',  ( 6.809999908187194197E-13, -9.988891130263535700, -5.559589141758142894 ) ) ;
#5819=CARTESIAN_POINT ( 'NONE',  ( -5.365059087799948223, 7.384370330706355290, -11.33316557810918646 ) ) ;
#5836=CARTESIAN_POINT ( 'NONE',  ( -5.871322893124554021, 8.081182679343978492, -5.906742014460232504 ) ) ;
#5841=DIRECTION ( 'NONE',  ( 0.000000000000000000, 1.000000000000000000, 0.000000000000000000 ) ) ;
#5852=CARTESIAN_POINT ( 'NONE',  ( -5.871322893123450015, -8.081182679344781405, 9.359589141758146269 ) ) ;
#5859=CARTESIAN_POINT ( 'NONE',  ( 5.871322893124553133, -8.081182679343980269, -9.759589141758143072 ) ) ;
#5862=CARTESIAN_POINT ( 'NONE',  ( 7.685661446561619314, 5.583959896779020049, 11.40674201446023517 ) ) ;
#5886=ADVANCED_FACE ( 'NONE', ( #9282 ), #15012, .T. ) ;
#5907=EDGE_LOOP ( 'NONE', ( #13914, #16950, #22525, #10405, #4551, #17152 ) ) ;
#5908=CARTESIAN_POINT ( 'NONE',  ( -5.365059087798939252, -7.384370330707086261, 5.933165578109187877 ) ) ;
#5915=CARTESIAN_POINT ( 'NONE',  ( -9.500000000000000000, -6.482511860946779655E-13, -3.059589141758143338 ) ) ;
#5928=CARTESIAN_POINT ( 'NONE',  ( -2.935661446561384391, -9.035036904804158553, -7.459589141758144137 ) ) ;
#5937=CARTESIAN_POINT ( 'NONE',  ( -6.233975306307045953E-13, 9.127583699786111282, -11.13316557810918894 ) ) ;
#5938=VECTOR ( 'NONE', #1969, 999.9999999999998863 ) ;
#5971=ORIENTED_EDGE ( 'NONE', *, *, #9291, .T. ) ;
#5974=CARTESIAN_POINT ( 'NONE',  ( -9.500000000000211386, 3.086737114211961064, 10.95958914175814414 ) ) ;
#5978=CARTESIAN_POINT ( 'NONE',  ( 0.000000000000000000, 0.000000000000000000, 0.000000000000000000 ) ) ;
#5983=CARTESIAN_POINT ( 'NONE',  ( 4.159489978096820195, -7.970633069177153196, -12.49999999999999822 ) ) ;
#5990=ORIENTED_EDGE ( 'NONE', *, *, #12020, .F. ) ;
#6004=DIRECTION ( 'NONE',  ( -1.000000000000000000, 0.000000000000000000, 0.000000000000000000 ) ) ;
#6005=CARTESIAN_POINT ( 'NONE',  ( -7.022953521754877748, -5.102474405760673015, 9.833165578109188232 ) ) ;
#6012=EDGE_CURVE ( 'NONE', #10046, #2012, #22692, .T. ) ;
#6016=CARTESIAN_POINT ( 'NONE',  ( -7.685661446561619314, -5.583959896779019161, -10.40674201446023339 ) ) ;
#6017=EDGE_LOOP ( 'NONE', ( #12439, #19647, #16687, #10708 ) ) ;
#6021=CARTESIAN_POINT ( 'NONE',  ( -8.512326165839379399, -4.253244381378425309, -3.501722726248814421 ) ) ;
#6022=ORIENTED_EDGE ( 'NONE', *, *, #24074, .T. ) ;
#6036=CARTESIAN_POINT ( 'NONE',  ( -2.935661446561384391, -9.035036904804158553, 11.45958914175814414 ) ) ;
#6037=EDGE_CURVE ( 'NONE', #22998, #14019, #19516, .T. ) ;
#6040=CARTESIAN_POINT ( 'NONE',  ( 9.500000000000200728, -3.086737114211976607, 5.959589141758144137 ) ) ;
#6054=CARTESIAN_POINT ( 'NONE',  ( 12.50000000000000178, 5.755434930044642846E-15, 2.500000000000000000 ) ) ;
#6062=CARTESIAN_POINT ( 'NONE',  ( 2.935661446562616295, -9.035036904803758873, -7.659589141758144315 ) ) ;
#6071=CARTESIAN_POINT ( 'NONE',  ( 8.680847955710813579, 2.820578480814259326, 10.73316557810918503 ) ) ;
#6078=CARTESIAN_POINT ( 'NONE',  ( -5.871322893124554021, 8.081182679343978492, -10.75958914175814130 ) ) ;
#6082=CARTESIAN_POINT ( 'NONE',  ( 6.507347684474039440, -5.969953219653517884, 12.49999999999999467 ) ) ;
#6084=CARTESIAN_POINT ( 'NONE',  ( -2.935661446561384391, -9.035036904804158553, 6.606742014460233570 ) ) ;
#6089=DIRECTION ( 'NONE',  ( 0.000000000000000000, -0.000000000000000000, 1.000000000000000000 ) ) ;
#6099=CARTESIAN_POINT ( 'NONE',  ( -9.499999999999790390, -3.086737114213257804, 12.30674201446023197 ) ) ;
#6107=CARTESIAN_POINT ( 'NONE',  ( 7.524481829284253465, -4.467250836390667779, -12.49999999999999645 ) ) ;
#6110=DIRECTION ( 'NONE',  ( 0.000000000000000000, -1.000000000000000000, 0.000000000000000000 ) ) ;
#6121=DIRECTION ( 'NONE',  ( -0.000000000000000000, -0.000000000000000000, -1.000000000000000000 ) ) ;
#6124=CARTESIAN_POINT ( 'NONE',  ( 6.809999908187194197E-13, -9.988891130263535700, -6.706742014460232326 ) ) ;
#6126=DIRECTION ( 'NONE',  ( -0.000000000000000000, -0.000000000000000000, -1.000000000000000000 ) ) ;
#6128=CARTESIAN_POINT ( 'NONE',  ( -7.022953521754877748, -5.102474405760673015, 11.83316557810918823 ) ) ;
#6138=CARTESIAN_POINT ( 'NONE',  ( -2.935661446562617183, 9.035036904803758873, -9.806742014460233747 ) ) ;
#6143=CARTESIAN_POINT ( 'NONE',  ( -9.453640352822144877, -1.087149405126631496, -3.499473001065527722 ) ) ;
#6148=CARTESIAN_POINT ( 'NONE',  ( 12.50000000000000178, 5.755434930044642846E-15, 2.500000000000000000 ) ) ;
#6150=PLANE ( 'NONE',  #16886 ) ;
#6158=CARTESIAN_POINT ( 'NONE',  ( -6.233975306307046963E-13, 9.127583699786111282, 5.133165578109188054 ) ) ;
#6164=CARTESIAN_POINT ( 'NONE',  ( -6.233975306307046963E-13, 9.127583699786111282, -7.133165578109187166 ) ) ;
#6166=EDGE_LOOP ( 'NONE', ( #12946, #11559, #15013, #1976, #3488 ) ) ;
#6185=CARTESIAN_POINT ( 'NONE',  ( 7.022953521755574080, -5.102474405759714671, -6.433165578109188765 ) ) ;
#6191=CARTESIAN_POINT ( 'NONE',  ( -2.682529543899159208, -8.255977015246598327, 8.033165578109189298 ) ) ;
#6197=CARTESIAN_POINT ( 'NONE',  ( 7.685661446562381371, -5.583959896777971110, -11.00674201446023304 ) ) ;
#6203=EDGE_CURVE ( 'NONE', #14137, #17696, #12167, .T. ) ;
#6214=CARTESIAN_POINT ( 'NONE',  ( 2.935661446562616295, -9.035036904803758873, 11.65958914175814520 ) ) ;
#6225=FACE_BOUND ( 'NONE', #10825, .T. ) ;
#6227=CARTESIAN_POINT ( 'NONE',  ( -3.567126290007196499, -8.444559533753546177, 12.34121854105286786 ) ) ;
#6228=CARTESIAN_POINT ( 'NONE',  ( 5.871322893124551356, -8.081182679343980269, 11.75958914175814485 ) ) ;
#6230=VECTOR ( 'NONE', #16705, 1000.000000000000000 ) ;
#6234=CARTESIAN_POINT ( 'NONE',  ( -7.685661446562381371, 5.583959896777970222, -8.006742014460233037 ) ) ;
#6235=CARTESIAN_POINT ( 'NONE',  ( -2.935661446562617183, 9.035036904803758873, 8.659589141758143427 ) ) ;
#6238=CARTESIAN_POINT ( 'NONE',  ( 7.685661446561619314, 5.583959896779020049, -7.406742014460233392 ) ) ;
#6241=CARTESIAN_POINT ( 'NONE',  ( -5.365059087798940141, -7.384370330707086261, 7.933165578109187877 ) ) ;
#6249=CARTESIAN_POINT ( 'NONE',  ( -9.500000000000211386, 3.086737114211961064, -8.106742014460232681 ) ) ;
#6259=( BOUNDED_CURVE ( )  B_SPLINE_CURVE ( 2, ( #10161, #13260, #17619, #5836, #240, #20716, #11554, #13144, #4000, #15330, #19593 ),
 .UNSPECIFIED., .F., .T. ) 
 B_SPLINE_CURVE_WITH_KNOTS ( ( 3, 2, 2, 2, 2, 3 ),
 ( 0.7000000000000000666, 0.7200000000000000844, 0.7400000000000001021, 0.7600000000000000089, 0.7800000000000000266, 0.8000000000000000444 ),
 .UNSPECIFIED. ) 
 CURVE ( )  GEOMETRIC_REPRESENTATION_ITEM ( )  RATIONAL_B_SPLINE_CURVE ( ( 0.9999999999999997780, 0.9510565162951537532, 1.000000000000000000, 0.9510565162951535312, 1.000000000000000000, 0.9510565162951535312, 1.000000000000000000, 0.9510565162951535312, 1.000000000000000000, 0.9510565162951535312, 1.000000000000000000 ) ) 
 REPRESENTATION_ITEM ( '' )  );
#6261=ORIENTED_EDGE ( 'NONE', *, *, #5308, .T. ) ;
#6267=CARTESIAN_POINT ( 'NONE',  ( 9.500000000000000000, 6.470877716354879437E-13, 10.05958914175814378 ) ) ;
#6270=EDGE_LOOP ( 'NONE', ( #22100, #402, #5407, #9902 ) ) ;
#6271=VERTEX_POINT ( 'NONE', #8925 ) ;
#6273=ORIENTED_EDGE ( 'NONE', *, *, #13659, .F. ) ;
#6275=CARTESIAN_POINT ( 'NONE',  ( -8.680847955711007202, -5.923547351154968927E-13, -3.633165578109188054 ) ) ;
#6293=CARTESIAN_POINT ( 'NONE',  ( -2.682529543900285862, 8.255977015246234174, -5.233165578109188587 ) ) ;
#6299=CARTESIAN_POINT ( 'NONE',  ( -8.680847955711200825, 2.820578480813073607, 11.53316557810918574 ) ) ;
#6305=CARTESIAN_POINT ( 'NONE',  ( -9.500000000000211386, 3.086737114211961064, -10.95958914175814414 ) ) ;
#6306=CARTESIAN_POINT ( 'NONE',  ( -9.499999999999799272, -3.086737114213243593, -10.30674201446023019 ) ) ;
#6308=CARTESIAN_POINT ( 'NONE',  ( 6.809999908187194197E-13, -9.988891130263535700, 6.706742014460232326 ) ) ;
#6320=DIRECTION ( 'NONE',  ( 1.000000000000000000, 0.000000000000000000, 0.000000000000000000 ) ) ;
#6331=CARTESIAN_POINT ( 'NONE',  ( 2.935661446562616295, -9.035036904803758873, 12.80674201446023375 ) ) ;
#6354=CARTESIAN_POINT ( 'NONE',  ( -0.9419320875194652221, -9.063431280198074091, 12.39598011385684373 ) ) ;
#6361=LINE ( 'NONE', #13804, #3624 ) ;
#6366=CARTESIAN_POINT ( 'NONE',  ( 2.935661446562616295, -9.035036904803758873, -4.806742014460232859 ) ) ;
#6369=CARTESIAN_POINT ( 'NONE',  ( -7.022953521755574080, 5.102474405759713783, 11.43316557810918965 ) ) ;
#6382=CARTESIAN_POINT ( 'NONE',  ( 9.499999999999790390, 3.086737114213260025, -11.30674201446023019 ) ) ;
#6386=CARTESIAN_POINT ( 'NONE',  ( -6.218841404285884167, -6.822046258104109029, -12.27696493876690909 ) ) ;
#6403=CARTESIAN_POINT ( 'NONE',  ( -9.500000000000000000, -6.482511860946779655E-13, 9.059589141758143782 ) ) ;
#6425=CARTESIAN_POINT ( 'NONE',  ( 7.685661446562381371, -5.583959896777971110, 7.859589141758143604 ) ) ;
#6432=DIRECTION ( 'NONE',  ( 0.000000000000000000, 0.000000000000000000, 1.000000000000000000 ) ) ;
#6435=CARTESIAN_POINT ( 'NONE',  ( 7.022953521754877748, 5.102474405760673903, -6.833165578109188232 ) ) ;
#6437=AXIS2_PLACEMENT_3D ( 'NONE', #12146, #4622, #21693 ) ;
#6463=CARTESIAN_POINT ( 'NONE',  ( -5.871322893124554021, 8.081182679343978492, -11.90674201446023339 ) ) ;
#6467=CARTESIAN_POINT ( 'NONE',  ( -7.685661446561619314, -5.583959896779019161, 7.259589141758143960 ) ) ;
#6472=EDGE_LOOP ( 'NONE', ( #9918, #23379, #22656 ) ) ;
#6476=CARTESIAN_POINT ( 'NONE',  ( -9.500000000000000000, -6.482511860946779655E-13, 3.059589141758143338 ) ) ;
#6477=CARTESIAN_POINT ( 'NONE',  ( -6.822232771736904647E-13, 9.988891130263535700, 6.559589141758143782 ) ) ;
#6478=CARTESIAN_POINT ( 'NONE',  ( 5.021738411795491075, -7.393327316361923529, -12.50000000000000178 ) ) ;
#6482=DIRECTION ( 'NONE',  ( 0.000000000000000000, 0.000000000000000000, -1.000000000000000000 ) ) ;
#6498=CARTESIAN_POINT ( 'NONE',  ( 5.871322893123449127, 8.081182679344781405, -5.506742014460233925 ) ) ;
#6501=CARTESIAN_POINT ( 'NONE',  ( 2.682529543900284974, -8.255977015246234174, 8.233165578109190363 ) ) ;
#6509=CARTESIAN_POINT ( 'NONE',  ( -9.499999999999799272, -3.086737114213243593, 5.159589141758141650 ) ) ;
#6513=CARTESIAN_POINT ( 'NONE',  ( 2.935661446562616295, -9.035036904803758873, -10.80674201446023197 ) ) ;
#6514=CARTESIAN_POINT ( 'NONE',  ( -2.467881479971292258, -8.804721359397014169, -12.36426617047028387 ) ) ;
#6525=DIRECTION ( 'NONE',  ( 1.000000000000000000, 0.000000000000000000, 0.000000000000000000 ) ) ;
#6534=CARTESIAN_POINT ( 'NONE',  ( -9.499999999999790390, -3.086737114213257804, 5.159589141758141650 ) ) ;
#6537=ORIENTED_EDGE ( 'NONE', *, *, #23603, .F. ) ;
#6542=CARTESIAN_POINT ( 'NONE',  ( -9.500000000000000000, 0.000000000000000000, 12.50000000000000000 ) ) ;
#6549=CARTESIAN_POINT ( 'NONE',  ( -9.500000000000000000, -6.482511860946779655E-13, 7.059589141758143782 ) ) ;
#6550=CARTESIAN_POINT ( 'NONE',  ( 2.935661446562616295, -9.035036904803758873, 6.806742014460233747 ) ) ;
#6557=CARTESIAN_POINT ( 'NONE',  ( 8.680847955710813579, 2.820578480814259326, -4.733165578109188587 ) ) ;
#6558=EDGE_CURVE ( 'NONE', #5096, #13543, #13602, .T. ) ;
#6560=ORIENTED_EDGE ( 'NONE', *, *, #9291, .F. ) ;
#6562=CARTESIAN_POINT ( 'NONE',  ( 2.682529543899157876, 8.255977015246598327, -11.03316557810918752 ) ) ;
#6563=CARTESIAN_POINT ( 'NONE',  ( 8.680847955710813579, 2.820578480814259326, 8.733165578109185034 ) ) ;
#6585=EDGE_CURVE ( 'NONE', #13405, #2012, #6361, .T. ) ;
#6589=CARTESIAN_POINT ( 'NONE',  ( -7.685661446561619314, -5.583959896779019161, -12.40674201446023339 ) ) ;
#6592=CARTESIAN_POINT ( 'NONE',  ( 9.500000000000000000, 6.470877716354879437E-13, 4.059589141758143782 ) ) ;
#6593=CARTESIAN_POINT ( 'NONE',  ( 7.937578510445243651, -3.514536757623948127, -12.49999999999998046 ) ) ;
#6595=FACE_OUTER_BOUND ( 'NONE', #2833, .T. ) ;
#6606=CARTESIAN_POINT ( 'NONE',  ( 9.500000000000000000, 1.163414459189985485E-15, 12.50000000000000000 ) ) ;
#6619=DIRECTION ( 'NONE',  ( 1.000000000000000000, 0.000000000000000000, 0.000000000000000000 ) ) ;
#6621=ADVANCED_FACE ( 'NONE', ( #2334 ), #11957, .T. ) ;
#6645=CARTESIAN_POINT ( 'NONE',  ( -6.822232771736903637E-13, 9.988891130263535700, 4.559589141758142894 ) ) ;
#6652=CARTESIAN_POINT ( 'NONE',  ( -2.935661446562617183, 9.035036904803758873, 7.806742014460233747 ) ) ;
#6663=CARTESIAN_POINT ( 'NONE',  ( -5.871322893124554021, 8.081182679343978492, 5.906742014460233392 ) ) ;
#6670=CARTESIAN_POINT ( 'NONE',  ( 2.682529543899157876, 8.255977015246598327, -11.03316557810918752 ) ) ;
#6678=DIRECTION ( 'NONE',  ( 1.000000000000000000, 0.000000000000000000, -0.000000000000000000 ) ) ;
#6683=CARTESIAN_POINT ( 'NONE',  ( -5.871322893124554021, 8.081182679343978492, -4.759589141758144848 ) ) ;
#6687=CARTESIAN_POINT ( 'NONE',  ( 8.417661073264101290, -2.391602252564205777, 12.49999999999999822 ) ) ;
#6691=CARTESIAN_POINT ( 'NONE',  ( -12.50000000000000178, 1.672973214995343413E-15, 2.500000000000000000 ) ) ;
#6692=DIRECTION ( 'NONE',  ( 1.000000000000000000, 6.485355633664481337E-14, 0.000000000000000000 ) ) ;
#6703=CARTESIAN_POINT ( 'NONE',  ( -5.871322893123450015, -8.081182679344781405, 7.359589141758143604 ) ) ;
#6704=CARTESIAN_POINT ( 'NONE',  ( -6.822232771736903637E-13, 9.988891130263535700, 5.706742014460234103 ) ) ;
#6717=ORIENTED_EDGE ( 'NONE', *, *, #12208, .T. ) ;
#6720=CARTESIAN_POINT ( 'NONE',  ( -9.500000000000000000, -6.482511860946779655E-13, 11.05958914175814556 ) ) ;
#6721=CARTESIAN_POINT ( 'NONE',  ( 8.932474687540359781, -3.867868693691564719, 11.92830913002138793 ) ) ;
#6729=CONICAL_SURFACE ( 'NONE', #7875, 9.000000000000001776, 0.7853981633974431720 ) ;
#6744=CARTESIAN_POINT ( 'NONE',  ( -2.935661446561384391, -9.035036904804158553, -11.45958914175814414 ) ) ;
#6745=CARTESIAN_POINT ( 'NONE',  ( 0.9902374497044862389, -9.042884052521602101, -12.43644623859449716 ) ) ;
#6760=CARTESIAN_POINT ( 'NONE',  ( 0.000000000000000000, 0.000000000000000000, 12.50000000000000000 ) ) ;
#6761=CARTESIAN_POINT ( 'NONE',  ( 5.871322893124553133, -8.081182679343980269, 5.759589141758144848 ) ) ;
#6779=CARTESIAN_POINT ( 'NONE',  ( 2.935661446562616295, -9.035036904803758873, -8.806742014460233747 ) ) ;
#6781=CARTESIAN_POINT ( 'NONE',  ( -2.935661446561384391, -9.035036904804158553, 6.606742014460233570 ) ) ;
#6797=CARTESIAN_POINT ( 'NONE',  ( -8.680847955711200825, 2.820578480813073607, 5.533165578109187521 ) ) ;
#6806=CARTESIAN_POINT ( 'NONE',  ( -9.500000000000211386, 3.086737114211961064, -8.959589141758140585 ) ) ;
#6822=CARTESIAN_POINT ( 'NONE',  ( -2.682529543899159208, -8.255977015246598327, -6.033165578109189298 ) ) ;
#6827=CARTESIAN_POINT ( 'NONE',  ( 9.500000000000209610, -3.086737114211962396, 13.10674201446023091 ) ) ;
#6828=CARTESIAN_POINT ( 'NONE',  ( 6.809999908187194197E-13, -9.988891130263535700, 6.706742014460232326 ) ) ;
#6836=CARTESIAN_POINT ( 'NONE',  ( 6.809999908187194197E-13, -9.988891130263535700, -4.706742014460233214 ) ) ;
#6846=CARTESIAN_POINT ( 'NONE',  ( -2.935661446562617183, 9.035036904803758873, 10.65958914175814343 ) ) ;
#6862=CARTESIAN_POINT ( 'NONE',  ( -1.749335460928132413, -9.337549220493531976, -3.500000000000076383 ) ) ;
#6872=CARTESIAN_POINT ( 'NONE',  ( -7.685661446561619314, -5.583959896779019161, -4.406742014460233392 ) ) ;
#6882=CARTESIAN_POINT ( 'NONE',  ( 0.6317332097104697564, -9.783628567664347742, -3.581108421866196156 ) ) ;
#6888=CARTESIAN_POINT ( 'NONE',  ( -6.153822176767817416E-13, 9.500000000000000000, -3.186529713919390439 ) ) ;
#6893=CARTESIAN_POINT ( 'NONE',  ( -2.935661446561384391, -9.035036904804158553, 3.459589141758144137 ) ) ;
#6898=CARTESIAN_POINT ( 'NONE',  ( -9.500000000000000000, -6.482511860946779655E-13, 12.20674201446023410 ) ) ;
#6911=DIRECTION ( 'NONE',  ( 0.7071067811865439090, 8.659560562354888485E-17, -0.7071067811865512365 ) ) ;
#6914=CARTESIAN_POINT ( 'NONE',  ( 6.222797240145152671E-13, -9.127583699786111282, -4.133165578109187166 ) ) ;
#6916=CARTESIAN_POINT ( 'NONE',  ( 2.682529543899157876, 8.255977015246598327, 11.03316557810918752 ) ) ;
#6924=CARTESIAN_POINT ( 'NONE',  ( -2.935661446562617183, 9.035036904803758873, -4.659589141758143427 ) ) ;
#6931=EDGE_CURVE ( 'NONE', #566, #22998, #8605, .T. ) ;
#6947=CARTESIAN_POINT ( 'NONE',  ( -7.685661446562381371, 5.583959896777970222, 4.859589141758143604 ) ) ;
#6948=CARTESIAN_POINT ( 'NONE',  ( -7.685661446562381371, 5.583959896777970222, 10.00674201446023481 ) ) ;
#6964=CARTESIAN_POINT ( 'NONE',  ( -2.166966487431423616, 9.254762091183735606, -3.500972724454019858 ) ) ;
#6968=CARTESIAN_POINT ( 'NONE',  ( -7.022953521754877748, -5.102474405760673015, -9.833165578109188232 ) ) ;
#6973=CARTESIAN_POINT ( 'NONE',  ( -8.680847955710813579, -2.820578480814257549, 3.733165578109188587 ) ) ;
#6980=CARTESIAN_POINT ( 'NONE',  ( -5.871322893124554021, 8.081182679343978492, -3.906742014460231616 ) ) ;
#6989=DIRECTION ( 'NONE',  ( 0.000000000000000000, -1.000000000000000000, 0.000000000000000000 ) ) ;
#6992=CARTESIAN_POINT ( 'NONE',  ( 7.685661446562381371, -5.583959896777971110, 3.859589141758143604 ) ) ;
#7007=ORIENTED_EDGE ( 'NONE', *, *, #11612, .T. ) ;
#7009=CARTESIAN_POINT ( 'NONE',  ( -2.935661446562617183, 9.035036904803758873, 5.806742014460233747 ) ) ;
#7021=EDGE_CURVE ( 'NONE', #8782, #9633, #11787, .T. ) ;
#7024=ORIENTED_EDGE ( 'NONE', *, *, #9722, .F. ) ;
#7028=CARTESIAN_POINT ( 'NONE',  ( -2.935661446561384391, -9.035036904804158553, -5.459589141758144137 ) ) ;
#7033=EDGE_LOOP ( 'NONE', ( #14398, #10796 ) ) ;
#7048=CARTESIAN_POINT ( 'NONE',  ( 2.935661446561383503, 9.035036904804158553, 9.606742014460232681 ) ) ;
#7049=CARTESIAN_POINT ( 'NONE',  ( -2.935661446562617183, 9.035036904803758873, 5.806742014460233747 ) ) ;
#7062=ORIENTED_EDGE ( 'NONE', *, *, #23282, .T. ) ;
#7066=CARTESIAN_POINT ( 'NONE',  ( -9.197647033420587093, 2.458369856709957002, -3.500931213193340330 ) ) ;
#7080=CARTESIAN_POINT ( 'NONE',  ( 8.000000000000000000, 0.000000000000000000, -12.50000000000000000 ) ) ;
#7089=CARTESIAN_POINT ( 'NONE',  ( -5.871322893123450015, -8.081182679344781405, -11.35958914175814272 ) ) ;
#7140=CARTESIAN_POINT ( 'NONE',  ( 8.680847955710813579, 2.820578480814259326, 8.733165578109185034 ) ) ;
#7148=CARTESIAN_POINT ( 'NONE',  ( -9.096421271198437353, 2.534255564213257372, -12.07085958584578300 ) ) ;
#7149=CARTESIAN_POINT ( 'NONE',  ( -9.500000000000211386, 3.086737114211961064, -4.959589141758145026 ) ) ;
#7156=CARTESIAN_POINT ( 'NONE',  ( 7.685661446562381371, -5.583959896777971110, -7.006742014460233037 ) ) ;
#7158=VECTOR ( 'NONE', #23848, 1000.000000000000000 ) ;
#7163=AXIS2_PLACEMENT_3D ( 'NONE', #16543, #7488, #16767 ) ;
#7174=CARTESIAN_POINT ( 'NONE',  ( -7.685661446561619314, -5.583959896779019161, 8.406742014460233392 ) ) ;
#7175=CARTESIAN_POINT ( 'NONE',  ( 9.500000000000209610, -3.086737114211962396, 7.106742014460232681 ) ) ;
#7177=ORIENTED_EDGE ( 'NONE', *, *, #5135, .T. ) ;
#7187=CARTESIAN_POINT ( 'NONE',  ( 2.935661446561383503, 9.035036904804158553, -10.45958914175814414 ) ) ;
#7189=DIRECTION ( 'NONE',  ( -0.000000000000000000, -0.000000000000000000, -1.000000000000000000 ) ) ;
#7193=( BOUNDED_CURVE ( )  B_SPLINE_CURVE ( 2, ( #11885, #15538, #23005, #17500, #6652, #2632, #2508, #10045, #4337, #1055, #801 ),
 .UNSPECIFIED., .F., .F. ) 
 B_SPLINE_CURVE_WITH_KNOTS ( ( 3, 2, 2, 2, 2, 3 ),
 ( 0.4999999999999999445, 0.5200000000000000178, 0.5400000000000000355, 0.5600000000000000533, 0.5800000000000000711, 0.6000000000000000888 ),
 .UNSPECIFIED. ) 
 CURVE ( )  GEOMETRIC_REPRESENTATION_ITEM ( )  RATIONAL_B_SPLINE_CURVE ( ( 1.000000000000000000, 0.9510565162951533091, 1.000000000000000000, 0.9510565162951535312, 1.000000000000000000, 0.9510565162951535312, 1.000000000000000000, 0.9510565162951535312, 1.000000000000000000, 0.9510565162951533091, 1.000000000000000222 ) ) 
 REPRESENTATION_ITEM ( '' )  );
#7214=CARTESIAN_POINT ( 'NONE',  ( -2.935661446562617183, 9.035036904803758873, -8.659589141758143427 ) ) ;
#7218=CARTESIAN_POINT ( 'NONE',  ( -6.153822176767817416E-13, 9.500000000000000000, -3.568914004820086916 ) ) ;
#7220=AXIS2_PLACEMENT_3D ( 'NONE', #9979, #21233, #14028 ) ;
#7232=CARTESIAN_POINT ( 'NONE',  ( -7.685661446562381371, 5.583959896777970222, -10.00674201446023481 ) ) ;
#7237=CARTESIAN_POINT ( 'NONE',  ( 5.365059087799946447, -7.384370330706356178, 6.333165578109187344 ) ) ;
#7247=CARTESIAN_POINT ( 'NONE',  ( -9.500000000000202505, 3.086737114211975275, 10.10674201446023268 ) ) ;
#7265=CARTESIAN_POINT ( 'NONE',  ( -5.365059087798939252, -7.384370330707086261, 7.933165578109187877 ) ) ;
#7274=CARTESIAN_POINT ( 'NONE',  ( -7.022953521754877748, -5.102474405760673015, -9.833165578109188232 ) ) ;
#7293=CARTESIAN_POINT ( 'NONE',  ( 2.935661446561383503, 9.035036904804158553, 7.606742014460233570 ) ) ;
#7296=( NAMED_UNIT ( * ) SI_UNIT ( $, .STERADIAN. ) SOLID_ANGLE_UNIT ( ) );
#7312=CARTESIAN_POINT ( 'NONE',  ( -5.622572944242077574E-13, 8.680847955711007202, -3.133165578109187610 ) ) ;
#7314=CARTESIAN_POINT ( 'NONE',  ( 8.680847955710813579, 2.820578480814259326, -10.73316557810918503 ) ) ;
#7320=ORIENTED_EDGE ( 'NONE', *, *, #3154, .F. ) ;
#7330=CARTESIAN_POINT ( 'NONE',  ( -2.935661446562617183, 9.035036904803758873, -4.659589141758143427 ) ) ;
#7332=VERTEX_POINT ( 'NONE', #4456 ) ;
#7343=CARTESIAN_POINT ( 'NONE',  ( 2.682529543899157876, 8.255977015246598327, 5.033165578109189298 ) ) ;
#7369=CARTESIAN_POINT ( 'NONE',  ( -5.365059087799947335, 7.384370330706355290, 11.33316557810918468 ) ) ;
#7376=ADVANCED_FACE ( 'NONE', ( #10637 ), #3602, .T. ) ;
#7378=CARTESIAN_POINT ( 'NONE',  ( -5.365059087798939252, -7.384370330707086261, -7.933165578109187877 ) ) ;
#7399=CARTESIAN_POINT ( 'NONE',  ( -2.935661446562617183, 9.035036904803758873, 9.806742014460233747 ) ) ;
#7403=CARTESIAN_POINT ( 'NONE',  ( 9.500000000000209610, -3.086737114211962396, 9.959589141758144137 ) ) ;
#7430=AXIS2_PLACEMENT_3D ( 'NONE', #10313, #10174, #21551 ) ;
#7431=CARTESIAN_POINT ( 'NONE',  ( 5.871322893123449127, 8.081182679344781405, -8.359589141758144493 ) ) ;
#7447=CARTESIAN_POINT ( 'NONE',  ( 0.000000000000000000, 0.000000000000000000, 12.50000000000000000 ) ) ;
#7449=VERTEX_POINT ( 'NONE', #3460 ) ;
#7455=CARTESIAN_POINT ( 'NONE',  ( -5.871322893124554021, 8.081182679343978492, 9.906742014460235168 ) ) ;
#7465=CARTESIAN_POINT ( 'NONE',  ( 7.685661446562381371, -5.583959896777971110, 11.00674201446023304 ) ) ;
#7474=CARTESIAN_POINT ( 'NONE',  ( -8.680847955710813579, -2.820578480814258437, 5.733165578109188587 ) ) ;
#7485=CARTESIAN_POINT ( 'NONE',  ( 5.365059087799946447, -7.384370330706356178, -8.333165578109190008 ) ) ;
#7488=DIRECTION ( 'NONE',  ( 6.811450227741984732E-14, -1.000000000000000000, 0.000000000000000000 ) ) ;
#7497=CARTESIAN_POINT ( 'NONE',  ( 9.500000000000000000, 6.470877716354879437E-13, -8.059589141758143782 ) ) ;
#7535=CARTESIAN_POINT ( 'NONE',  ( 5.365059087798938364, 7.384370330707087149, -6.933165578109188765 ) ) ;
#7540=CARTESIAN_POINT ( 'NONE',  ( 0.000000000000000000, 0.000000000000000000, 12.50000000000000000 ) ) ;
#7542=DIRECTION ( 'NONE',  ( 1.000000000000000000, 0.000000000000000000, 0.000000000000000000 ) ) ;
#7552=CARTESIAN_POINT ( 'NONE',  ( -9.499999999999790390, -3.086737114213257804, -7.159589141758144315 ) ) ;
#7556=CARTESIAN_POINT ( 'NONE',  ( 9.500000000000000000, 6.470877716354879437E-13, 11.20674201446023410 ) ) ;
#7558=CARTESIAN_POINT ( 'NONE',  ( -6.250000000000000888, 10.82531754730548279, 2.500000000000000000 ) ) ;
#7565=CYLINDRICAL_SURFACE ( 'NONE', #18095, 9.500000000000000000 ) ;
#7567=ORIENTED_EDGE ( 'NONE', *, *, #10744, .T. ) ;
#7604=CARTESIAN_POINT ( 'NONE',  ( -9.499999999999790390, -3.086737114213257804, 11.15958914175814520 ) ) ;
#7610=CARTESIAN_POINT ( 'NONE',  ( 7.022953521754877748, 5.102474405760673903, -10.83316557810919001 ) ) ;
#7626=DIRECTION ( 'NONE',  ( -1.000000000000000000, 0.000000000000000000, 0.000000000000000000 ) ) ;
#7633=CARTESIAN_POINT ( 'NONE',  ( -8.680847955711007202, -5.923547351154968927E-13, -11.63316557810919072 ) ) ;
#7643=CARTESIAN_POINT ( 'NONE',  ( 9.500000000000000000, 6.470877716354879437E-13, 10.05958914175814378 ) ) ;
#7649=EDGE_CURVE ( 'NONE', #4813, #8141, #17158, .T. ) ;
#7661=CARTESIAN_POINT ( 'NONE',  ( 6.222797240145152671E-13, -9.127583699786111282, -6.133165578109188942 ) ) ;
#7665=CARTESIAN_POINT ( 'NONE',  ( -9.499999999999799272, -3.086737114213243593, -9.159589141758143427 ) ) ;
#7675=CARTESIAN_POINT ( 'NONE',  ( -7.685661446561619314, -5.583959896779019161, -7.259589141758143960 ) ) ;
#7677=FACE_OUTER_BOUND ( 'NONE', #7836, .T. ) ;
#7685=CARTESIAN_POINT ( 'NONE',  ( -9.500000000000216716, 3.086737114211953514, -8.106742014460232681 ) ) ;
#7693=CARTESIAN_POINT ( 'NONE',  ( 9.500000000000000000, 1.163414459189985485E-15, 12.50000000000000000 ) ) ;
#7723=CARTESIAN_POINT ( 'NONE',  ( 2.682529543899157876, 8.255977015246598327, 5.033165578109189298 ) ) ;
#7732=CARTESIAN_POINT ( 'NONE',  ( 8.680847955710813579, 2.820578480814259326, -10.73316557810918503 ) ) ;
#7746=CARTESIAN_POINT ( 'NONE',  ( 9.499999999999790390, 3.086737114213260025, -8.159589141758143427 ) ) ;
#7761=CARTESIAN_POINT ( 'NONE',  ( 6.976272796952942556, -5.349986750954705883, 12.50000000000000000 ) ) ;
#7776=CARTESIAN_POINT ( 'NONE',  ( 5.871322893124553133, -8.081182679343980269, 9.759589141758143072 ) ) ;
#7778=EDGE_CURVE ( 'NONE', #17766, #21563, #3227, .T. ) ;
#7790=CARTESIAN_POINT ( 'NONE',  ( -8.999999999999998224, 1.132798289211301501E-15, -12.50000000000000000 ) ) ;
#7792=CARTESIAN_POINT ( 'NONE',  ( 0.000000000000000000, 0.000000000000000000, -3.499999999999999556 ) ) ;
#7799=CARTESIAN_POINT ( 'NONE',  ( 2.935661446562616295, -9.035036904803758873, -6.806742014460233747 ) ) ;
#7802=CARTESIAN_POINT ( 'NONE',  ( 8.680847955711007202, 5.912916378492122225E-13, 10.63316557810918894 ) ) ;
#7805=EDGE_CURVE ( 'NONE', #18693, #3802, #20447, .T. ) ;
#7810=VECTOR ( 'NONE', #14828, 1000.000000000000000 ) ;
#7812=CARTESIAN_POINT ( 'NONE',  ( -5.871322893123450015, -8.081182679344781405, -10.50674201446023304 ) ) ;
#7820=ORIENTED_EDGE ( 'NONE', *, *, #12455, .F. ) ;
#7834=CARTESIAN_POINT ( 'NONE',  ( 7.685661446562381371, -5.583959896777971110, 11.85958914175814449 ) ) ;
#7836=EDGE_LOOP ( 'NONE', ( #23774, #4263, #10204, #8524, #8973, #5048 ) ) ;
#7853=CARTESIAN_POINT ( 'NONE',  ( 7.685661446562381371, -5.583959896777971110, -7.859589141758143604 ) ) ;
#7867=ORIENTED_EDGE ( 'NONE', *, *, #16738, .F. ) ;
#7873=CARTESIAN_POINT ( 'NONE',  ( 9.500000000000209610, -3.086737114211962396, -11.10674201446023446 ) ) ;
#7875=AXIS2_PLACEMENT_3D ( 'NONE', #23039, #2178, #20718 ) ;
#7876=CARTESIAN_POINT ( 'NONE',  ( 9.500000000000200728, -3.086737114211976607, 7.106742014460232681 ) ) ;
#7878=AXIS2_PLACEMENT_3D ( 'NONE', #5124, #22211, #14636 ) ;
#7894=CARTESIAN_POINT ( 'NONE',  ( 7.685661446562381371, -5.583959896777971110, 5.006742014460233037 ) ) ;
#7895=CARTESIAN_POINT ( 'NONE',  ( 2.682529543899157876, 8.255977015246598327, -7.033165578109189298 ) ) ;
#7899=CARTESIAN_POINT ( 'NONE',  ( 7.685661446562381371, -5.583959896777971110, 9.859589141758144493 ) ) ;
#7901=AXIS2_PLACEMENT_3D ( 'NONE', #4822, #2983, #21284 ) ;
#7911=CARTESIAN_POINT ( 'NONE',  ( 5.626939011991851203, -6.906580693685427264, -12.50000000000000000 ) ) ;
#7917=ADVANCED_FACE ( 'NONE', ( #613 ), #19686, .F. ) ;
#7921=CARTESIAN_POINT ( 'NONE',  ( -9.097401919247191771, 2.531095547992308514, 12.07092629224149327 ) ) ;
#7923=CIRCLE ( 'NONE', #23533, 9.500000000000000000 ) ;
#7927=CARTESIAN_POINT ( 'NONE',  ( 5.871322893123448239, 8.081182679344781405, -7.506742014460233037 ) ) ;
#7929=CARTESIAN_POINT ( 'NONE',  ( -5.871322893123450015, -8.081182679344781405, -8.506742014460233037 ) ) ;
#7933=CARTESIAN_POINT ( 'NONE',  ( -8.680847955711200825, 2.820578480813073607, 7.533165578109189298 ) ) ;
#7952=CARTESIAN_POINT ( 'NONE',  ( -6.963597943683918601, -6.484993096924836387, -3.499616577185218791 ) ) ;
#7957=( BOUNDED_CURVE ( )  B_SPLINE_CURVE ( 2, ( #22630, #6040, #11626, #1017, #17252, #21502, #553, #8309, #15763, #6509, #4803 ),
 .UNSPECIFIED., .F., .F. ) 
 B_SPLINE_CURVE_WITH_KNOTS ( ( 3, 2, 2, 2, 2, 3 ),
 ( 0.6000000000000000888, 0.6200000000000001066, 0.6400000000000001243, 0.6600000000000001421, 0.6800000000000001599, 0.7000000000000000666 ),
 .UNSPECIFIED. ) 
 CURVE ( )  GEOMETRIC_REPRESENTATION_ITEM ( )  RATIONAL_B_SPLINE_CURVE ( ( 0.9999999999999997780, 0.9510565162951537532, 1.000000000000000000, 0.9510565162951535312, 1.000000000000000000, 0.9510565162951535312, 1.000000000000000000, 0.9510565162951535312, 1.000000000000000000, 0.9510565162951533091, 1.000000000000000222 ) ) 
 REPRESENTATION_ITEM ( '' )  );
#7968=CARTESIAN_POINT ( 'NONE',  ( -8.680847955710813579, -2.820578480814258437, 3.733165578109188587 ) ) ;
#7978=PLANE ( 'NONE',  #19995 ) ;
#7979=CARTESIAN_POINT ( 'NONE',  ( -5.365059087798939252, -7.384370330707086261, -5.933165578109187877 ) ) ;
#7997=CARTESIAN_POINT ( 'NONE',  ( 2.935661446562616295, -9.035036904803758873, -5.659589141758144315 ) ) ;
#7998=CARTESIAN_POINT ( 'NONE',  ( -7.022953521754877748, -5.102474405760673015, -7.833165578109188232 ) ) ;
#8005=AXIS2_PLACEMENT_3D ( 'NONE', #5978, #22344, #13412 ) ;
#8008=CARTESIAN_POINT ( 'NONE',  ( 7.685661446561619314, 5.583959896779020049, -10.25958914175814485 ) ) ;
#8039=CARTESIAN_POINT ( 'NONE',  ( 6.507347684473966609, -5.969953219653604037, -12.49999999999999467 ) ) ;
#8046=CARTESIAN_POINT ( 'NONE',  ( 3.230323549912128112, -8.426447456003312908, 12.48391671383376078 ) ) ;
#8053=CARTESIAN_POINT ( 'NONE',  ( -2.935661446562617183, 9.035036904803758873, -5.806742014460233747 ) ) ;
#8054=EDGE_LOOP ( 'NONE', ( #17281, #2393, #22362, #22151, #13115, #17456 ) ) ;
#8056=CARTESIAN_POINT ( 'NONE',  ( 8.680847955710813579, 2.820578480814259326, 6.733165578109188587 ) ) ;
#8061=EDGE_CURVE ( 'NONE', #22670, #6271, #22063, .T. ) ;
#8067=CARTESIAN_POINT ( 'NONE',  ( 6.809999908187194197E-13, -9.988891130263535700, -8.706742014460230550 ) ) ;
#8079=CARTESIAN_POINT ( 'NONE',  ( -10.49999999999999822, 1.285879139104720633E-15, 3.499999999999999556 ) ) ;
#8084=VERTEX_POINT ( 'NONE', #23447 ) ;
#8085=CARTESIAN_POINT ( 'NONE',  ( -9.500000000000211386, 3.086737114211961064, 6.959589141758143249 ) ) ;
#8093=CARTESIAN_POINT ( 'NONE',  ( -7.022953521754877748, -5.102474405760673015, -3.833165578109188676 ) ) ;
#8110=CARTESIAN_POINT ( 'NONE',  ( -5.365059087798940141, -7.384370330707086261, -5.933165578109187877 ) ) ;
#8117=CARTESIAN_POINT ( 'NONE',  ( 5.365059087799946447, -7.384370330706356178, 8.333165578109190008 ) ) ;
#8119=EDGE_CURVE ( 'NONE', #20703, #9099, #496, .T. ) ;
#8128=CARTESIAN_POINT ( 'NONE',  ( -9.500000000000000000, -6.482511860946779655E-13, 4.206742014460233214 ) ) ;
#8139=CARTESIAN_POINT ( 'NONE',  ( -9.499999999999790390, -3.086737114213257804, -12.30674201446023197 ) ) ;
#8141=VERTEX_POINT ( 'NONE', #4661 ) ;
#8158=DIRECTION ( 'NONE',  ( 1.000000000000000000, 0.000000000000000000, 0.000000000000000000 ) ) ;
#8168=CARTESIAN_POINT ( 'NONE',  ( 9.500000000000209610, -3.086737114211962396, -5.106742014460234458 ) ) ;
#8171=CARTESIAN_POINT ( 'NONE',  ( 8.680847955711199049, -2.820578480813074496, 8.533165578109187521 ) ) ;
#8181=CARTESIAN_POINT ( 'NONE',  ( 9.500000000000000000, 6.470877716354879437E-13, -13.20674201446023410 ) ) ;
#8186=CARTESIAN_POINT ( 'NONE',  ( -2.018988670968663524, -9.287031262157933398, -3.500000381810258077 ) ) ;
#8187=EDGE_CURVE ( 'NONE', #13405, #17583, #3975, .T. ) ;
#8193=CARTESIAN_POINT ( 'NONE',  ( 9.500000000000000000, 6.470877716354879437E-13, 7.206742014460234103 ) ) ;
#8202=CARTESIAN_POINT ( 'NONE',  ( 9.500000000000000000, 6.470877716354879437E-13, 4.059589141758143782 ) ) ;
#8206=DIRECTION ( 'NONE',  ( 0.000000000000000000, 0.000000000000000000, 1.000000000000000000 ) ) ;
#8212=DIRECTION ( 'NONE',  ( 1.000000000000000000, 0.000000000000000000, 0.000000000000000000 ) ) ;
#8216=DIRECTION ( 'NONE',  ( -0.000000000000000000, -0.000000000000000000, -1.000000000000000000 ) ) ;
#8219=CARTESIAN_POINT ( 'NONE',  ( 6.809999908187194197E-13, -9.988891130263535700, 7.559589141758143782 ) ) ;
#8226=LINE ( 'NONE', #12013, #20064 ) ;
#8227=CARTESIAN_POINT ( 'NONE',  ( 6.222797240145152671E-13, -9.127583699786111282, -6.133165578109188054 ) ) ;
#8230=ORIENTED_EDGE ( 'NONE', *, *, #24004, .F. ) ;
#8232=CARTESIAN_POINT ( 'NONE',  ( 6.222797240145152671E-13, -9.127583699786111282, 8.133165578109188942 ) ) ;
#8244=CARTESIAN_POINT ( 'NONE',  ( 4.029965094393306726E-41, -5.916456789157588541E-28, 12.50000000000000000 ) ) ;
#8245=ORIENTED_EDGE ( 'NONE', *, *, #1616, .F. ) ;
#8255=EDGE_CURVE ( 'NONE', #15773, #2680, #16464, .T. ) ;
#8264=CARTESIAN_POINT ( 'NONE',  ( 2.935661446562616295, -9.035036904803758873, -12.80674201446023375 ) ) ;
#8267=CARTESIAN_POINT ( 'NONE',  ( 9.500000000000209610, -3.086737114211962396, 3.959589141758145026 ) ) ;
#8268=CARTESIAN_POINT ( 'NONE',  ( 9.500000000000209610, -3.086737114211962396, 13.10674201446023091 ) ) ;
#8276=CARTESIAN_POINT ( 'NONE',  ( -2.935661446562617183, 9.035036904803758873, 6.659589141758144315 ) ) ;
#8278=EDGE_CURVE ( 'NONE', #2680, #11511, #11825, .T. ) ;
#8281=CARTESIAN_POINT ( 'NONE',  ( 9.500000000000000000, 6.470877716354879437E-13, -8.059589141758143782 ) ) ;
#8290=DIRECTION ( 'NONE',  ( 1.000000000000000000, 0.000000000000000000, -0.000000000000000000 ) ) ;
#8292=FACE_OUTER_BOUND ( 'NONE', #13772, .T. ) ;
#8301=CARTESIAN_POINT ( 'NONE',  ( 9.500000000000209610, -3.086737114211962396, -7.106742014460232681 ) ) ;
#8302=ORIENTED_EDGE ( 'NONE', *, *, #1510, .F. ) ;
#8305=CARTESIAN_POINT ( 'NONE',  ( -5.365059087799948223, 7.384370330706355290, 9.333165578109190008 ) ) ;
#8308=DIRECTION ( 'NONE',  ( 0.4999999999999998890, 0.8660254037844385966, 0.000000000000000000 ) ) ;
#8309=CARTESIAN_POINT ( 'NONE',  ( -5.871322893123449127, -8.081182679344781405, 5.359589141758143604 ) ) ;
#8316=CARTESIAN_POINT ( 'NONE',  ( -5.871322893124554021, 8.081182679343978492, -9.906742014460235168 ) ) ;
#8317=ORIENTED_EDGE ( 'NONE', *, *, #12020, .T. ) ;
#8320=CARTESIAN_POINT ( 'NONE',  ( -6.503161203208929209, -6.562476031654467690, -12.26909456176216828 ) ) ;
#8337=CARTESIAN_POINT ( 'NONE',  ( -6.822232771736903637E-13, 9.988891130263535700, 6.559589141758143782 ) ) ;
#8348=CARTESIAN_POINT ( 'NONE',  ( 2.682529543899157876, 8.255977015246598327, -5.033165578109189298 ) ) ;
#8366=CARTESIAN_POINT ( 'NONE',  ( -5.365059087799948223, 7.384370330706355290, -9.333165578109190008 ) ) ;
#8372=CARTESIAN_POINT ( 'NONE',  ( 2.682529543899157876, 8.255977015246598327, 9.033165578109187521 ) ) ;
#8398=CARTESIAN_POINT ( 'NONE',  ( 9.499999999999790390, 3.086737114213260025, -11.30674201446023019 ) ) ;
#8405=CARTESIAN_POINT ( 'NONE',  ( 7.685661446561619314, 5.583959896779020049, 6.259589141758143960 ) ) ;
#8406=CARTESIAN_POINT ( 'NONE',  ( -5.871322893123450015, -8.081182679344781405, 10.50674201446023304 ) ) ;
#8411=CARTESIAN_POINT ( 'NONE',  ( -1.504652183083727168, 9.499999999999904077, 2.610843423304989308 ) ) ;
#8416=CARTESIAN_POINT ( 'NONE',  ( -9.499999999999962697, -8.297908579805900909E-07, -3.500254135480583617 ) ) ;
#8423=LINE ( 'NONE', #6606, #13384 ) ;
#8435=CARTESIAN_POINT ( 'NONE',  ( -7.022953521755574080, 5.102474405759713783, 3.433165578109189209 ) ) ;
#8437=DIRECTION ( 'NONE',  ( 1.000000000000000000, 0.000000000000000000, 0.000000000000000000 ) ) ;
#8448=CARTESIAN_POINT ( 'NONE',  ( -9.500000000000000000, -6.482511860946779655E-13, -11.05958914175814556 ) ) ;
#8464=LINE ( 'NONE', #2618, #5652 ) ;
#8469=CARTESIAN_POINT ( 'NONE',  ( 9.499999999999790390, 3.086737114213260025, 8.159589141758143427 ) ) ;
#8484=CARTESIAN_POINT ( 'NONE',  ( -7.685661446561619314, -5.583959896779019161, 6.406742014460233392 ) ) ;
#8488=CARTESIAN_POINT ( 'NONE',  ( 9.500000000000000000, 6.470877716354879437E-13, 4.059589141758143782 ) ) ;
#8493=CARTESIAN_POINT ( 'NONE',  ( -2.682529543899159208, -8.255977015246598327, -10.03316557810918930 ) ) ;
#8498=CARTESIAN_POINT ( 'NONE',  ( 5.365059087798938364, 7.384370330707087149, 4.933165578109187877 ) ) ;
#8502=DIRECTION ( 'NONE',  ( 1.000000000000000000, 0.000000000000000000, 0.000000000000000000 ) ) ;
#8505=CARTESIAN_POINT ( 'NONE',  ( 2.935661446562616295, -9.035036904803758873, -5.659589141758144315 ) ) ;
#8509=CARTESIAN_POINT ( 'NONE',  ( -2.935661446562617183, 9.035036904803758873, 3.806742014460233303 ) ) ;
#8516=ORIENTED_EDGE ( 'NONE', *, *, #14406, .T. ) ;
#8522=CARTESIAN_POINT ( 'NONE',  ( 2.682529543899157876, 8.255977015246598327, -5.033165578109189298 ) ) ;
#8523=VERTEX_POINT ( 'NONE', #17305 ) ;
#8524=ORIENTED_EDGE ( 'NONE', *, *, #18792, .T. ) ;
#8525=CARTESIAN_POINT ( 'NONE',  ( 5.871322893123449127, 8.081182679344781405, 6.359589141758142716 ) ) ;
#8526=CARTESIAN_POINT ( 'NONE',  ( 2.935661446562616295, -9.035036904803758873, 4.806742014460232859 ) ) ;
#8530=CARTESIAN_POINT ( 'NONE',  ( -9.500000000000211386, 3.086737114211961064, 6.959589141758143249 ) ) ;
#8539=DIRECTION ( 'NONE',  ( 1.000000000000000000, 0.000000000000000000, 0.000000000000000000 ) ) ;
#8549=CARTESIAN_POINT ( 'NONE',  ( 5.365059087798939252, 7.384370330707087149, 4.933165578109186988 ) ) ;
#8556=CARTESIAN_POINT ( 'NONE',  ( -9.500000000000211386, 3.086737114211961064, -6.106742014460234458 ) ) ;
#8559=CARTESIAN_POINT ( 'NONE',  ( -9.363405990316115535, -0.7769257075329323303, -12.13659400968388269 ) ) ;
#8576=CARTESIAN_POINT ( 'NONE',  ( -6.153822176767817416E-13, 9.500000000000000000, 2.559589141758142894 ) ) ;
#8577=CARTESIAN_POINT ( 'NONE',  ( 9.500000000000209610, -3.086737114211962396, 5.959589141758143249 ) ) ;
#8590=CARTESIAN_POINT ( 'NONE',  ( 2.935661446562616295, -9.035036904803758873, 4.806742014460232859 ) ) ;
#8592=EDGE_CURVE ( 'NONE', #23710, #15773, #2067, .T. ) ;
#8598=CARTESIAN_POINT ( 'NONE',  ( -7.022953521755574080, 5.102474405759713783, -3.433165578109189209 ) ) ;
#8602=CARTESIAN_POINT ( 'NONE',  ( -8.680847955711007202, -5.923547351154968927E-13, 7.633165578109188942 ) ) ;
#8605=( BOUNDED_CURVE ( )  B_SPLINE_CURVE ( 2, ( #9337, #14955, #16782, #22653, #100, #22433, #13134, #17149, #2028, #9454, #7633, #15074, #22544, #5819, #17035, #5937, #6670, #4494, #9809, #14099, #13993, #11649, #10318, #17779, #1070, #23153, #8493, #2759, #19117, #11901, #17277, #4238, #21437, #8366, #15556, #4726, #19486, #10060, #9945, #10178, #2391, #12131, #943, #4612, #577, #19374, #12014, #19609, #7998, #15935, #2889, #17635, #23400, #4357, #701, #17514, #13877, #15446, #6435, #21321, #15818, #22909, #6185, #13621, #2648, #8227, #21061, #8110, #11764, #17406, #19245, #2524, #23020, #23283, #6293, #13739, #21190, #816, #15678, #6557, #5077, #14441, #10437, #3018, #14335, #6914, #1437, #17898, #8848, #3365, #23508, #8954, #8598, #18140, #21683, #14571, #4977 ),
 .UNSPECIFIED., .F., .F. ) 
 B_SPLINE_CURVE_WITH_KNOTS ( ( 3, 2, 2, 2, 2, 2, 2, 2, 2, 2, 2, 2, 2, 2, 2, 2, 2, 2, 2, 2, 2, 2, 2, 2, 2, 2, 2, 2, 2, 2, 2, 2, 2, 2, 2, 2, 2, 2, 2, 2, 2, 2, 2, 2, 2, 2, 2, 2, 3 ),
 ( 0.01324393663734964137, 0.02000000000000000042, 0.04000000000000000083, 0.05999999999999999778, 0.08000000000000000167, 0.1000000000000000056, 0.1199999999999999956, 0.1400000000000000133, 0.1600000000000000033, 0.1799999999999999933, 0.2000000000000000111, 0.2200000000000000011, 0.2399999999999999911, 0.2600000000000000644, 0.2800000000000000266, 0.2999999999999999889, 0.3200000000000000067, 0.3400000000000000244, 0.3599999999999999867, 0.3799999999999999489, 0.4000000000000000222, 0.4199999999999999845, 0.4400000000000000022, 0.4600000000000000200, 0.4799999999999999822, 0.5000000000000000000, 0.5200000000000000178, 0.5400000000000000355, 0.5600000000000000533, 0.5799999999999999600, 0.5999999999999999778, 0.6199999999999998845, 0.6400000000000000133, 0.6600000000000000311, 0.6800000000000000488, 0.6999999999999999556, 0.7199999999999999734, 0.7399999999999999911, 0.7600000000000000089, 0.7800000000000000266, 0.8000000000000001554, 0.8199999999999999512, 0.8399999999999999689, 0.8599999999999999867, 0.8800000000000000044, 0.9000000000000000222, 0.9200000000000000400, 0.9399999999999998357, 0.9500000000000000666 ),
 .UNSPECIFIED. ) 
 CURVE ( )  GEOMETRIC_REPRESENTATION_ITEM ( )  RATIONAL_B_SPLINE_CURVE ( ( 0.9781034501096599332, 0.9834667361450606382, 1.000000000000000000, 0.9510565162951535312, 1.000000000000000000, 0.9510565162951535312, 1.000000000000000000, 0.9510565162951535312, 1.000000000000000000, 0.9510565162951535312, 1.000000000000000000, 0.9510565162951535312, 1.000000000000000000, 0.9510565162951535312, 1.000000000000000000, 0.9510565162951535312, 1.000000000000000000, 0.9510565162951535312, 1.000000000000000000, 0.9510565162951535312, 1.000000000000000000, 0.9510565162951535312, 1.000000000000000000, 0.9510565162951535312, 1.000000000000000000, 0.9510565162951535312, 1.000000000000000000, 0.9510565162951535312, 1.000000000000000000, 0.9510565162951535312, 1.000000000000000000, 0.9510565162951535312, 1.000000000000000000, 0.9510565162951535312, 1.000000000000000000, 0.9510565162951535312, 1.000000000000000000, 0.9510565162951535312, 1.000000000000000000, 0.9510565162951535312, 1.000000000000000000, 0.9510565162951535312, 1.000000000000000000, 0.9510565162951535312, 1.000000000000000000, 0.9510565162951535312, 1.000000000000000000, 0.9510565162951535312, 1.000000000000000000, 0.9510565162951535312, 1.000000000000000000, 0.9510565162951535312, 1.000000000000000000, 0.9510565162951535312, 1.000000000000000000, 0.9510565162951535312, 1.000000000000000000, 0.9510565162951535312, 1.000000000000000000, 0.9510565162951535312, 1.000000000000000000, 0.9510565162951535312, 1.000000000000000000, 0.9510565162951535312, 1.000000000000000000, 0.9510565162951535312, 1.000000000000000000, 0.9510565162951535312, 1.000000000000000000, 0.9510565162951535312, 1.000000000000000000, 0.9510565162951535312, 1.000000000000000000, 0.9510565162951535312, 1.000000000000000000, 0.9510565162951535312, 1.000000000000000000, 0.9510565162951535312, 1.000000000000000000, 0.9510565162951535312, 1.000000000000000000, 0.9510565162951535312, 1.000000000000000000, 0.9510565162951535312, 1.000000000000000000, 0.9510565162951535312, 1.000000000000000000, 0.9510565162951535312, 1.000000000000000000, 0.9510565162951535312, 1.000000000000000000, 0.9510565162951535312, 1.000000000000000000, 0.9510565162951535312, 1.000000000000000000, 0.9755282581475764880, 0.9755282581475768211 ) ) 
 REPRESENTATION_ITEM ( '' )  );
#8611=CARTESIAN_POINT ( 'NONE',  ( -6.822232771736903637E-13, 9.988891130263535700, -4.559589141758142894 ) ) ;
#8626=CARTESIAN_POINT ( 'NONE',  ( 9.500000000000209610, -3.086737114211962396, -13.10674201446023091 ) ) ;
#8630=CARTESIAN_POINT ( 'NONE',  ( -9.499999999999790390, -3.086737114213257804, 5.159589141758141650 ) ) ;
#8631=CARTESIAN_POINT ( 'NONE',  ( 7.685661446561619314, 5.583959896779020049, 9.406742014460235168 ) ) ;
#8652=CARTESIAN_POINT ( 'NONE',  ( 0.000000000000000000, 0.000000000000000000, 12.50000000000000000 ) ) ;
#8655=CARTESIAN_POINT ( 'NONE',  ( 9.500000000000000000, 6.470877716354879437E-13, 8.059589141758143782 ) ) ;
#8657=CARTESIAN_POINT ( 'NONE',  ( 7.685661446561619314, 5.583959896779020049, -6.259589141758143960 ) ) ;
#8660=CARTESIAN_POINT ( 'NONE',  ( -6.233975306307045953E-13, 9.127583699786111282, 5.133165578109188054 ) ) ;
#8675=CARTESIAN_POINT ( 'NONE',  ( 7.685661446561619314, 5.583959896779020049, -5.406742014460233392 ) ) ;
#8678=CARTESIAN_POINT ( 'NONE',  ( -0.9343984967527667607, -9.063981491316820183, -12.39613733928520567 ) ) ;
#8689=FACE_OUTER_BOUND ( 'NONE', #6166, .T. ) ;
#8705=ORIENTED_EDGE ( 'NONE', *, *, #10905, .T. ) ;
#8734=CARTESIAN_POINT ( 'NONE',  ( 8.680847955711199049, -2.820578480813074496, 4.533165578109188409 ) ) ;
#8741=CARTESIAN_POINT ( 'NONE',  ( 9.499999999999790390, 3.086737114213260025, -6.159589141758145203 ) ) ;
#8748=DIRECTION ( 'NONE',  ( -0.000000000000000000, -0.000000000000000000, -1.000000000000000000 ) ) ;
#8752=DIRECTION ( 'NONE',  ( -0.000000000000000000, -0.000000000000000000, 1.000000000000000000 ) ) ;
#8768=CARTESIAN_POINT ( 'NONE',  ( -5.871322893123450015, -8.081182679344781405, 12.50674201446023481 ) ) ;
#8769=CARTESIAN_POINT ( 'NONE',  ( -7.685661446561619314, -5.583959896779019161, 8.406742014460233392 ) ) ;
#8782=VERTEX_POINT ( 'NONE', #3753 ) ;
#8790=DIRECTION ( 'NONE',  ( 1.000000000000000000, 0.000000000000000000, 0.000000000000000000 ) ) ;
#8798=CARTESIAN_POINT ( 'NONE',  ( 8.417661073264035565, -2.391602252564381192, -12.49999999999999822 ) ) ;
#8799=CARTESIAN_POINT ( 'NONE',  ( -9.500000000000211386, 3.086737114211961064, -2.959589141758143249 ) ) ;
#8808=CARTESIAN_POINT ( 'NONE',  ( -9.500000000000000000, -6.482511860946779655E-13, -4.206742014460233214 ) ) ;
#8816=CARTESIAN_POINT ( 'NONE',  ( 7.685661446562381371, -5.583959896777971110, -3.859589141758143604 ) ) ;
#8825=TOROIDAL_SURFACE ( 'NONE', #20920, 10.49999999999999822, 1.000000000000000000 ) ;
#8826=LINE ( 'NONE', #3100, #1232 ) ;
#8833=( NAMED_UNIT ( * ) SI_UNIT ( $, .STERADIAN. ) SOLID_ANGLE_UNIT ( ) );
#8842=CARTESIAN_POINT ( 'NONE',  ( 5.871322893124553133, -8.081182679343980269, 6.906742014460234280 ) ) ;
#8848=CARTESIAN_POINT ( 'NONE',  ( -7.022953521754877748, -5.102474405760673015, -3.833165578109188676 ) ) ;
#8852=CARTESIAN_POINT ( 'NONE',  ( -7.022953521755574080, 5.102474405759713783, 11.43316557810918965 ) ) ;
#8856=PLANE ( 'NONE',  #21039 ) ;
#8860=CARTESIAN_POINT ( 'NONE',  ( -6.822232771736903637E-13, 9.988891130263535700, -6.559589141758143782 ) ) ;
#8878=CARTESIAN_POINT ( 'NONE',  ( 9.500000000000000000, 6.470877716354879437E-13, -9.206742014460234103 ) ) ;
#8880=ADVANCED_FACE ( 'NONE', ( #19189 ), #13749, .F. ) ;
#8884=CARTESIAN_POINT ( 'NONE',  ( -9.499999999999790390, -3.086737114213257804, 10.30674201446023375 ) ) ;
#8885=CARTESIAN_POINT ( 'NONE',  ( 2.935661446562616295, -9.035036904803758873, 6.806742014460233747 ) ) ;
#8899=( BOUNDED_CURVE ( )  B_SPLINE_CURVE ( 2, ( #6862, #20271, #18088, #12450, #1381, #20038, #3670, #8799, #23809, #14764, #1500, #16246, #22122 ),
 .UNSPECIFIED., .F., .T. ) 
 B_SPLINE_CURVE_WITH_KNOTS ( ( 3, 2, 2, 2, 2, 2, 3 ),
 ( 0.8558632199373886751, 0.8599999999999999867, 0.8800000000000000044, 0.9000000000000000222, 0.9200000000000000400, 0.9399999999999999467, 0.9500000000000000666 ),
 .UNSPECIFIED. ) 
 CURVE ( )  GEOMETRIC_REPRESENTATION_ITEM ( )  RATIONAL_B_SPLINE_CURVE ( ( 0.9839409940142134214, 0.9898765786207525119, 1.000000000000000000, 0.9510565162951535312, 1.000000000000000000, 0.9510565162951535312, 1.000000000000000000, 0.9510565162951535312, 1.000000000000000000, 0.9510565162951535312, 1.000000000000000000, 0.9755282581475764880, 0.9755282581475768211 ) ) 
 REPRESENTATION_ITEM ( '' )  );
#8904=CARTESIAN_POINT ( 'NONE',  ( 9.499999999999799272, 3.086737114213245370, -6.159589141758142539 ) ) ;
#8916=CARTESIAN_POINT ( 'NONE',  ( 2.935661446561383503, 9.035036904804158553, -7.606742014460233570 ) ) ;
#8925=CARTESIAN_POINT ( 'NONE',  ( -7.561939491010504000, 5.750397476200735269, 11.99999999999999822 ) ) ;
#8929=AXIS2_PLACEMENT_3D ( 'NONE', #14090, #8216, #17398 ) ;
#8932=DIRECTION ( 'NONE',  ( -0.7071067811865487940, 8.659560562354948882E-17, 0.7071067811865463515 ) ) ;
#8945=ORIENTED_EDGE ( 'NONE', *, *, #17424, .F. ) ;
#8948=CARTESIAN_POINT ( 'NONE',  ( -9.500000000000202505, 3.086737114211975275, 6.106742014460232681 ) ) ;
#8952=CIRCLE ( 'NONE', #19499, 8.999999999999998224 ) ;
#8954=CARTESIAN_POINT ( 'NONE',  ( -8.680847955711200825, 2.820578480813073607, -3.533165578109187965 ) ) ;
#8956=CARTESIAN_POINT ( 'NONE',  ( -8.680847955711007202, -5.923547351154968927E-13, 11.63316557810919072 ) ) ;
#8963=CARTESIAN_POINT ( 'NONE',  ( 2.935661446562616295, -9.035036904803758873, -9.659589141758143427 ) ) ;
#8965=PLANE ( 'NONE',  #7163 ) ;
#8968=EDGE_CURVE ( 'NONE', #23710, #16661, #2026, .T. ) ;
#8971=ORIENTED_EDGE ( 'NONE', *, *, #8187, .T. ) ;
#8972=CARTESIAN_POINT ( 'NONE',  ( 9.500000000000000000, 6.470877716354879437E-13, -7.206742014460234103 ) ) ;
#8973=ORIENTED_EDGE ( 'NONE', *, *, #9879, .T. ) ;
#8976=DIRECTION ( 'NONE',  ( 1.000000000000000000, 0.000000000000000000, 0.000000000000000000 ) ) ;
#8978=B_SPLINE_CURVE_WITH_KNOTS ( 'NONE', 3,
 ( #11644, #15178, #15551, #22649 ),
 .UNSPECIFIED., .F., .F.,
 ( 4, 4 ),
 ( 0.000000000000000000, 1.000000000000000000 ),
 .UNSPECIFIED. ) ;
#8982=CARTESIAN_POINT ( 'NONE',  ( 9.500000000000000000, 6.470877716354879437E-13, -11.20674201446023410 ) ) ;
#8986=CARTESIAN_POINT ( 'NONE',  ( -5.871322893123450015, -8.081182679344781405, 8.506742014460233037 ) ) ;
#8987=CARTESIAN_POINT ( 'NONE',  ( -9.499999999999790390, -3.086737114213257804, 8.306742014460233747 ) ) ;
#9005=VECTOR ( 'NONE', #1486, 1000.000000000000000 ) ;
#9008=FACE_OUTER_BOUND ( 'NONE', #14049, .T. ) ;
#9011=CARTESIAN_POINT ( 'NONE',  ( -9.500000000000000000, -6.482511860946779655E-13, -11.05958914175814556 ) ) ;
#9018=ORIENTED_EDGE ( 'NONE', *, *, #10913, .F. ) ;
#9033=CARTESIAN_POINT ( 'NONE',  ( 9.500000000000209610, -3.086737114211962396, -9.959589141758145914 ) ) ;
#9040=VECTOR ( 'NONE', #8308, 1000.000000000000227 ) ;
#9047=CARTESIAN_POINT ( 'NONE',  ( 0.000000000000000000, 0.000000000000000000, -3.499999999999999556 ) ) ;
#9052=CARTESIAN_POINT ( 'NONE',  ( -6.153822176767817416E-13, 9.500000000000000000, -3.706742014460231882 ) ) ;
#9053=CARTESIAN_POINT ( 'NONE',  ( -9.500000000000000000, -6.482511860946779655E-13, 3.059589141758143338 ) ) ;
#9055=ORIENTED_EDGE ( 'NONE', *, *, #16738, .T. ) ;
#9065=ORIENTED_EDGE ( 'NONE', *, *, #10905, .F. ) ;
#9082=CARTESIAN_POINT ( 'NONE',  ( -2.682529543899159208, -8.255977015246598327, 8.033165578109189298 ) ) ;
#9085=EDGE_CURVE ( 'NONE', #19174, #18693, #20304, .T. ) ;
#9094=CARTESIAN_POINT ( 'NONE',  ( -5.365059087798939252, -7.384370330707086261, -11.93316557810918965 ) ) ;
#9097=VECTOR ( 'NONE', #18972, 1000.000000000000000 ) ;
#9099=VERTEX_POINT ( 'NONE', #15199 ) ;
#9115=CARTESIAN_POINT ( 'NONE',  ( -5.871322893124554021, 8.081182679343978492, 7.906742014460233392 ) ) ;
#9120=( LENGTH_UNIT ( ) NAMED_UNIT ( * ) SI_UNIT ( .MILLI., .METRE. ) );
#9130=DIRECTION ( 'NONE',  ( -0.5000000000000003331, 0.8660254037844384856, 0.000000000000000000 ) ) ;
#9139=VECTOR ( 'NONE', #11358, 1000.000000000000000 ) ;
#9147=CARTESIAN_POINT ( 'NONE',  ( 9.500000000000000000, 6.470877716354879437E-13, -10.05958914175814378 ) ) ;
#9154=CARTESIAN_POINT ( 'NONE',  ( 7.937578510445358226, -3.514536757623690999, 12.49999999999999112 ) ) ;
#9158=CARTESIAN_POINT ( 'NONE',  ( -9.500000000000211386, 3.086737114211961064, -4.959589141758145026 ) ) ;
#9163=CARTESIAN_POINT ( 'NONE',  ( 0.000000000000000000, 0.000000000000000000, 12.50000000000000000 ) ) ;
#9179=CARTESIAN_POINT ( 'NONE',  ( 7.022953521754877748, 5.102474405760673903, 4.833165578109188232 ) ) ;
#9187=CARTESIAN_POINT ( 'NONE',  ( -6.822232771736904647E-13, 9.988891130263535700, 9.706742014460232326 ) ) ;
#9191=CARTESIAN_POINT ( 'NONE',  ( 0.000000000000000000, 0.000000000000000000, 12.50000000000000000 ) ) ;
#9202=ADVANCED_FACE ( 'NONE', ( #15092 ), #6729, .T. ) ;
#9209=CARTESIAN_POINT ( 'NONE',  ( -7.022953521755574080, 5.102474405759713783, 9.433165578109189653 ) ) ;
#9217=CARTESIAN_POINT ( 'NONE',  ( 7.022953521754877748, 5.102474405760673903, -8.833165578109190008 ) ) ;
#9223=LINE ( 'NONE', #18381, #16669 ) ;
#9228=CARTESIAN_POINT ( 'NONE',  ( -9.499999999999790390, -3.086737114213257804, -7.159589141758144315 ) ) ;
#9239=CARTESIAN_POINT ( 'NONE',  ( 5.871322893123449127, 8.081182679344781405, 9.506742014460231260 ) ) ;
#9245=CARTESIAN_POINT ( 'NONE',  ( -9.499999999999799272, -3.086737114213243593, 9.159589141758143427 ) ) ;
#9255=CARTESIAN_POINT ( 'NONE',  ( -5.871322893123449127, -8.081182679344781405, -11.35958914175814272 ) ) ;
#9263=VERTEX_POINT ( 'NONE', #23172 ) ;
#9270=CARTESIAN_POINT ( 'NONE',  ( 7.685661446561619314, 5.583959896779020049, -6.259589141758143960 ) ) ;
#9278=VERTEX_POINT ( 'NONE', #16066 ) ;
#9279=CLOSED_SHELL ( 'NONE', ( #19053, #2235, #15459, #14241, #23984, #12788, #23484, #21195, #21592, #23763, #12618, #5191, #5886, #17329, #9202, #7376, #6621, #3512, #13614, #17977, #11564, #17181, #9657, #3815, #3931, #10041, #9388, #454, #2268, #18790, #18937, #23366, #14166, #5280, #22526, #17589, #1586, #343, #19646, #5742, #2914, #9363, #16188, #17973, #18563, #597, #7917, #8880, #15424, #5017, #22199, #20695 ) ) ;
#9281=DIRECTION ( 'NONE',  ( -0.000000000000000000, -0.000000000000000000, -1.000000000000000000 ) ) ;
#9282=FACE_OUTER_BOUND ( 'NONE', #18700, .T. ) ;
#9288=CARTESIAN_POINT ( 'NONE',  ( -2.682529543900285862, 8.255977015246234174, 7.233165578109188587 ) ) ;
#9290=VERTEX_POINT ( 'NONE', #6691 ) ;
#9291=EDGE_CURVE ( 'NONE', #9099, #7332, #21701, .T. ) ;
#9310=EDGE_LOOP ( 'NONE', ( #13250, #11798, #770, #5971, #18797 ) ) ;
#9311=CARTESIAN_POINT ( 'NONE',  ( 2.935661446561383503, 9.035036904804158553, 10.45958914175814414 ) ) ;
#9319=CARTESIAN_POINT ( 'NONE',  ( 8.680847955711007202, 5.912916378492122225E-13, -8.633165578109188942 ) ) ;
#9333=CARTESIAN_POINT ( 'NONE',  ( -7.685661446562381371, 5.583959896777970222, -8.859589141758144493 ) ) ;
#9337=CARTESIAN_POINT ( 'NONE',  ( 7.937578510445243651, -3.514536757623948127, -12.49999999999998046 ) ) ;
#9341=EDGE_LOOP ( 'NONE', ( #21300, #2208, #3025, #1628, #12574 ) ) ;
#9363=ADVANCED_FACE ( 'NONE', ( #1326 ), #19981, .T. ) ;
#9373=CARTESIAN_POINT ( 'NONE',  ( 9.500000000000000000, 6.470877716354879437E-13, -8.059589141758143782 ) ) ;
#9376=CARTESIAN_POINT ( 'NONE',  ( 9.499999999999790390, 3.086737114213260025, 11.30674201446023197 ) ) ;
#9378=DIRECTION ( 'NONE',  ( 0.8191520442889927978, 5.579613378627572123E-14, -0.5735764363510448272 ) ) ;
#9388=ADVANCED_FACE ( 'NONE', ( #22289 ), #16547, .T. ) ;
#9420=CARTESIAN_POINT ( 'NONE',  ( -8.680847955711007202, -5.923547351154968927E-13, 3.633165578109188054 ) ) ;
#9432=LINE ( 'NONE', #15163, #11001 ) ;
#9433=CARTESIAN_POINT ( 'NONE',  ( -9.500000000000211386, 3.086737114211961064, -2.959589141758143249 ) ) ;
#9438=DIRECTION ( 'NONE',  ( -0.000000000000000000, -0.000000000000000000, -1.000000000000000000 ) ) ;
#9442=CYLINDRICAL_SURFACE ( 'NONE', #20375, 9.500000000000000000 ) ;
#9452=AXIS2_PLACEMENT_3D ( 'NONE', #9642, #20401, #22491 ) ;
#9454=CARTESIAN_POINT ( 'NONE',  ( -8.680847955710813579, -2.820578480814257549, -11.73316557810918859 ) ) ;
#9458=ORIENTED_EDGE ( 'NONE', *, *, #8187, .F. ) ;
#9459=CARTESIAN_POINT ( 'NONE',  ( -7.685661446562381371, 5.583959896777970222, 4.006742014460233925 ) ) ;
#9475=CARTESIAN_POINT ( 'NONE',  ( -9.500000000000220268, 3.086737114211950406, -10.95958914175814236 ) ) ;
#9476=ORIENTED_EDGE ( 'NONE', *, *, #10790, .F. ) ;
#9483=CARTESIAN_POINT ( 'NONE',  ( 2.682529543900284974, -8.255977015246234174, -6.233165578109188587 ) ) ;
#9487=ORIENTED_EDGE ( 'NONE', *, *, #10125, .F. ) ;
#9488=CARTESIAN_POINT ( 'NONE',  ( -2.935661446561384391, -9.035036904804158553, -9.459589141758144137 ) ) ;
#9503=CARTESIAN_POINT ( 'NONE',  ( -2.935661446562617183, 9.035036904803758873, -6.659589141758144315 ) ) ;
#9506=DIRECTION ( 'NONE',  ( 1.000000000000000000, 0.000000000000000000, -0.000000000000000000 ) ) ;
#9522=DIRECTION ( 'NONE',  ( 1.000000000000000000, 6.485355633664482599E-14, 0.000000000000000000 ) ) ;
#9525=EDGE_CURVE ( 'NONE', #13543, #3116, #22813, .T. ) ;
#9545=CARTESIAN_POINT ( 'NONE',  ( -8.745930587506380860, -3.750307784154818247, -3.501341891226013914 ) ) ;
#9559=CARTESIAN_POINT ( 'NONE',  ( -7.022953521754877748, -5.102474405760673015, 5.833165578109188232 ) ) ;
#9563=ORIENTED_EDGE ( 'NONE', *, *, #19498, .F. ) ;
#9565=CARTESIAN_POINT ( 'NONE',  ( 2.682529543900284974, -8.255977015246234174, -12.23316557810919036 ) ) ;
#9579=CARTESIAN_POINT ( 'NONE',  ( -6.153822176767817416E-13, 9.500000000000000000, 3.499999999999999556 ) ) ;
#9597=CARTESIAN_POINT ( 'NONE',  ( 5.871322893124551356, -8.081182679343980269, 9.759589141758143072 ) ) ;
#9619=CARTESIAN_POINT ( 'NONE',  ( 9.500000000000209610, -3.086737114211962396, 7.959589141758143249 ) ) ;
#9629=CARTESIAN_POINT ( 'NONE',  ( -1.504652183083727168, 9.499999999999904077, -2.610843423304989308 ) ) ;
#9631=CARTESIAN_POINT ( 'NONE',  ( 2.935661446561383503, 9.035036904804158553, 11.60674201446023268 ) ) ;
#9633=VERTEX_POINT ( 'NONE', #9579 ) ;
#9642=CARTESIAN_POINT ( 'NONE',  ( 0.000000000000000000, 0.000000000000000000, 12.50000000000000000 ) ) ;
#9644=FACE_OUTER_BOUND ( 'NONE', #6270, .T. ) ;
#9645=CARTESIAN_POINT ( 'NONE',  ( 2.682529543900284974, -8.255977015246234174, 12.23316557810919036 ) ) ;
#9657=ADVANCED_FACE ( 'NONE', ( #3860 ), #9442, .T. ) ;
#9659=VERTEX_POINT ( 'NONE', #22538 ) ;
#9664=( BOUNDED_CURVE ( )  B_SPLINE_CURVE ( 2, ( #3231, #21428, #5070, #18133, #6779, #12122, #12378, #15927, #12257, #12007, #10170 ),
 .UNSPECIFIED., .F., .T. ) 
 B_SPLINE_CURVE_WITH_KNOTS ( ( 3, 2, 2, 2, 2, 3 ),
 ( 0.4000000000000000222, 0.4199999999999999845, 0.4400000000000000022, 0.4599999999999999645, 0.4799999999999999267, 0.4999999999999999445 ),
 .UNSPECIFIED. ) 
 CURVE ( )  GEOMETRIC_REPRESENTATION_ITEM ( )  RATIONAL_B_SPLINE_CURVE ( ( 1.000000000000000000, 0.9510565162951535312, 1.000000000000000000, 0.9510565162951535312, 1.000000000000000000, 0.9510565162951535312, 1.000000000000000000, 0.9510565162951535312, 1.000000000000000000, 0.9510565162951536422, 0.9999999999999998890 ) ) 
 REPRESENTATION_ITEM ( '' )  );
#9672=CARTESIAN_POINT ( 'NONE',  ( -7.022953521755574080, 5.102474405759713783, 3.433165578109189209 ) ) ;
#9674=ORIENTED_EDGE ( 'NONE', *, *, #15659, .F. ) ;
#9684=ORIENTED_EDGE ( 'NONE', *, *, #23216, .F. ) ;
#9686=LINE ( 'NONE', #3970, #24012 ) ;
#9702=CARTESIAN_POINT ( 'NONE',  ( 5.365059087799946447, -7.384370330706356178, 10.33316557810919001 ) ) ;
#9710=CARTESIAN_POINT ( 'NONE',  ( 5.998136232247472499, -6.550536670409162987, 12.49999999999999289 ) ) ;
#9722=EDGE_CURVE ( 'NONE', #7449, #3425, #11088, .T. ) ;
#9748=CARTESIAN_POINT ( 'NONE',  ( -7.685661446562381371, 5.583959896777970222, -6.006742014460233037 ) ) ;
#9751=CARTESIAN_POINT ( 'NONE',  ( 7.022953521755574080, -5.102474405759714671, 10.43316557810918788 ) ) ;
#9760=ORIENTED_EDGE ( 'NONE', *, *, #2396, .F. ) ;
#9762=CARTESIAN_POINT ( 'NONE',  ( -9.500000000000211386, 3.086737114211961064, -10.10674201446023446 ) ) ;
#9768=VERTEX_POINT ( 'NONE', #21548 ) ;
#9773=DIRECTION ( 'NONE',  ( -0.5000000000000003331, 0.8660254037844384856, 0.000000000000000000 ) ) ;
#9779=CARTESIAN_POINT ( 'NONE',  ( -7.685661446561619314, -5.583959896779019161, 11.25958914175814307 ) ) ;
#9791=CARTESIAN_POINT ( 'NONE',  ( -5.365059087799947335, 7.384370330706355290, -3.333165578109187344 ) ) ;
#9807=CARTESIAN_POINT ( 'NONE',  ( -9.500000000000000000, -6.482511860946779655E-13, -5.059589141758143782 ) ) ;
#9809=CARTESIAN_POINT ( 'NONE',  ( 7.022953521754877748, 5.102474405760673903, -10.83316557810919001 ) ) ;
#9812=CARTESIAN_POINT ( 'NONE',  ( 7.685661446562381371, -5.583959896777971110, -9.006742014460233037 ) ) ;
#9819=CARTESIAN_POINT ( 'NONE',  ( -2.682529543899159208, -8.255977015246598327, 12.03316557810918930 ) ) ;
#9831=ORIENTED_EDGE ( 'NONE', *, *, #166, .F. ) ;
#9838=FACE_OUTER_BOUND ( 'NONE', #4804, .T. ) ;
#9845=CARTESIAN_POINT ( 'NONE',  ( -5.871322893123449127, -8.081182679344781405, 4.506742014460232149 ) ) ;
#9851=CARTESIAN_POINT ( 'NONE',  ( -7.685661446561619314, -5.583959896779019161, 11.25958914175814307 ) ) ;
#9852=CARTESIAN_POINT ( 'NONE',  ( 9.500000000000000000, 6.470877716354879437E-13, 13.20674201446023410 ) ) ;
#9865=CARTESIAN_POINT ( 'NONE',  ( 7.751944208201828168, -4.001916517787142524, -12.50000000000000178 ) ) ;
#9867=CARTESIAN_POINT ( 'NONE',  ( -9.500000000000000000, -6.482511860946779655E-13, -3.059589141758143338 ) ) ;
#9870=ORIENTED_EDGE ( 'NONE', *, *, #23492, .F. ) ;
#9871=CARTESIAN_POINT ( 'NONE',  ( 3.934052222107095265, -8.094642247421083070, 12.50000000000000000 ) ) ;
#9879=EDGE_CURVE ( 'NONE', #17662, #9290, #13292, .T. ) ;
#9884=CARTESIAN_POINT ( 'NONE',  ( -1.504652183083727168, 9.499999999999904077, -3.757996296007079184 ) ) ;
#9888=CARTESIAN_POINT ( 'NONE',  ( 5.365059087798939252, 7.384370330707087149, 10.93316557810918965 ) ) ;
#9897=EDGE_CURVE ( 'NONE', #17902, #4215, #22582, .T. ) ;
#9898=CARTESIAN_POINT ( 'NONE',  ( 5.871322893123449127, 8.081182679344781405, -11.50674201446023126 ) ) ;
#9902=ORIENTED_EDGE ( 'NONE', *, *, #16147, .T. ) ;
#9904=EDGE_CURVE ( 'NONE', #10554, #20510, #16248, .T. ) ;
#9915=CARTESIAN_POINT ( 'NONE',  ( -12.50000000000000178, 1.672973214995343413E-15, 2.500000000000000000 ) ) ;
#9918=ORIENTED_EDGE ( 'NONE', *, *, #9897, .T. ) ;
#9921=CARTESIAN_POINT ( 'NONE',  ( 5.871322893123449127, 8.081182679344781405, 10.35958914175814627 ) ) ;
#9927=DIRECTION ( 'NONE',  ( -0.000000000000000000, -0.000000000000000000, -1.000000000000000000 ) ) ;
#9928=CARTESIAN_POINT ( 'NONE',  ( -2.682529543899159208, -8.255977015246598327, -4.033165578109189298 ) ) ;
#9931=ORIENTED_EDGE ( 'NONE', *, *, #3154, .T. ) ;
#9933=CARTESIAN_POINT ( 'NONE',  ( -6.250000000000000888, 10.82531754730548279, -2.500000000000000000 ) ) ;
#9938=CARTESIAN_POINT ( 'NONE',  ( -9.500000000000000000, -6.482511860946779655E-13, -6.206742014460234103 ) ) ;
#9944=FACE_OUTER_BOUND ( 'NONE', #16457, .T. ) ;
#9945=CARTESIAN_POINT ( 'NONE',  ( 7.022953521754877748, 5.102474405760673903, -8.833165578109190008 ) ) ;
#9966=CYLINDRICAL_SURFACE ( 'NONE', #13433, 9.500000000000000000 ) ;
#9975=CARTESIAN_POINT ( 'NONE',  ( 9.500000000000209610, -3.086737114211962396, 11.95958914175814591 ) ) ;
#9976=CARTESIAN_POINT ( 'NONE',  ( 2.935661446561383503, 9.035036904804158553, 11.60674201446023268 ) ) ;
#9979=CARTESIAN_POINT ( 'NONE',  ( 12.50000000000000178, 5.755434930044642846E-15, 2.500000000000000000 ) ) ;
#9988=CARTESIAN_POINT ( 'NONE',  ( -2.935661446562617183, 9.035036904803758873, -2.659589141758143871 ) ) ;
#10000=CARTESIAN_POINT ( 'NONE',  ( 9.500000000000000000, 6.470877716354879437E-13, -7.206742014460234103 ) ) ;
#10001=CARTESIAN_POINT ( 'NONE',  ( 5.871322893123448239, 8.081182679344781405, 8.359589141758144493 ) ) ;
#10003=CARTESIAN_POINT ( 'NONE',  ( -5.871322893124554021, 8.081182679343978492, -7.906742014460233392 ) ) ;
#10006=CARTESIAN_POINT ( 'NONE',  ( -8.680847955710813579, -2.820578480814257549, 7.733165578109188587 ) ) ;
#10016=CARTESIAN_POINT ( 'NONE',  ( 9.500000000000209610, -3.086737114211962396, -11.10674201446023446 ) ) ;
#10034=CARTESIAN_POINT ( 'NONE',  ( 6.809999908187194197E-13, -9.988891130263535700, 9.559589141758145558 ) ) ;
#10041=ADVANCED_FACE ( 'NONE', ( #22842, #19295 ), #19534, .F. ) ;
#10044=EDGE_CURVE ( 'NONE', #3733, #22670, #17753, .T. ) ;
#10045=CARTESIAN_POINT ( 'NONE',  ( 5.871322893123448239, 8.081182679344781405, 7.506742014460233037 ) ) ;
#10046=VERTEX_POINT ( 'NONE', #7790 ) ;
#10053=CIRCLE ( 'NONE', #23337, 9.500000000000000000 ) ;
#10060=CARTESIAN_POINT ( 'NONE',  ( 5.365059087798939252, 7.384370330707087149, -8.933165578109187877 ) ) ;
#10062=EDGE_LOOP ( 'NONE', ( #8302, #21040, #22829 ) ) ;
#10067=CARTESIAN_POINT ( 'NONE',  ( 7.022953521755574080, -5.102474405759714671, 8.433165578109187877 ) ) ;
#10078=DIRECTION ( 'NONE',  ( 1.000000000000000000, 0.000000000000000000, 0.000000000000000000 ) ) ;
#10091=CARTESIAN_POINT ( 'NONE',  ( -9.500000000000000000, -6.482511860946779655E-13, -12.20674201446023410 ) ) ;
#10094=CARTESIAN_POINT ( 'NONE',  ( -2.935661446562617183, 9.035036904803758873, 10.65958914175814343 ) ) ;
#10095=CARTESIAN_POINT ( 'NONE',  ( -9.500000000000211386, 3.086737114211961064, 12.10674201446023091 ) ) ;
#10119=CARTESIAN_POINT ( 'NONE',  ( -2.935661446562617183, 9.035036904803758873, -7.806742014460233747 ) ) ;
#10123=CARTESIAN_POINT ( 'NONE',  ( -8.680847955711200825, 2.820578480813073607, 9.533165578109189298 ) ) ;
#10124=FACE_OUTER_BOUND ( 'NONE', #17840, .T. ) ;
#10125=EDGE_CURVE ( 'NONE', #13543, #11621, #8423, .T. ) ;
#10132=CARTESIAN_POINT ( 'NONE',  ( 6.809999908187194197E-13, -9.988891130263535700, -12.70674201446023410 ) ) ;
#10149=EDGE_CURVE ( 'NONE', #9099, #18771, #2206, .T. ) ;
#10153=CARTESIAN_POINT ( 'NONE',  ( -9.499999999999790390, -3.086737114213257804, 9.159589141758145203 ) ) ;
#10159=CARTESIAN_POINT ( 'NONE',  ( 2.682529543900284974, -8.255977015246234174, -4.233165578109187699 ) ) ;
#10161=CARTESIAN_POINT ( 'NONE',  ( -9.500000000000000000, -6.482511860946779655E-13, -6.206742014460234103 ) ) ;
#10170=CARTESIAN_POINT ( 'NONE',  ( -9.500000000000000000, -6.482511860946779655E-13, -8.206742014460234103 ) ) ;
#10174=DIRECTION ( 'NONE',  ( 0.000000000000000000, 0.000000000000000000, 1.000000000000000000 ) ) ;
#10178=CARTESIAN_POINT ( 'NONE',  ( 8.680847955710813579, 2.820578480814259326, -8.733165578109186811 ) ) ;
#10184=CARTESIAN_POINT ( 'NONE',  ( -8.680847955711007202, -5.923547351154968927E-13, -11.63316557810919072 ) ) ;
#10185=CARTESIAN_POINT ( 'NONE',  ( 2.682529543899157876, 8.255977015246598327, 11.03316557810918752 ) ) ;
#10186=PRODUCT ( 'Nipple', 'Nipple', '', ( #23754 ) ) ;
#10204=ORIENTED_EDGE ( 'NONE', *, *, #5629, .T. ) ;
#10213=CARTESIAN_POINT ( 'NONE',  ( 7.685661446561619314, 5.583959896779020049, -11.40674201446023517 ) ) ;
#10217=CARTESIAN_POINT ( 'NONE',  ( 2.935661446561383503, 9.035036904804158553, 4.459589141758144137 ) ) ;
#10218=CARTESIAN_POINT ( 'NONE',  ( 6.809999908187194197E-13, -9.988891130263535700, 10.70674201446023233 ) ) ;
#10222=CARTESIAN_POINT ( 'NONE',  ( 0.000000000000000000, 0.000000000000000000, -3.499999999999999556 ) ) ;
#10234=AXIS2_PLACEMENT_3D ( 'NONE', #18322, #8206, #1386 ) ;
#10241=CARTESIAN_POINT ( 'NONE',  ( -6.232140916353180238, -6.843256600934770617, 12.27698021605092471 ) ) ;
#10242=CARTESIAN_POINT ( 'NONE',  ( 6.809999908187194197E-13, -9.988891130263535700, 11.55958914175814201 ) ) ;
#10255=CARTESIAN_POINT ( 'NONE',  ( -9.500000000000000000, -6.482511860946779655E-13, -4.206742014460233214 ) ) ;
#10258=CARTESIAN_POINT ( 'NONE',  ( -7.022953521754877748, -5.102474405760673015, 5.833165578109188232 ) ) ;
#10268=CARTESIAN_POINT ( 'NONE',  ( 2.935661446561383503, 9.035036904804158553, -5.606742014460233570 ) ) ;
#10276=ORIENTED_EDGE ( 'NONE', *, *, #4485, .T. ) ;
#10286=DIRECTION ( 'NONE',  ( 1.224646799147353207E-16, 1.000000000000000000, -0.000000000000000000 ) ) ;
#10289=CARTESIAN_POINT ( 'NONE',  ( -5.871322893124554021, 8.081182679343978492, 4.759589141758144848 ) ) ;
#10313=CARTESIAN_POINT ( 'NONE',  ( 0.000000000000000000, 0.000000000000000000, -12.50000000000000000 ) ) ;
#10318=CARTESIAN_POINT ( 'NONE',  ( 7.022953521755574080, -5.102474405759714671, -10.43316557810918788 ) ) ;
#10323=CARTESIAN_POINT ( 'NONE',  ( 7.022953521755574080, -5.102474405759714671, 4.433165578109187877 ) ) ;
#10324=B_SPLINE_CURVE_WITH_KNOTS ( 'NONE', 3,
 ( #19079, #8186, #13832, #4573, #534, #22873, #13327, #22741, #17108, #4078, #7952, #18834, #412, #16995, #15145, #6021, #9545, #22984, #15402, #6143, #4315, #11721 ),
 .UNSPECIFIED., .F., .F.,
 ( 4, 2, 2, 2, 2, 2, 2, 2, 2, 2, 4 ),
 ( 0.000000000000000000, 0.02930362155383451836, 0.05860724310766903672, 0.1172144862153381151, 0.1758217293230072142, 0.2344289724306762857, 0.2637325939845108769, 0.2930362155383454681, 0.3516434586460146505, 0.4102507017536837219, 0.4688579448613529044 ),
 .UNSPECIFIED. ) ;
#10327=( BOUNDED_CURVE ( )  B_SPLINE_CURVE ( 2, ( #22157, #58, #7465, #5428, #16394, #23847, #14567, #22037, #13697, #3946, #20791 ),
 .UNSPECIFIED., .F., .T. ) 
 B_SPLINE_CURVE_WITH_KNOTS ( ( 3, 2, 2, 2, 2, 3 ),
 ( 0.2000000000000000111, 0.2200000000000000289, 0.2400000000000000466, 0.2600000000000000644, 0.2800000000000001377, 0.3000000000000000999 ),
 .UNSPECIFIED. ) 
 CURVE ( )  GEOMETRIC_REPRESENTATION_ITEM ( )  RATIONAL_B_SPLINE_CURVE ( ( 1.000000000000000000, 0.9510565162951535312, 1.000000000000000000, 0.9510565162951535312, 1.000000000000000000, 0.9510565162951535312, 1.000000000000000000, 0.9510565162951535312, 1.000000000000000000, 0.9510565162951533091, 1.000000000000000222 ) ) 
 REPRESENTATION_ITEM ( '' )  );
#10330=CARTESIAN_POINT ( 'NONE',  ( -2.935661446561384391, -9.035036904804158553, -11.45958914175814414 ) ) ;
#10338=ORIENTED_EDGE ( 'NONE', *, *, #988, .T. ) ;
#10347=CARTESIAN_POINT ( 'NONE',  ( -2.682529543899159208, -8.255977015246598327, -4.033165578109189298 ) ) ;
#10352=CARTESIAN_POINT ( 'NONE',  ( -7.685661446561619314, -5.583959896779019161, 5.259589141758143960 ) ) ;
#10353=CARTESIAN_POINT ( 'NONE',  ( 2.935661446562616295, -9.035036904803758873, 10.80674201446023197 ) ) ;
#10364=LINE ( 'NONE', #12316, #491 ) ;
#10377=DIRECTION ( 'NONE',  ( 0.000000000000000000, 0.000000000000000000, -1.000000000000000000 ) ) ;
#10385=CARTESIAN_POINT ( 'NONE',  ( 8.680847955710813579, 2.820578480814259326, 4.733165578109188587 ) ) ;
#10400=CARTESIAN_POINT ( 'NONE',  ( 6.809999908187194197E-13, -9.988891130263535700, -4.706742014460233214 ) ) ;
#10403=CARTESIAN_POINT ( 'NONE',  ( -7.966265201740081459, -4.769768961436826160, -12.22297199169018711 ) ) ;
#10405=ORIENTED_EDGE ( 'NONE', *, *, #14997, .F. ) ;
#10417=CARTESIAN_POINT ( 'NONE',  ( -6.822232771736903637E-13, 9.988891130263535700, 8.559589141758145558 ) ) ;
#10430=CARTESIAN_POINT ( 'NONE',  ( 9.499999999999790390, 3.086737114213260025, 5.306742014460231971 ) ) ;
#10432=CARTESIAN_POINT ( 'NONE',  ( -9.500000000000202505, 3.086737114211975275, 4.959589141758144137 ) ) ;
#10437=CARTESIAN_POINT ( 'NONE',  ( 7.022953521755574080, -5.102474405759714671, -4.433165578109187877 ) ) ;
#10443=CARTESIAN_POINT ( 'NONE',  ( -7.022953521754877748, -5.102474405760673015, 5.833165578109188232 ) ) ;
#10447=FACE_OUTER_BOUND ( 'NONE', #8054, .T. ) ;
#10450=LINE ( 'NONE', #4986, #12652 ) ;
#10451=CARTESIAN_POINT ( 'NONE',  ( -5.871322893123450015, -8.081182679344781405, -9.359589141758146269 ) ) ;
#10466=CARTESIAN_POINT ( 'NONE',  ( -8.680847955711200825, 2.820578480813073607, -5.533165578109187521 ) ) ;
#10467=( BOUNDED_CURVE ( )  B_SPLINE_CURVE ( 2, ( #15930, #21550, #2387, #22904, #17510, #21316, #4353 ),
 .UNSPECIFIED., .F., .T. ) 
 B_SPLINE_CURVE_WITH_KNOTS ( ( 3, 2, 2, 3 ),
 ( 0.8000000000000000444, 0.8199999999999999512, 0.8399999999999999689, 0.8558632199373861216 ),
 .UNSPECIFIED. ) 
 CURVE ( )  GEOMETRIC_REPRESENTATION_ITEM ( )  RATIONAL_B_SPLINE_CURVE ( ( 1.000000000000000000, 0.9510565162951535312, 1.000000000000000000, 0.9510565162951535312, 1.000000000000000000, 0.9611799376744073475, 0.9839409940142059829 ) ) 
 REPRESENTATION_ITEM ( '' )  );
#10470=CARTESIAN_POINT ( 'NONE',  ( -1.504652183083727168, 9.499999999999904077, 2.610843423304989308 ) ) ;
#10472=CARTESIAN_POINT ( 'NONE',  ( -2.935661446562617183, 9.035036904803758873, 9.806742014460233747 ) ) ;
#10479=VECTOR ( 'NONE', #3919, 1000.000000000000000 ) ;
#10484=CARTESIAN_POINT ( 'NONE',  ( 0.000000000000000000, 0.000000000000000000, 12.50000000000000000 ) ) ;
#10506=CARTESIAN_POINT ( 'NONE',  ( -9.500000000000000000, -6.482511860946779655E-13, -6.206742014460234103 ) ) ;
#10509=CARTESIAN_POINT ( 'NONE',  ( 0.2211988718727270209, -9.109688270588595316, -12.42028818705274773 ) ) ;
#10519=CARTESIAN_POINT ( 'NONE',  ( 5.871322893123448239, 8.081182679344781405, -9.506742014460231260 ) ) ;
#10524=CARTESIAN_POINT ( 'NONE',  ( -6.153822176767817416E-13, 9.500000000000000000, 2.559589141758142450 ) ) ;
#10525=AXIS2_PLACEMENT_3D ( 'NONE', #5514, #11222, #6004 ) ;
#10533=DIRECTION ( 'NONE',  ( -0.000000000000000000, -0.000000000000000000, -1.000000000000000000 ) ) ;
#10538=CARTESIAN_POINT ( 'NONE',  ( -9.500000000000211386, 3.086737114211961064, 4.106742014460232681 ) ) ;
#10541=CARTESIAN_POINT ( 'NONE',  ( -6.822232771736904647E-13, 9.988891130263535700, 4.559589141758142894 ) ) ;
#10548=CARTESIAN_POINT ( 'NONE',  ( -8.680847955711200825, 2.820578480813073607, 9.533165578109187521 ) ) ;
#10550=CARTESIAN_POINT ( 'NONE',  ( 8.680847955711007202, 5.912916378492122225E-13, 6.633165578109188942 ) ) ;
#10554=VERTEX_POINT ( 'NONE', #19641 ) ;
#10556=CARTESIAN_POINT ( 'NONE',  ( 5.871322893124553133, -8.081182679343980269, -9.759589141758143072 ) ) ;
#10558=CARTESIAN_POINT ( 'NONE',  ( -6.153822176767817416E-13, 9.500000000000000000, 2.559589141758142894 ) ) ;
#10577=CARTESIAN_POINT ( 'NONE',  ( -2.935661446562617183, 9.035036904803758873, -9.806742014460233747 ) ) ;
#10581=CARTESIAN_POINT ( 'NONE',  ( -5.871322893124554021, 8.081182679343978492, 2.759589141758142627 ) ) ;
#10582=CARTESIAN_POINT ( 'NONE',  ( -9.499999999999790390, -3.086737114213257804, 4.306742014460233747 ) ) ;
#10583=ORIENTED_EDGE ( 'NONE', *, *, #20212, .T. ) ;
#10588=DIRECTION ( 'NONE',  ( -0.000000000000000000, -0.000000000000000000, -1.000000000000000000 ) ) ;
#10589=AXIS2_PLACEMENT_3D ( 'NONE', #22482, #22697, #9506 ) ;
#10625=VECTOR ( 'NONE', #16279, 1000.000000000000227 ) ;
#10635=ORIENTED_EDGE ( 'NONE', *, *, #2297, .F. ) ;
#10636=CARTESIAN_POINT ( 'NONE',  ( 10.49999999999999822, 0.000000000000000000, 3.499999999999999556 ) ) ;
#10637=FACE_OUTER_BOUND ( 'NONE', #10062, .T. ) ;
#10661=CARTESIAN_POINT ( 'NONE',  ( 9.090423977855502713, 6.191897047423500831E-13, 12.34637735993366725 ) ) ;
#10662=CARTESIAN_POINT ( 'NONE',  ( -5.871322893123450015, -8.081182679344781405, 4.506742014460231260 ) ) ;
#10673=CARTESIAN_POINT ( 'NONE',  ( -5.365059087799947335, 7.384370330706355290, 9.333165578109190008 ) ) ;
#10681=CARTESIAN_POINT ( 'NONE',  ( 9.499999999999790390, 3.086737114213260025, -8.159589141758143427 ) ) ;
#10699=EDGE_LOOP ( 'NONE', ( #21377, #13574, #16345, #22182 ) ) ;
#10705=CARTESIAN_POINT ( 'NONE',  ( 2.935661446562616295, -9.035036904803758873, 5.659589141758144315 ) ) ;
#10706=CARTESIAN_POINT ( 'NONE',  ( 6.809999908187194197E-13, -9.988891130263535700, 8.706742014460230550 ) ) ;
#10708=ORIENTED_EDGE ( 'NONE', *, *, #18349, .F. ) ;
#10710=EDGE_LOOP ( 'NONE', ( #20092, #2846, #11986, #18045, #22176 ) ) ;
#10711=CARTESIAN_POINT ( 'NONE',  ( -9.500000000000000000, -6.482511860946779655E-13, -4.206742014460233214 ) ) ;
#10719=CARTESIAN_POINT ( 'NONE',  ( 6.250000000000000000, 10.82531754730548279, -2.500000000000000000 ) ) ;
#10725=CARTESIAN_POINT ( 'NONE',  ( -5.796569164227505233, 7.552650514639522861, -3.500400752039017238 ) ) ;
#10744=EDGE_CURVE ( 'NONE', #13405, #17352, #5459, .T. ) ;
#10747=CARTESIAN_POINT ( 'NONE',  ( 7.685661446562381371, -5.583959896777971110, -11.85958914175814449 ) ) ;
#10756=( GEOMETRIC_REPRESENTATION_CONTEXT ( 3 ) GLOBAL_UNCERTAINTY_ASSIGNED_CONTEXT ( ( #345 ) ) GLOBAL_UNIT_ASSIGNED_CONTEXT ( ( #9120, #20844, #7296 ) ) REPRESENTATION_CONTEXT ( 'NONE', 'WORKASPACE' ) );
#10760=CARTESIAN_POINT ( 'NONE',  ( 9.500000000000000000, 6.470877716354879437E-13, -9.206742014460234103 ) ) ;
#10766=EDGE_CURVE ( 'NONE', #3802, #11621, #19528, .T. ) ;
#10768=EDGE_LOOP ( 'NONE', ( #17638, #22084, #150 ) ) ;
#10778=CARTESIAN_POINT ( 'NONE',  ( 9.500000000000000000, 6.470877716354879437E-13, 5.206742014460234103 ) ) ;
#10779=CYLINDRICAL_SURFACE ( 'NONE', #23378, 8.000000000000000000 ) ;
#10783=DIRECTION ( 'NONE',  ( -0.000000000000000000, -0.000000000000000000, -1.000000000000000000 ) ) ;
#10788=CARTESIAN_POINT ( 'NONE',  ( -8.680847955710813579, -2.820578480814258437, 9.733165578109186811 ) ) ;
#10790=EDGE_CURVE ( 'NONE', #13492, #8141, #8978, .T. ) ;
#10794=FACE_OUTER_BOUND ( 'NONE', #9341, .T. ) ;
#10796=ORIENTED_EDGE ( 'NONE', *, *, #10865, .T. ) ;
#10798=CARTESIAN_POINT ( 'NONE',  ( 2.935661446562616295, -9.035036904803758873, -3.659589141758142983 ) ) ;
#10801=CARTESIAN_POINT ( 'NONE',  ( 6.250000000000000000, -10.82531754730548279, -2.500000000000000000 ) ) ;
#10819=CARTESIAN_POINT ( 'NONE',  ( 6.809999908187194197E-13, -9.988891130263535700, 8.706742014460230550 ) ) ;
#10820=CARTESIAN_POINT ( 'NONE',  ( 2.935661446562616295, -9.035036904803758873, 8.806742014460233747 ) ) ;
#10825=EDGE_LOOP ( 'NONE', ( #18041, #19997 ) ) ;
#10826=VECTOR ( 'NONE', #14914, 1000.000000000000000 ) ;
#10836=CARTESIAN_POINT ( 'NONE',  ( 9.500000000000000000, 6.470877716354879437E-13, 10.05958914175814378 ) ) ;
#10837=CARTESIAN_POINT ( 'NONE',  ( -7.543350946223124076, 5.782987462899389364, -3.500723002159527919 ) ) ;
#10838=CARTESIAN_POINT ( 'NONE',  ( -5.799656021750657521E-13, 8.953898637140671468, -3.324357723559535849 ) ) ;
#10856=CARTESIAN_POINT ( 'NONE',  ( 5.871322893123449127, 8.081182679344781405, -10.35958914175814627 ) ) ;
#10861=EDGE_CURVE ( 'NONE', #18771, #13485, #13503, .T. ) ;
#10865=EDGE_CURVE ( 'NONE', #23486, #8523, #17986, .T. ) ;
#10873=CARTESIAN_POINT ( 'NONE',  ( 8.000000000000000000, 0.000000000000000000, 12.50000000000000000 ) ) ;
#10875=AXIS2_PLACEMENT_3D ( 'NONE', #3487, #21917, #6678 ) ;
#10886=B_SPLINE_CURVE_WITH_KNOTS ( 'NONE', 3,
 ( #19537, #2813, #17700, #15876 ),
 .UNSPECIFIED., .F., .F.,
 ( 4, 4 ),
 ( 3.940689367451708065E-16, 0.001795700496623581352 ),
 .UNSPECIFIED. ) ;
#10897=CARTESIAN_POINT ( 'NONE',  ( 2.682529543900284974, -8.255977015246234174, 8.233165578109190363 ) ) ;
#10904=CARTESIAN_POINT ( 'NONE',  ( -5.871322893123450015, -8.081182679344781405, -7.359589141758143604 ) ) ;
#10905=EDGE_CURVE ( 'NONE', #17223, #5066, #3010, .T. ) ;
#10908=CARTESIAN_POINT ( 'NONE',  ( 6.250000000000000000, -10.82531754730548279, -2.500000000000000000 ) ) ;
#10913=EDGE_CURVE ( 'NONE', #4215, #19427, #937, .T. ) ;
#10920=CARTESIAN_POINT ( 'NONE',  ( -5.871322893123450015, -8.081182679344781405, -10.50674201446023304 ) ) ;
#10924=CARTESIAN_POINT ( 'NONE',  ( -9.500000000000000000, -6.482511860946779655E-13, 10.20674201446023233 ) ) ;
#10925=CARTESIAN_POINT ( 'NONE',  ( 7.685661446562381371, -5.583959896777971110, 5.006742014460233037 ) ) ;
#10929=ORIENTED_EDGE ( 'NONE', *, *, #20212, .F. ) ;
#10941=DIRECTION ( 'NONE',  ( 0.000000000000000000, 0.000000000000000000, 1.000000000000000000 ) ) ;
#10963=CARTESIAN_POINT ( 'NONE',  ( -5.871322893123450015, -8.081182679344781405, -7.359589141758143604 ) ) ;
#10975=VECTOR ( 'NONE', #24027, 1000.000000000000000 ) ;
#11001=VECTOR ( 'NONE', #9927, 1000.000000000000000 ) ;
#11017=CARTESIAN_POINT ( 'NONE',  ( 8.680847955711199049, -2.820578480813074496, 12.53316557810918752 ) ) ;
#11027=CARTESIAN_POINT ( 'NONE',  ( -8.790499351057960098, 3.504513977298572946, -12.05035160442407971 ) ) ;
#11028=CARTESIAN_POINT ( 'NONE',  ( 8.680847955711199049, -2.820578480813074496, -8.533165578109187521 ) ) ;
#11046=CARTESIAN_POINT ( 'NONE',  ( -7.685661446562381371, 5.583959896777970222, -10.00674201446023481 ) ) ;
#11050=CARTESIAN_POINT ( 'NONE',  ( 2.935661446561383503, 9.035036904804158553, 11.60674201446023268 ) ) ;
#11057=CARTESIAN_POINT ( 'NONE',  ( -2.935661446561384391, -9.035036904804158553, 9.459589141758144137 ) ) ;
#11088=( BOUNDED_CURVE ( )  B_SPLINE_CURVE ( 2, ( #21314, #4846, #6425, #17889, #16167, #8219, #23142, #12379, #12008, #19844, #6549 ),
 .UNSPECIFIED., .F., .T. ) 
 B_SPLINE_CURVE_WITH_KNOTS ( ( 3, 2, 2, 2, 2, 3 ),
 ( 0.4000000000000000222, 0.4199999999999999845, 0.4400000000000000022, 0.4600000000000000200, 0.4799999999999999822, 0.5000000000000000000 ),
 .UNSPECIFIED. ) 
 CURVE ( )  GEOMETRIC_REPRESENTATION_ITEM ( )  RATIONAL_B_SPLINE_CURVE ( ( 1.000000000000000000, 0.9510565162951535312, 1.000000000000000000, 0.9510565162951535312, 1.000000000000000000, 0.9510565162951535312, 1.000000000000000000, 0.9510565162951535312, 1.000000000000000000, 0.9510565162951535312, 1.000000000000000000 ) ) 
 REPRESENTATION_ITEM ( '' )  );
#11090=CARTESIAN_POINT ( 'NONE',  ( -5.871322893123450015, -8.081182679344781405, -9.359589141758146269 ) ) ;
#11109=CARTESIAN_POINT ( 'NONE',  ( -9.500000000000000000, -6.482511860946779655E-13, -4.206742014460233214 ) ) ;
#11113=CARTESIAN_POINT ( 'NONE',  ( -5.365059087799947335, 7.384370330706355290, 7.333165578109188232 ) ) ;
#11117=EDGE_CURVE ( 'NONE', #5371, #7332, #10327, .T. ) ;
#11122=CARTESIAN_POINT ( 'NONE',  ( 2.935661446561383503, 9.035036904804158553, 9.606742014460232681 ) ) ;
#11140=CARTESIAN_POINT ( 'NONE',  ( -2.682529543900285862, 8.255977015246234174, 3.233165578109188587 ) ) ;
#11148=CARTESIAN_POINT ( 'NONE',  ( -7.022953521755574080, 5.102474405759713783, -9.433165578109189653 ) ) ;
#11166=( LENGTH_UNIT ( ) NAMED_UNIT ( * ) SI_UNIT ( .MILLI., .METRE. ) );
#11171=CARTESIAN_POINT ( 'NONE',  ( 5.871322893123449127, 8.081182679344781405, 11.50674201446023126 ) ) ;
#11180=CARTESIAN_POINT ( 'NONE',  ( -9.500000000000000000, -6.482511860946779655E-13, -11.05958914175814556 ) ) ;
#11191=CARTESIAN_POINT ( 'NONE',  ( 7.022953521754877748, 5.102474405760673903, -8.833165578109190008 ) ) ;
#11195=DIRECTION ( 'NONE',  ( -0.000000000000000000, -0.000000000000000000, -1.000000000000000000 ) ) ;
#11207=CARTESIAN_POINT ( 'NONE',  ( 7.685661446562381371, -5.583959896777971110, -5.859589141758143604 ) ) ;
#11222=DIRECTION ( 'NONE',  ( -0.000000000000000000, -0.000000000000000000, -1.000000000000000000 ) ) ;
#11225=CONICAL_SURFACE ( 'NONE', #744, 9.000000000000001776, 0.7853981633974431720 ) ;
#11247=DIRECTION ( 'NONE',  ( 0.000000000000000000, 0.000000000000000000, 1.000000000000000000 ) ) ;
#11250=ORIENTED_EDGE ( 'NONE', *, *, #13542, .T. ) ;
#11251=CARTESIAN_POINT ( 'NONE',  ( -1.374911245008260563, 8.680847955710920161, 3.184419859656034024 ) ) ;
#11258=CARTESIAN_POINT ( 'NONE',  ( 5.365059087799946447, -7.384370330706356178, -10.33316557810919001 ) ) ;
#11261=CARTESIAN_POINT ( 'NONE',  ( -8.000000000000000000, 9.797174393178825657E-16, -12.50000000000000000 ) ) ;
#11276=CARTESIAN_POINT ( 'NONE',  ( -2.935661446561384391, -9.035036904804158553, 8.606742014460234458 ) ) ;
#11308=CARTESIAN_POINT ( 'NONE',  ( 0.000000000000000000, 0.000000000000000000, 2.500000000000000000 ) ) ;
#11317=CARTESIAN_POINT ( 'NONE',  ( -9.500000000000211386, 3.086737114211961064, -6.959589141758143249 ) ) ;
#11336=EDGE_LOOP ( 'NONE', ( #7062, #6537, #16999, #23831 ) ) ;
#11342=EDGE_CURVE ( 'NONE', #1207, #19938, #19703, .T. ) ;
#11358=DIRECTION ( 'NONE',  ( 1.000000000000000000, 0.000000000000000000, 0.000000000000000000 ) ) ;
#11359=ORIENTED_EDGE ( 'NONE', *, *, #902, .T. ) ;
#11366=CARTESIAN_POINT ( 'NONE',  ( -5.365059087798939252, -7.384370330707086261, 3.933165578109188321 ) ) ;
#11369=AXIS2_PLACEMENT_3D ( 'NONE', #16417, #1800, #18161 ) ;
#11381=CARTESIAN_POINT ( 'NONE',  ( 6.222797240145152671E-13, -9.127583699786111282, -8.133165578109188942 ) ) ;
#11386=ORIENTED_EDGE ( 'NONE', *, *, #23259, .T. ) ;
#11388=DIRECTION ( 'NONE',  ( -0.000000000000000000, -0.000000000000000000, -1.000000000000000000 ) ) ;
#11418=CARTESIAN_POINT ( 'NONE',  ( 5.871322893124551356, -8.081182679343980269, -10.90674201446023339 ) ) ;
#11438=CARTESIAN_POINT ( 'NONE',  ( 9.499999999999790390, 3.086737114213260025, 10.15958914175814520 ) ) ;
#11451=CARTESIAN_POINT ( 'NONE',  ( -5.871322893124554021, 8.081182679343978492, -2.759589141758142627 ) ) ;
#11470=CARTESIAN_POINT ( 'NONE',  ( 6.222797240145152671E-13, -9.127583699786111282, 8.133165578109188942 ) ) ;
#11475=ORIENTED_EDGE ( 'NONE', *, *, #15034, .T. ) ;
#11482=VERTEX_POINT ( 'NONE', #495 ) ;
#11487=CARTESIAN_POINT ( 'NONE',  ( 9.499999999999790390, 3.086737114213260025, 9.306742014460233747 ) ) ;
#11495=CARTESIAN_POINT ( 'NONE',  ( 4.029965094393306726E-41, -5.916456789157588541E-28, -12.50000000000000000 ) ) ;
#11509=CARTESIAN_POINT ( 'NONE',  ( 5.365059087799946447, -7.384370330706356178, 4.333165578109189120 ) ) ;
#11511=VERTEX_POINT ( 'NONE', #377 ) ;
#11516=CARTESIAN_POINT ( 'NONE',  ( -8.680847955711007202, -5.923547351154968927E-13, -9.633165578109188942 ) ) ;
#11540=CARTESIAN_POINT ( 'NONE',  ( -5.871322893123449127, -8.081182679344781405, 8.506742014460233037 ) ) ;
#11551=CARTESIAN_POINT ( 'NONE',  ( 3.934052222107095265, -8.094642247421083070, 12.50000000000000000 ) ) ;
#11554=CARTESIAN_POINT ( 'NONE',  ( 2.935661446561383503, 9.035036904804158553, -5.606742014460233570 ) ) ;
#11559=ORIENTED_EDGE ( 'NONE', *, *, #8592, .F. ) ;
#11564=ADVANCED_FACE ( 'NONE', ( #12430 ), #12057, .T. ) ;
#11570=CARTESIAN_POINT ( 'NONE',  ( 7.685661446562381371, -5.583959896777971110, 7.859589141758143604 ) ) ;
#11576=CARTESIAN_POINT ( 'NONE',  ( 6.976272796952845745, -5.349986750954834669, -12.49999999999999467 ) ) ;
#11581=CARTESIAN_POINT ( 'NONE',  ( -7.783282916316068167, -5.092938787329413408, 12.23045887587376690 ) ) ;
#11590=DIRECTION ( 'NONE',  ( -1.000000000000000000, 0.000000000000000000, 0.000000000000000000 ) ) ;
#11591=CARTESIAN_POINT ( 'NONE',  ( 7.685661446562381371, -5.583959896777971110, -5.006742014460233037 ) ) ;
#11594=CARTESIAN_POINT ( 'NONE',  ( -7.022953521754877748, -5.102474405760673015, 7.833165578109188232 ) ) ;
#11603=CARTESIAN_POINT ( 'NONE',  ( -6.822232771736903637E-13, 9.988891130263535700, -11.70674201446023410 ) ) ;
#11612=EDGE_CURVE ( 'NONE', #8084, #19174, #10364, .T. ) ;
#11621=VERTEX_POINT ( 'NONE', #8281 ) ;
#11623=CARTESIAN_POINT ( 'NONE',  ( -9.500000000000000000, -6.482511860946779655E-13, 11.05958914175814556 ) ) ;
#11626=CARTESIAN_POINT ( 'NONE',  ( 7.685661446562381371, -5.583959896777971110, 5.859589141758143604 ) ) ;
#11630=CARTESIAN_POINT ( 'NONE',  ( 8.680847955711007202, 5.912916378492122225E-13, -4.633165578109188942 ) ) ;
#11644=CARTESIAN_POINT ( 'NONE',  ( -6.153822176767817416E-13, 9.500000000000000000, 2.559589141758142894 ) ) ;
#11649=CARTESIAN_POINT ( 'NONE',  ( 8.680847955711199049, -2.820578480813074496, -10.53316557810918752 ) ) ;
#11652=CARTESIAN_POINT ( 'NONE',  ( 7.022953521755574080, -5.102474405759714671, 10.43316557810918788 ) ) ;
#11658=CARTESIAN_POINT ( 'NONE',  ( 4.379988124296517071, -7.836644668421621773, 12.50000000000000178 ) ) ;
#11673=ORIENTED_EDGE ( 'NONE', *, *, #2852, .T. ) ;
#11676=CARTESIAN_POINT ( 'NONE',  ( -2.935661446561384391, -9.035036904804158553, 9.459589141758144137 ) ) ;
#11683=ORIENTED_EDGE ( 'NONE', *, *, #17052, .T. ) ;
#11684=CARTESIAN_POINT ( 'NONE',  ( 7.685661446561619314, 5.583959896779020049, 6.259589141758143960 ) ) ;
#11695=CARTESIAN_POINT ( 'NONE',  ( -8.478934877242544133, 4.214451526824021244, 12.03486692402043978 ) ) ;
#11700=CARTESIAN_POINT ( 'NONE',  ( -5.871322893124554021, 8.081182679343978492, 8.759589141758144848 ) ) ;
#11701=CARTESIAN_POINT ( 'NONE',  ( -9.500000000000211386, 3.086737114211961064, -4.106742014460232681 ) ) ;
#11704=CARTESIAN_POINT ( 'NONE',  ( 8.680847955710813579, 2.820578480814259326, 10.73316557810918681 ) ) ;
#11715=CARTESIAN_POINT ( 'NONE',  ( 2.935661446562616295, -9.035036904803758873, -8.806742014460233747 ) ) ;
#11721=CARTESIAN_POINT ( 'NONE',  ( -9.499999999999962697, -8.297908579805900909E-07, -3.500254135480583617 ) ) ;
#11729=ORIENTED_EDGE ( 'NONE', *, *, #23216, .T. ) ;
#11734=CARTESIAN_POINT ( 'NONE',  ( -2.935661446561384391, -9.035036904804158553, 5.459589141758144137 ) ) ;
#11745=CARTESIAN_POINT ( 'NONE',  ( 8.680847955710813579, 2.820578480814259326, -6.733165578109187699 ) ) ;
#11758=CARTESIAN_POINT ( 'NONE',  ( -7.685661446561619314, -5.583959896779019161, -6.406742014460233392 ) ) ;
#11764=CARTESIAN_POINT ( 'NONE',  ( -7.022953521754877748, -5.102474405760673015, -5.833165578109188232 ) ) ;
#11768=VECTOR ( 'NONE', #19022, 1000.000000000000000 ) ;
#11775=CARTESIAN_POINT ( 'NONE',  ( -5.365059087799947335, 7.384370330706355290, 11.33316557810918468 ) ) ;
#11787=CIRCLE ( 'NONE', #23125, 9.500000000000000000 ) ;
#11798=ORIENTED_EDGE ( 'NONE', *, *, #21290, .T. ) ;
#11799=CARTESIAN_POINT ( 'NONE',  ( 8.680847955711199049, -2.820578480813074496, -4.533165578109188409 ) ) ;
#11822=CARTESIAN_POINT ( 'NONE',  ( -9.253409020823845310, -1.536709113333740273, 12.15192428665581303 ) ) ;
#11825=B_SPLINE_CURVE_WITH_KNOTS ( 'NONE', 3,
 ( #5483, #16233, #18304, #7066, #3067, #16107, #16340, #23568, #10837, #14277, #21966, #3300, #10725, #3171, #23690, #18197, #1488, #21737, #6964, #5253, #1589, #23795 ),
 .UNSPECIFIED., .F., .F.,
 ( 4, 2, 2, 2, 2, 2, 2, 2, 2, 2, 4 ),
 ( 0.4688579448613529044, 0.5352507017536837219, 0.6016434586460146505, 0.6680362155383455791, 0.7012325939845110989, 0.7344289724306765077, 0.8008217293230073253, 0.8672144862153383649, 0.9004108646615036626, 0.9336072431076691824, 1.000000000000000000 ),
 .UNSPECIFIED. ) ;
#11828=EDGE_CURVE ( 'NONE', #12486, #9768, #23786, .T. ) ;
#11837=ORIENTED_EDGE ( 'NONE', *, *, #16614, .F. ) ;
#11842=CARTESIAN_POINT ( 'NONE',  ( -5.365059087799948223, 7.384370330706355290, 7.333165578109188232 ) ) ;
#11846=LINE ( 'NONE', #17961, #12938 ) ;
#11849=AXIS2_PLACEMENT_3D ( 'NONE', #7540, #11195, #13275 ) ;
#11860=EDGE_CURVE ( 'NONE', #14197, #12486, #21959, .T. ) ;
#11873=EDGE_LOOP ( 'NONE', ( #18778, #9831, #17182, #4576, #12270 ) ) ;
#11877=CARTESIAN_POINT ( 'NONE',  ( 7.685661446561619314, 5.583959896779020049, 4.259589141758143960 ) ) ;
#11884=CARTESIAN_POINT ( 'NONE',  ( -2.682529543900285862, 8.255977015246234174, -3.233165578109188587 ) ) ;
#11885=CARTESIAN_POINT ( 'NONE',  ( -9.500000000000000000, -6.482511860946779655E-13, 8.206742014460234103 ) ) ;
#11888=DIRECTION ( 'NONE',  ( -0.000000000000000000, -0.000000000000000000, -1.000000000000000000 ) ) ;
#11901=CARTESIAN_POINT ( 'NONE',  ( -8.680847955710813579, -2.820578480814257549, -9.733165578109186811 ) ) ;
#11905=CARTESIAN_POINT ( 'NONE',  ( 5.365059087798938364, 7.384370330707087149, 10.93316557810918788 ) ) ;
#11917=CARTESIAN_POINT ( 'NONE',  ( -5.871322893123449127, -8.081182679344781405, 6.506742014460233925 ) ) ;
#11929=EDGE_CURVE ( 'NONE', #18651, #1630, #17051, .T. ) ;
#11932=CARTESIAN_POINT ( 'NONE',  ( 5.871322893124553133, -8.081182679343980269, -12.90674201446023517 ) ) ;
#11936=CARTESIAN_POINT ( 'NONE',  ( -6.822232771736903637E-13, 9.988891130263535700, 10.55958914175814378 ) ) ;
#11939=CARTESIAN_POINT ( 'NONE',  ( -5.365059087798939252, -7.384370330707086261, -11.93316557810918965 ) ) ;
#11941=CARTESIAN_POINT ( 'NONE',  ( -9.500000000000000000, -6.482511860946779655E-13, 7.059589141758143782 ) ) ;
#11943=B_SPLINE_CURVE_WITH_KNOTS ( 'NONE', 3,
 ( #5266, #5038, #12693, #5137, #8798, #12447, #1724, #20161 ),
 .UNSPECIFIED., .F., .F.,
 ( 4, 2, 2, 4 ),
 ( 0.000000000000000000, 0.001825626494867788573, 0.002738439742301682859, 0.003651252989735577145 ),
 .UNSPECIFIED. ) ;
#11952=CARTESIAN_POINT ( 'NONE',  ( -7.313784335799641489, -5.723601837928314673, 12.24551935885542875 ) ) ;
#11953=CARTESIAN_POINT ( 'NONE',  ( 2.935661446562616295, -9.035036904803758873, 11.65958914175814520 ) ) ;
#11957=CYLINDRICAL_SURFACE ( 'NONE', #17231, 9.500000000000000000 ) ;
#11960=CARTESIAN_POINT ( 'NONE',  ( 6.809999908187194197E-13, -9.988891130263535700, -4.706742014460233214 ) ) ;
#11963=CARTESIAN_POINT ( 'NONE',  ( 2.682529543900284974, -8.255977015246234174, 10.23316557810918859 ) ) ;
#11969=CARTESIAN_POINT ( 'NONE',  ( 7.685661446561619314, 5.583959896779020049, -9.406742014460235168 ) ) ;
#11972=CARTESIAN_POINT ( 'NONE',  ( -1.322535313088504250, -9.023848918650378081, -12.38804728513980180 ) ) ;
#11986=ORIENTED_EDGE ( 'NONE', *, *, #16556, .F. ) ;
#11989=CARTESIAN_POINT ( 'NONE',  ( 9.500000000000000000, 6.470877716354879437E-13, 8.059589141758143782 ) ) ;
#11993=ORIENTED_EDGE ( 'NONE', *, *, #10044, .T. ) ;
#11996=CARTESIAN_POINT ( 'NONE',  ( 5.365059087799946447, -7.384370330706356178, -6.333165578109187344 ) ) ;
#12007=CARTESIAN_POINT ( 'NONE',  ( -9.499999999999786837, -3.086737114213265354, -8.306742014460233747 ) ) ;
#12008=CARTESIAN_POINT ( 'NONE',  ( -7.685661446561619314, -5.583959896779019161, 7.259589141758143960 ) ) ;
#12013=CARTESIAN_POINT ( 'NONE',  ( -9.000000000000001776, 0.000000000000000000, 12.50000000000000000 ) ) ;
#12014=CARTESIAN_POINT ( 'NONE',  ( -2.682529543899159208, -8.255977015246598327, -8.033165578109189298 ) ) ;
#12018=CARTESIAN_POINT ( 'NONE',  ( -5.365059087798939252, -7.384370330707086261, 9.933165578109189653 ) ) ;
#12020=EDGE_CURVE ( 'NONE', #3116, #1372, #6259, .T. ) ;
#12024=CARTESIAN_POINT ( 'NONE',  ( 9.500000000000000000, 6.470877716354879437E-13, -12.05958914175814378 ) ) ;
#12042=CARTESIAN_POINT ( 'NONE',  ( 8.680847955710813579, 2.820578480814259326, -4.733165578109188587 ) ) ;
#12045=CARTESIAN_POINT ( 'NONE',  ( -2.935661446562617183, 9.035036904803758873, 6.659589141758144315 ) ) ;
#12046=CARTESIAN_POINT ( 'NONE',  ( 9.499999999999790390, 3.086737114213260025, 11.30674201446023019 ) ) ;
#12047=ORIENTED_EDGE ( 'NONE', *, *, #14862, .F. ) ;
#12055=CARTESIAN_POINT ( 'NONE',  ( 4.810877257134754004, -7.548248927254270768, -12.49999999999999822 ) ) ;
#12057=CYLINDRICAL_SURFACE ( 'NONE', #12141, 9.500000000000000000 ) ;
#12073=CARTESIAN_POINT ( 'NONE',  ( -7.022953521755574080, 5.102474405759713783, 5.433165578109188765 ) ) ;
#12079=CARTESIAN_POINT ( 'NONE',  ( -6.249999999999999112, -10.82531754730548279, -2.500000000000000000 ) ) ;
#12084=CARTESIAN_POINT ( 'NONE',  ( -9.500000000000211386, 3.086737114211961064, -12.10674201446023091 ) ) ;
#12086=CARTESIAN_POINT ( 'NONE',  ( 2.511895845244684455, -8.709941883493257819, -12.46858854093511049 ) ) ;
#12098=CARTESIAN_POINT ( 'NONE',  ( -1.749335460928132413, -9.337549220493531976, -3.500000000000076383 ) ) ;
#12102=CARTESIAN_POINT ( 'NONE',  ( -2.935661446561384391, -9.035036904804158553, 7.459589141758144137 ) ) ;
#12114=ORIENTED_EDGE ( 'NONE', *, *, #2324, .T. ) ;
#12122=CARTESIAN_POINT ( 'NONE',  ( 6.809999908187194197E-13, -9.988891130263535700, -8.706742014460232326 ) ) ;
#12124=CARTESIAN_POINT ( 'NONE',  ( 6.809999908187194197E-13, -9.988891130263535700, 6.706742014460232326 ) ) ;
#12125=ORIENTED_EDGE ( 'NONE', *, *, #21365, .F. ) ;
#12131=CARTESIAN_POINT ( 'NONE',  ( 8.680847955711199049, -2.820578480813074496, -8.533165578109187521 ) ) ;
#12141=AXIS2_PLACEMENT_3D ( 'NONE', #4773, #10588, #19891 ) ;
#12144=CARTESIAN_POINT ( 'NONE',  ( -2.935661446562617183, 9.035036904803758873, -11.80674201446023375 ) ) ;
#12146=CARTESIAN_POINT ( 'NONE',  ( 0.000000000000000000, 0.000000000000000000, -12.00000000000000000 ) ) ;
#12147=CARTESIAN_POINT ( 'NONE',  ( 2.935661446562616295, -9.035036904803758873, -11.65958914175814520 ) ) ;
#12167=( BOUNDED_CURVE ( )  B_SPLINE_CURVE ( 2, ( #18224, #18106, #8816, #16261, #16141, #6882, #23718 ),
 .UNSPECIFIED., .F., .F. ) 
 B_SPLINE_CURVE_WITH_KNOTS ( ( 3, 2, 2, 3 ),
 ( 0.8000000000000000444, 0.8199999999999999512, 0.8399999999999999689, 0.8558632199373886751 ),
 .UNSPECIFIED. ) 
 CURVE ( )  GEOMETRIC_REPRESENTATION_ITEM ( )  RATIONAL_B_SPLINE_CURVE ( ( 1.000000000000000000, 0.9510565162951535312, 1.000000000000000000, 0.9510565162951535312, 1.000000000000000000, 0.9611799376744010193, 0.9839409940142134214 ) ) 
 REPRESENTATION_ITEM ( '' )  );
#12171=CARTESIAN_POINT ( 'NONE',  ( -6.822232771736903637E-13, 9.988891130263535700, 4.559589141758142894 ) ) ;
#12184=EDGE_LOOP ( 'NONE', ( #3989, #4352, #11837 ) ) ;
#12195=DIRECTION ( 'NONE',  ( -1.000000000000000000, 0.000000000000000000, 0.000000000000000000 ) ) ;
#12208=EDGE_CURVE ( 'NONE', #7332, #13485, #1155, .T. ) ;
#12224=CARTESIAN_POINT ( 'NONE',  ( 9.301232020971124115, 6.335487896752474877E-13, 12.19876797902887233 ) ) ;
#12239=CARTESIAN_POINT ( 'NONE',  ( 0.000000000000000000, 0.000000000000000000, 12.50000000000000000 ) ) ;
#12240=FACE_OUTER_BOUND ( 'NONE', #22679, .T. ) ;
#12241=CARTESIAN_POINT ( 'NONE',  ( 6.809999908187194197E-13, -9.988891130263535700, 7.559589141758143782 ) ) ;
#12257=CARTESIAN_POINT ( 'NONE',  ( -7.685661446561619314, -5.583959896779019161, -8.406742014460233392 ) ) ;
#12270=ORIENTED_EDGE ( 'NONE', *, *, #7778, .F. ) ;
#12274=CARTESIAN_POINT ( 'NONE',  ( 7.022953521754877748, 5.102474405760673903, 6.833165578109188232 ) ) ;
#12280=CARTESIAN_POINT ( 'NONE',  ( 7.685661446561619314, 5.583959896779020049, -6.259589141758143960 ) ) ;
#12299=ORIENTED_EDGE ( 'NONE', *, *, #6203, .T. ) ;
#12300=CARTESIAN_POINT ( 'NONE',  ( 6.222797240145152671E-13, -9.127583699786111282, -4.133165578109187166 ) ) ;
#12304=CARTESIAN_POINT ( 'NONE',  ( -5.871322893123450015, -8.081182679344781405, 3.359589141758143160 ) ) ;
#12305=CARTESIAN_POINT ( 'NONE',  ( 5.871322893123449127, 8.081182679344781405, 5.506742014460233925 ) ) ;
#12316=CARTESIAN_POINT ( 'NONE',  ( -9.500000000000000000, 0.000000000000000000, 12.50000000000000000 ) ) ;
#12334=EDGE_LOOP ( 'NONE', ( #8705, #4730, #18980, #1051, #2603, #19132 ) ) ;
#12335=CARTESIAN_POINT ( 'NONE',  ( -2.682529543900285862, 8.255977015246234174, 5.233165578109188587 ) ) ;
#12341=CARTESIAN_POINT ( 'NONE',  ( -6.153822176767817416E-13, 9.500000000000000000, 3.706742014460231882 ) ) ;
#12344=CARTESIAN_POINT ( 'NONE',  ( 9.499999999999790390, 3.086737114213260025, -7.306742014460234635 ) ) ;
#12347=B_SPLINE_CURVE_WITH_KNOTS ( 'NONE', 3,
 ( #16061, #4988, #17796, #10558 ),
 .UNSPECIFIED., .F., .F.,
 ( 4, 4 ),
 ( 0.1802218513154718038, 1.000000000000000000 ),
 .UNSPECIFIED. ) ;
#12359=DIRECTION ( 'NONE',  ( 0.000000000000000000, 0.000000000000000000, -1.000000000000000000 ) ) ;
#12378=CARTESIAN_POINT ( 'NONE',  ( -2.935661446561384391, -9.035036904804158553, -8.606742014460234458 ) ) ;
#12379=CARTESIAN_POINT ( 'NONE',  ( -5.871322893123449127, -8.081182679344781405, 7.359589141758142716 ) ) ;
#12380=CARTESIAN_POINT ( 'NONE',  ( -9.499999999999790390, -3.086737114213257804, 4.306742014460233747 ) ) ;
#12391=CARTESIAN_POINT ( 'NONE',  ( -7.022953521755574080, 5.102474405759713783, -11.43316557810918965 ) ) ;
#12392=CARTESIAN_POINT ( 'NONE',  ( 5.365059087799946447, -7.384370330706356178, 4.333165578109189120 ) ) ;
#12395=CARTESIAN_POINT ( 'NONE',  ( 0.000000000000000000, 0.000000000000000000, 12.50000000000000000 ) ) ;
#12400=CARTESIAN_POINT ( 'NONE',  ( 9.500000000000000000, 6.470877716354879437E-13, -4.059589141758143782 ) ) ;
#12419=ORIENTED_EDGE ( 'NONE', *, *, #21264, .T. ) ;
#12420=CARTESIAN_POINT ( 'NONE',  ( -7.685661446561619314, -5.583959896779019161, 3.259589141758143516 ) ) ;
#12421=CARTESIAN_POINT ( 'NONE',  ( 9.500000000000000000, 6.470877716354879437E-13, 7.206742014460234103 ) ) ;
#12430=FACE_OUTER_BOUND ( 'NONE', #3746, .T. ) ;
#12435=CARTESIAN_POINT ( 'NONE',  ( 0.000000000000000000, 0.000000000000000000, -12.00000000000000000 ) ) ;
#12439=ORIENTED_EDGE ( 'NONE', *, *, #10861, .F. ) ;
#12441=CARTESIAN_POINT ( 'NONE',  ( 9.500000000000000000, 6.470877716354879437E-13, -6.059589141758143782 ) ) ;
#12444=CARTESIAN_POINT ( 'NONE',  ( 5.365059087799947335, -7.384370330706356178, 4.333165578109189120 ) ) ;
#12447=CARTESIAN_POINT ( 'NONE',  ( 8.199992213793557028, -2.961991314798682939, -12.49999999999999645 ) ) ;
#12450=CARTESIAN_POINT ( 'NONE',  ( -5.871322893123449127, -8.081182679344781405, -3.359589141758143160 ) ) ;
#12455=EDGE_CURVE ( 'NONE', #16852, #2012, #22877, .T. ) ;
#12458=CARTESIAN_POINT ( 'NONE',  ( 5.871322893123449127, 8.081182679344781405, -5.506742014460233925 ) ) ;
#12459=ORIENTED_EDGE ( 'NONE', *, *, #317, .T. ) ;
#12486=VERTEX_POINT ( 'NONE', #23476 ) ;
#12496=CARTESIAN_POINT ( 'NONE',  ( 5.365059087799946447, -7.384370330706356178, 12.33316557810918646 ) ) ;
#12502=CARTESIAN_POINT ( 'NONE',  ( -9.378401895172221003, -4.713374146359802882E-16, -12.12159810482778788 ) ) ;
#12503=CARTESIAN_POINT ( 'NONE',  ( -7.685661446561619314, -5.583959896779019161, -7.259589141758143960 ) ) ;
#12506=DIRECTION ( 'NONE',  ( 0.4999999999999998890, 0.8660254037844385966, 0.000000000000000000 ) ) ;
#12527=CARTESIAN_POINT ( 'NONE',  ( 5.871322893124553133, -8.081182679343980269, 7.759589141758143072 ) ) ;
#12528=CARTESIAN_POINT ( 'NONE',  ( -7.685661446562381371, 5.583959896777970222, 6.006742014460233037 ) ) ;
#12542=PRODUCT_DEFINITION ( 'UNKNOWN', '', #2597, #590 ) ;
#12544=CARTESIAN_POINT ( 'NONE',  ( 7.685661446561619314, 5.583959896779020049, 10.25958914175814485 ) ) ;
#12546=CARTESIAN_POINT ( 'NONE',  ( 8.932474687540457481, -3.867868693691433268, -11.92830913002139503 ) ) ;
#12548=EDGE_CURVE ( 'NONE', #13405, #16852, #21405, .T. ) ;
#12550=CARTESIAN_POINT ( 'NONE',  ( 5.365059087798938364, 7.384370330707087149, -8.933165578109186100 ) ) ;
#12553=CARTESIAN_POINT ( 'NONE',  ( -6.822232771736904647E-13, 9.988891130263535700, -6.559589141758143782 ) ) ;
#12572=CARTESIAN_POINT ( 'NONE',  ( 2.935661446562616295, -9.035036904803758873, -4.806742014460232859 ) ) ;
#12574=ORIENTED_EDGE ( 'NONE', *, *, #15980, .F. ) ;
#12603=ORIENTED_EDGE ( 'NONE', *, *, #16032, .T. ) ;
#12618=ADVANCED_FACE ( 'NONE', ( #19450 ), #2729, .T. ) ;
#12628=CARTESIAN_POINT ( 'NONE',  ( -5.365059087798939252, -7.384370330707086261, 9.933165578109189653 ) ) ;
#12635=CARTESIAN_POINT ( 'NONE',  ( 5.871322893123449127, 8.081182679344781405, -4.359589141758143604 ) ) ;
#12652=VECTOR ( 'NONE', #14002, 1000.000000000000000 ) ;
#12659=CARTESIAN_POINT ( 'NONE',  ( 9.499999999999790390, 3.086737114213260025, 11.30674201446023019 ) ) ;
#12660=CARTESIAN_POINT ( 'NONE',  ( 7.685661446562381371, -5.583959896777971110, 9.006742014460233037 ) ) ;
#12667=CARTESIAN_POINT ( 'NONE',  ( -7.685661446561619314, -5.583959896779019161, -4.406742014460233392 ) ) ;
#12678=CARTESIAN_POINT ( 'NONE',  ( 0.000000000000000000, 0.000000000000000000, 12.50000000000000000 ) ) ;
#12680=CARTESIAN_POINT ( 'NONE',  ( 6.809999908187194197E-13, -9.988891130263535700, -11.55958914175814201 ) ) ;
#12683=CARTESIAN_POINT ( 'NONE',  ( -2.682529543899159208, -8.255977015246598327, -8.033165578109189298 ) ) ;
#12693=CARTESIAN_POINT ( 'NONE',  ( 8.746907971560203165, -1.213523871515275410, -12.49999999999999289 ) ) ;
#12700=EDGE_LOOP ( 'NONE', ( #14644, #14705, #4340, #3635, #22722, #22886 ) ) ;
#12706=CARTESIAN_POINT ( 'NONE',  ( -1.504652183083727168, 9.499999999999904077, -3.757996296007079184 ) ) ;
#12738=ORIENTED_EDGE ( 'NONE', *, *, #23696, .F. ) ;
#12748=CARTESIAN_POINT ( 'NONE',  ( 7.022953521754877748, 5.102474405760673903, 10.83316557810919001 ) ) ;
#12751=SHAPE_DEFINITION_REPRESENTATION ( #13270, #23456 ) ;
#12757=CARTESIAN_POINT ( 'NONE',  ( 9.500000000000209610, -3.086737114211962396, -5.959589141758143249 ) ) ;
#12766=CARTESIAN_POINT ( 'NONE',  ( 6.809999908187194197E-13, -9.988891130263535700, -6.706742014460232326 ) ) ;
#12774=CARTESIAN_POINT ( 'NONE',  ( 7.685661446562381371, -5.583959896777971110, -11.00674201446023304 ) ) ;
#12779=CARTESIAN_POINT ( 'NONE',  ( -6.822232771736903637E-13, 9.988891130263535700, 9.706742014460232326 ) ) ;
#12780=CARTESIAN_POINT ( 'NONE',  ( 9.500000000000209610, -3.086737114211962396, 9.106742014460232681 ) ) ;
#12788=ADVANCED_FACE ( 'NONE', ( #4298 ), #7565, .T. ) ;
#12790=DIRECTION ( 'NONE',  ( 0.000000000000000000, 0.000000000000000000, 1.000000000000000000 ) ) ;
#12794=CARTESIAN_POINT ( 'NONE',  ( 7.685661446561619314, 5.583959896779020049, -10.25958914175814485 ) ) ;
#12800=CARTESIAN_POINT ( 'NONE',  ( 9.500000000000000000, 1.163414459189985485E-15, 12.50000000000000000 ) ) ;
#12817=CARTESIAN_POINT ( 'NONE',  ( -9.499999999999790390, -3.086737114213257804, -9.159589141758145203 ) ) ;
#12818=ORIENTED_EDGE ( 'NONE', *, *, #18792, .F. ) ;
#12833=CARTESIAN_POINT ( 'NONE',  ( 2.682529543899157876, 8.255977015246598327, 7.033165578109189298 ) ) ;
#12841=CARTESIAN_POINT ( 'NONE',  ( -7.685661446562381371, 5.583959896777970222, 10.00674201446023481 ) ) ;
#12845=VERTEX_POINT ( 'NONE', #512 ) ;
#12859=CARTESIAN_POINT ( 'NONE',  ( 5.365059087799946447, -7.384370330706356178, 10.33316557810919001 ) ) ;
#12866=CARTESIAN_POINT ( 'NONE',  ( -7.022953521755574080, 5.102474405759713783, -11.43316557810918965 ) ) ;
#12878=ORIENTED_EDGE ( 'NONE', *, *, #17521, .F. ) ;
#12880=CARTESIAN_POINT ( 'NONE',  ( 9.500000000000000000, 0.000000000000000000, -12.00000000000000000 ) ) ;
#12891=ORIENTED_EDGE ( 'NONE', *, *, #8061, .T. ) ;
#12893=CARTESIAN_POINT ( 'NONE',  ( -7.685661446562381371, 5.583959896777970222, 8.006742014460233037 ) ) ;
#12903=CARTESIAN_POINT ( 'NONE',  ( -6.822232771736904647E-13, 9.988891130263535700, -10.55958914175814201 ) ) ;
#12909=CARTESIAN_POINT ( 'NONE',  ( 9.330908268522616567, -1.784418920661929642, -11.99999999999998934 ) ) ;
#12913=CARTESIAN_POINT ( 'NONE',  ( 7.022953521755574080, -5.102474405759714671, -10.43316557810918788 ) ) ;
#12931=CARTESIAN_POINT ( 'NONE',  ( -2.935661446562617183, 9.035036904803758873, -10.65958914175814343 ) ) ;
#12938=VECTOR ( 'NONE', #1248, 1000.000000000000000 ) ;
#12946=ORIENTED_EDGE ( 'NONE', *, *, #8255, .F. ) ;
#12949=CARTESIAN_POINT ( 'NONE',  ( 5.365059087799947335, -7.384370330706356178, 12.33316557810918823 ) ) ;
#12952=( BOUNDED_SURFACE ( )  B_SPLINE_SURFACE ( 1, 2, ( 
 ( #2567, #17439, #15591, #23055, #13783, #21231, #4534, #11939, #19405, #4616, #10184, #4862, #12391, #17412, #2529, #707, #6562, #3437, #17775, #7314, #23695, #18553, #12913, #1712, #3784, #5378, #16588, #10, #6968, #22333, #13038, #14753, #20501, #1492, #5257, #18422, #3657, #12550, #11191, #1369, #14391, #21847, #23799, #20023, #3306, #14503, #12683, #18308, #1592, #4154, #361, #2308, #479, #22937, #4270, #15473, #7895, #7535, #19142, #2422, #17310, #3895, #13649, #610, #9483, #7661, #6822, #23049, #13773, #3046, #2674, #10466, #21351, #19275, #17810, #14251, #8522, #19771, #21716, #12042, #17432, #11799, #4886, #15964, #23180, #12300, #10347, #17674, #17544, #23424, #2559, #17928, #21221, #14132, #16079, #4527, #14020 ),
 ( #1215, #8626, #730, #11932, #8264, #975, #21465, #19399, #6589, #8139, #10091, #842, #15715, #6463, #13909, #4640, #19512, #2792, #10213, #8398, #8982, #16426, #12774, #18524, #20234, #19876, #23889, #10920, #16558, #14365, #20345, #3628, #11046, #1340, #10577, #1810, #16682, #21823, #3152, #18170, #8878, #16317, #9812, #3841, #2249, #18590, #17571, #7929, #4667, #4556, #19428, #2705, #2592, #10003, #10119, #644, #874, #19308, #6238, #13937, #17460, #8301, #2335, #13678, #7799, #6124, #15380, #4299, #23217, #21378, #13808, #759, #9748, #17205, #8053, #15498, #15612, #6498, #513, #21008, #21118, #8168, #11591, #23077, #6366, #11960, #21259, #22850, #19062, #22713, #10255, #11701, #2458, #13565, #4425, #9884, #22966 ) ),
 .UNSPECIFIED., .F., .F., .T. ) 
 B_SPLINE_SURFACE_WITH_KNOTS ( ( 2, 2 ),
 ( 3, 2, 2, 2, 2, 2, 2, 2, 2, 2, 2, 2, 2, 2, 2, 2, 2, 2, 2, 2, 2, 2, 2, 2, 2, 2, 2, 2, 2, 2, 2, 2, 2, 2, 2, 2, 2, 2, 2, 2, 2, 2, 2, 2, 2, 2, 2, 2, 3 ),
 ( 0.000000000000000000, 1.000000000000000000 ),
 ( 0.000000000000000000, 0.02000000000000000042, 0.04000000000000000083, 0.05999999999999999778, 0.08000000000000000167, 0.1000000000000000056, 0.1199999999999999956, 0.1400000000000000133, 0.1600000000000000033, 0.1799999999999999933, 0.2000000000000000111, 0.2200000000000000011, 0.2399999999999999911, 0.2600000000000000089, 0.2800000000000000266, 0.2999999999999999889, 0.3200000000000000067, 0.3400000000000000244, 0.3599999999999999867, 0.3800000000000000044, 0.4000000000000000222, 0.4199999999999999845, 0.4400000000000000022, 0.4600000000000000200, 0.4799999999999999822, 0.5000000000000000000, 0.5200000000000000178, 0.5400000000000000355, 0.5600000000000000533, 0.5799999999999999600, 0.5999999999999999778, 0.6199999999999999956, 0.6400000000000000133, 0.6600000000000000311, 0.6800000000000000488, 0.6999999999999999556, 0.7199999999999999734, 0.7399999999999999911, 0.7600000000000000089, 0.7800000000000000266, 0.8000000000000000444, 0.8199999999999999512, 0.8399999999999999689, 0.8599999999999999867, 0.8800000000000000044, 0.9000000000000000222, 0.9200000000000000400, 0.9399999999999999467, 0.9500000000000000666 ),
 .UNSPECIFIED. ) 
 GEOMETRIC_REPRESENTATION_ITEM ( )  RATIONAL_B_SPLINE_SURFACE ( (
 ( 1.000000000000000000, 0.9510565162951535312, 1.000000000000000000, 0.9510565162951535312, 1.000000000000000000, 0.9510565162951535312, 1.000000000000000000, 0.9510565162951535312, 1.000000000000000000, 0.9510565162951535312, 1.000000000000000000, 0.9510565162951535312, 1.000000000000000000, 0.9510565162951535312, 1.000000000000000000, 0.9510565162951535312, 1.000000000000000000, 0.9510565162951535312, 1.000000000000000000, 0.9510565162951535312, 1.000000000000000000, 0.9510565162951535312, 1.000000000000000000, 0.9510565162951535312, 1.000000000000000000, 0.9510565162951535312, 1.000000000000000000, 0.9510565162951535312, 1.000000000000000000, 0.9510565162951535312, 1.000000000000000000, 0.9510565162951535312, 1.000000000000000000, 0.9510565162951535312, 1.000000000000000000, 0.9510565162951535312, 1.000000000000000000, 0.9510565162951535312, 1.000000000000000000, 0.9510565162951535312, 1.000000000000000000, 0.9510565162951535312, 1.000000000000000000, 0.9510565162951535312, 1.000000000000000000, 0.9510565162951535312, 1.000000000000000000, 0.9510565162951535312, 1.000000000000000000, 0.9510565162951535312, 1.000000000000000000, 0.9510565162951535312, 1.000000000000000000, 0.9510565162951535312, 1.000000000000000000, 0.9510565162951535312, 1.000000000000000000, 0.9510565162951535312, 1.000000000000000000, 0.9510565162951535312, 1.000000000000000000, 0.9510565162951535312, 1.000000000000000000, 0.9510565162951535312, 1.000000000000000000, 0.9510565162951535312, 1.000000000000000000, 0.9510565162951535312, 1.000000000000000000, 0.9510565162951535312, 1.000000000000000000, 0.9510565162951535312, 1.000000000000000000, 0.9510565162951535312, 1.000000000000000000, 0.9510565162951535312, 1.000000000000000000, 0.9510565162951535312, 1.000000000000000000, 0.9510565162951535312, 1.000000000000000000, 0.9510565162951535312, 1.000000000000000000, 0.9510565162951535312, 1.000000000000000000, 0.9510565162951535312, 1.000000000000000000, 0.9510565162951535312, 1.000000000000000000, 0.9510565162951535312, 1.000000000000000000, 0.9510565162951535312, 1.000000000000000000, 0.9510565162951535312, 1.000000000000000000, 0.9755282581475764880, 0.9755282581475768211),
 ( 1.000000000000000000, 0.9510565162951535312, 1.000000000000000000, 0.9510565162951535312, 1.000000000000000000, 0.9510565162951535312, 1.000000000000000000, 0.9510565162951535312, 1.000000000000000000, 0.9510565162951535312, 1.000000000000000000, 0.9510565162951535312, 1.000000000000000000, 0.9510565162951535312, 1.000000000000000000, 0.9510565162951535312, 1.000000000000000000, 0.9510565162951535312, 1.000000000000000000, 0.9510565162951535312, 1.000000000000000000, 0.9510565162951535312, 1.000000000000000000, 0.9510565162951535312, 1.000000000000000000, 0.9510565162951535312, 1.000000000000000000, 0.9510565162951535312, 1.000000000000000000, 0.9510565162951535312, 1.000000000000000000, 0.9510565162951535312, 1.000000000000000000, 0.9510565162951535312, 1.000000000000000000, 0.9510565162951535312, 1.000000000000000000, 0.9510565162951535312, 1.000000000000000000, 0.9510565162951535312, 1.000000000000000000, 0.9510565162951535312, 1.000000000000000000, 0.9510565162951535312, 1.000000000000000000, 0.9510565162951535312, 1.000000000000000000, 0.9510565162951535312, 1.000000000000000000, 0.9510565162951535312, 1.000000000000000000, 0.9510565162951535312, 1.000000000000000000, 0.9510565162951535312, 1.000000000000000000, 0.9510565162951535312, 1.000000000000000000, 0.9510565162951535312, 1.000000000000000000, 0.9510565162951535312, 1.000000000000000000, 0.9510565162951535312, 1.000000000000000000, 0.9510565162951535312, 1.000000000000000000, 0.9510565162951535312, 1.000000000000000000, 0.9510565162951535312, 1.000000000000000000, 0.9510565162951535312, 1.000000000000000000, 0.9510565162951535312, 1.000000000000000000, 0.9510565162951535312, 1.000000000000000000, 0.9510565162951535312, 1.000000000000000000, 0.9510565162951535312, 1.000000000000000000, 0.9510565162951535312, 1.000000000000000000, 0.9510565162951535312, 1.000000000000000000, 0.9510565162951535312, 1.000000000000000000, 0.9510565162951535312, 1.000000000000000000, 0.9510565162951535312, 1.000000000000000000, 0.9510565162951535312, 1.000000000000000000, 0.9510565162951535312, 1.000000000000000000, 0.9510565162951535312, 1.000000000000000000, 0.9755282581475764880, 0.9755282581475768211) ) ) 
 REPRESENTATION_ITEM ( '' )  SURFACE ( )  );
#12990=CARTESIAN_POINT ( 'NONE',  ( -7.561939491010498671, 5.750397476200742375, -11.99999999999999822 ) ) ;
#12991=CARTESIAN_POINT ( 'NONE',  ( -2.682529543899159208, -8.255977015246598327, -10.03316557810918930 ) ) ;
#12997=EDGE_CURVE ( 'NONE', #18651, #7449, #13910, .T. ) ;
#13007=CARTESIAN_POINT ( 'NONE',  ( -9.500000000000000000, -6.482511860946779655E-13, -9.059589141758143782 ) ) ;
#13017=CARTESIAN_POINT ( 'NONE',  ( 2.935661446562616295, -9.035036904803758873, 10.80674201446023197 ) ) ;
#13034=CARTESIAN_POINT ( 'NONE',  ( -6.153822176767817416E-13, 9.500000000000000000, -3.706742014460231882 ) ) ;
#13038=CARTESIAN_POINT ( 'NONE',  ( -8.680847955711007202, -5.923547351154968927E-13, -9.633165578109188942 ) ) ;
#13059=CARTESIAN_POINT ( 'NONE',  ( -5.871322893124554021, 8.081182679343978492, -6.759589141758143072 ) ) ;
#13087=EDGE_CURVE ( 'NONE', #9263, #8782, #2547, .T. ) ;
#13089=ORIENTED_EDGE ( 'NONE', *, *, #14406, .F. ) ;
#13097=CARTESIAN_POINT ( 'NONE',  ( -5.799656021750657521E-13, 8.953898637140671468, -2.941973432658839371 ) ) ;
#13108=CARTESIAN_POINT ( 'NONE',  ( -2.682529543899159208, -8.255977015246598327, 6.033165578109189298 ) ) ;
#13115=ORIENTED_EDGE ( 'NONE', *, *, #11860, .F. ) ;
#13118=CARTESIAN_POINT ( 'NONE',  ( -8.680847955710813579, -2.820578480814258437, -11.73316557810918859 ) ) ;
#13120=ORIENTED_EDGE ( 'NONE', *, *, #2297, .T. ) ;
#13134=CARTESIAN_POINT ( 'NONE',  ( -2.682529543899159208, -8.255977015246598327, -12.03316557810918930 ) ) ;
#13143=FACE_OUTER_BOUND ( 'NONE', #11873, .T. ) ;
#13144=CARTESIAN_POINT ( 'NONE',  ( 5.871322893123448239, 8.081182679344781405, -5.506742014460233925 ) ) ;
#13156=DIRECTION ( 'NONE',  ( -0.000000000000000000, -0.000000000000000000, -1.000000000000000000 ) ) ;
#13170=CARTESIAN_POINT ( 'NONE',  ( 2.935661446562616295, -9.035036904803758873, -9.659589141758143427 ) ) ;
#13173=CARTESIAN_POINT ( 'NONE',  ( -6.822232771736904647E-13, 9.988891130263535700, 11.70674201446023410 ) ) ;
#13185=FACE_OUTER_BOUND ( 'NONE', #1923, .T. ) ;
#13211=CARTESIAN_POINT ( 'NONE',  ( -5.976739099259236459E-13, 9.226949318570335734, -2.750781287208490689 ) ) ;
#13215=ORIENTED_EDGE ( 'NONE', *, *, #6558, .T. ) ;
#13222=CARTESIAN_POINT ( 'NONE',  ( 8.680847955711199049, -2.820578480813074496, 6.533165578109188409 ) ) ;
#13228=CARTESIAN_POINT ( 'NONE',  ( -8.680847955711200825, 2.820578480813073607, -11.53316557810918574 ) ) ;
#13232=CARTESIAN_POINT ( 'NONE',  ( 0.000000000000000000, 0.000000000000000000, 12.50000000000000000 ) ) ;
#13244=CARTESIAN_POINT ( 'NONE',  ( -5.871322893123449127, -8.081182679344781405, -5.359589141758143604 ) ) ;
#13250=ORIENTED_EDGE ( 'NONE', *, *, #843, .F. ) ;
#13260=CARTESIAN_POINT ( 'NONE',  ( -9.500000000000202505, 3.086737114211975275, -6.106742014460232681 ) ) ;
#13270=PRODUCT_DEFINITION_SHAPE ( 'NONE', 'NONE',  #12542 ) ;
#13275=DIRECTION ( 'NONE',  ( -1.000000000000000000, 0.000000000000000000, 0.000000000000000000 ) ) ;
#13277=CARTESIAN_POINT ( 'NONE',  ( -2.935661446562617183, 9.035036904803758873, 8.659589141758143427 ) ) ;
#13286=CARTESIAN_POINT ( 'NONE',  ( 7.685661446562381371, -5.583959896777971110, -9.859589141758144493 ) ) ;
#13288=CARTESIAN_POINT ( 'NONE',  ( -9.500000000000000000, -6.482511860946779655E-13, 8.206742014460234103 ) ) ;
#13292=LINE ( 'NONE', #7558, #10625 ) ;
#13297=CARTESIAN_POINT ( 'NONE',  ( 7.685661446561619314, 5.583959896779020049, -7.406742014460233392 ) ) ;
#13305=LINE ( 'NONE', #7693, #24029 ) ;
#13327=CARTESIAN_POINT ( 'NONE',  ( -4.327215458830174555, -8.475258530630579656, -3.501890472894100714 ) ) ;
#13338=CARTESIAN_POINT ( 'NONE',  ( 0.000000000000000000, 0.000000000000000000, 3.499999999999999556 ) ) ;
#13341=CARTESIAN_POINT ( 'NONE',  ( -2.682529543900285862, 8.255977015246234174, 5.233165578109188587 ) ) ;
#13347=DIRECTION ( 'NONE',  ( 0.000000000000000000, 0.000000000000000000, -1.000000000000000000 ) ) ;
#13354=CARTESIAN_POINT ( 'NONE',  ( -5.871322893124554021, 8.081182679343978492, -2.759589141758142627 ) ) ;
#13384=VECTOR ( 'NONE', #4780, 1000.000000000000000 ) ;
#13387=VECTOR ( 'NONE', #783, 999.9999999999998863 ) ;
#13405=VERTEX_POINT ( 'NONE', #1777 ) ;
#13408=CARTESIAN_POINT ( 'NONE',  ( -5.871322893124554021, 8.081182679343978492, 8.759589141758141295 ) ) ;
#13412=DIRECTION ( 'NONE',  ( 1.000000000000000000, 0.000000000000000000, 0.000000000000000000 ) ) ;
#13424=CARTESIAN_POINT ( 'NONE',  ( 9.500000000000209610, -3.086737114211962396, -3.959589141758145026 ) ) ;
#13433=AXIS2_PLACEMENT_3D ( 'NONE', #16935, #17302, #3889 ) ;
#13443=CARTESIAN_POINT ( 'NONE',  ( -2.682529543899159208, -8.255977015246598327, 12.03316557810918930 ) ) ;
#13455=CARTESIAN_POINT ( 'NONE',  ( -6.822232771736903637E-13, 9.988891130263535700, -9.706742014460232326 ) ) ;
#13478=CARTESIAN_POINT ( 'NONE',  ( -5.871322893123450015, -8.081182679344781405, 11.35958914175814272 ) ) ;
#13481=ORIENTED_EDGE ( 'NONE', *, *, #12997, .T. ) ;
#13485=VERTEX_POINT ( 'NONE', #19455 ) ;
#13492=VERTEX_POINT ( 'NONE', #8576 ) ;
#13497=EDGE_LOOP ( 'NONE', ( #16467, #8516 ) ) ;
#13503=LINE ( 'NONE', #3978, #1236 ) ;
#13509=CARTESIAN_POINT ( 'NONE',  ( 9.500000000000000000, 6.470877716354879437E-13, 9.206742014460234103 ) ) ;
#13512=CARTESIAN_POINT ( 'NONE',  ( -7.022953521754877748, -5.102474405760673015, 9.833165578109188232 ) ) ;
#13525=CARTESIAN_POINT ( 'NONE',  ( -7.685661446561619314, -5.583959896779019161, 6.406742014460233392 ) ) ;
#13539=CARTESIAN_POINT ( 'NONE',  ( 6.809999908187194197E-13, -9.988891130263535700, 9.559589141758145558 ) ) ;
#13542=EDGE_CURVE ( 'NONE', #19938, #14137, #4718, .T. ) ;
#13543=VERTEX_POINT ( 'NONE', #23612 ) ;
#13556=CARTESIAN_POINT ( 'NONE',  ( -4.622819170558153168, -7.943728616300125722, 12.31730142689806051 ) ) ;
#13565=CARTESIAN_POINT ( 'NONE',  ( -5.871322893124554021, 8.081182679343978492, -3.906742014460231616 ) ) ;
#13569=CARTESIAN_POINT ( 'NONE',  ( 5.365059087798939252, 7.384370330707087149, 6.933165578109188765 ) ) ;
#13574=ORIENTED_EDGE ( 'NONE', *, *, #902, .F. ) ;
#13579=CARTESIAN_POINT ( 'NONE',  ( 7.685661446561619314, 5.583959896779020049, -11.40674201446023517 ) ) ;
#13596=CARTESIAN_POINT ( 'NONE',  ( -7.685661446562381371, 5.583959896777970222, 10.85958914175814449 ) ) ;
#13597=ORIENTED_EDGE ( 'NONE', *, *, #23603, .T. ) ;
#13600=CARTESIAN_POINT ( 'NONE',  ( 9.500000000000000000, 6.470877716354879437E-13, -12.63316557810918894 ) ) ;
#13601=CARTESIAN_POINT ( 'NONE',  ( -2.682529543900285862, 8.255977015246234174, -7.233165578109188587 ) ) ;
#13602=( BOUNDED_CURVE ( )  B_SPLINE_CURVE ( 2, ( #509, #7685, #6234, #2702, #13675, #15608, #283, #7927, #13297, #15123, #10000 ),
 .UNSPECIFIED., .F., .T. ) 
 B_SPLINE_CURVE_WITH_KNOTS ( ( 3, 2, 2, 2, 2, 3 ),
 ( 0.4999999999999999445, 0.5200000000000000178, 0.5400000000000000355, 0.5600000000000000533, 0.5800000000000000711, 0.6000000000000000888 ),
 .UNSPECIFIED. ) 
 CURVE ( )  GEOMETRIC_REPRESENTATION_ITEM ( )  RATIONAL_B_SPLINE_CURVE ( ( 1.000000000000000000, 0.9510565162951533091, 1.000000000000000000, 0.9510565162951535312, 1.000000000000000000, 0.9510565162951535312, 1.000000000000000000, 0.9510565162951535312, 1.000000000000000000, 0.9510565162951533091, 1.000000000000000222 ) ) 
 REPRESENTATION_ITEM ( '' )  );
#13614=ADVANCED_FACE ( 'NONE', ( #12240 ), #19711, .T. ) ;
#13621=CARTESIAN_POINT ( 'NONE',  ( 5.365059087799947335, -7.384370330706356178, -6.333165578109188232 ) ) ;
#13622=CARTESIAN_POINT ( 'NONE',  ( 2.935661446562616295, -9.035036904803758873, 8.806742014460233747 ) ) ;
#13625=CARTESIAN_POINT ( 'NONE',  ( -6.153822176767817416E-13, 9.500000000000000000, 3.706742014460232326 ) ) ;
#13629=CARTESIAN_POINT ( 'NONE',  ( 7.685661446562381371, -5.583959896777971110, -9.859589141758144493 ) ) ;
#13633=CARTESIAN_POINT ( 'NONE',  ( 8.871028110654306076, 6.042456644462176420E-13, 12.50000000000000000 ) ) ;
#13640=EDGE_CURVE ( 'NONE', #1207, #14734, #14524, .T. ) ;
#13647=CARTESIAN_POINT ( 'NONE',  ( 9.500000000000209610, -3.086737114211962396, 5.106742014460234458 ) ) ;
#13649=CARTESIAN_POINT ( 'NONE',  ( 7.022953521755574080, -5.102474405759714671, -6.433165578109188765 ) ) ;
#13653=CARTESIAN_POINT ( 'NONE',  ( -7.685661446562381371, 5.583959896777970222, 10.85958914175814449 ) ) ;
#13654=CARTESIAN_POINT ( 'NONE',  ( 6.809999908187194197E-13, -9.988891130263535700, 12.70674201446023410 ) ) ;
#13658=CARTESIAN_POINT ( 'NONE',  ( -5.871322893124554021, 8.081182679343978492, 6.759589141758143072 ) ) ;
#13659=EDGE_CURVE ( 'NONE', #3340, #18614, #16591, .T. ) ;
#13671=CARTESIAN_POINT ( 'NONE',  ( -5.871322893123449127, -8.081182679344781405, 11.35958914175814272 ) ) ;
#13675=CARTESIAN_POINT ( 'NONE',  ( -2.935661446562617183, 9.035036904803758873, -7.806742014460233747 ) ) ;
#13676=CARTESIAN_POINT ( 'NONE',  ( -6.822232771736904647E-13, 9.988891130263535700, 8.559589141758142006 ) ) ;
#13678=CARTESIAN_POINT ( 'NONE',  ( 5.871322893124553133, -8.081182679343980269, -6.906742014460234280 ) ) ;
#13681=CARTESIAN_POINT ( 'NONE',  ( 7.022953521755574080, -5.102474405759714671, 6.433165578109188765 ) ) ;
#13690=CARTESIAN_POINT ( 'NONE',  ( -4.632213926375346347, -7.938484784988568244, -12.31707955932596477 ) ) ;
#13697=CARTESIAN_POINT ( 'NONE',  ( -7.685661446561619314, -5.583959896779019161, 10.40674201446023339 ) ) ;
#13702=ORIENTED_EDGE ( 'NONE', *, *, #14661, .T. ) ;
#13707=CARTESIAN_POINT ( 'NONE',  ( 2.935661446561383503, 9.035036904804158553, 6.459589141758144137 ) ) ;
#13718=CARTESIAN_POINT ( 'NONE',  ( -2.682529543900285862, 8.255977015246234174, -5.233165578109188587 ) ) ;
#13739=CARTESIAN_POINT ( 'NONE',  ( -6.233975306307045953E-13, 9.127583699786111282, -5.133165578109188054 ) ) ;
#13749=( BOUNDED_SURFACE ( )  B_SPLINE_SURFACE ( 1, 2, ( 
 ( #8181, #22978, #22867, #15624, #406, #10132, #20910, #23093, #4681, #2349, #19324, #12084, #19557, #17585, #4439, #11603, #889, #9898, #13579, #6382, #19073, #10016, #15513, #22732, #6513, #13825, #2719, #7812, #6016, #660, #21274, #9762, #21021, #8316, #6138, #13455, #528, #15253, #11969, #17222, #4196, #15396, #4310, #2832, #11715, #8067, #15770, #2474, #17357, #23235, #13950, #6249, #17104, #17967, #21756, #5046, #8916, #14528, #14061, #12344, #18096, #4931, #21508, #16357, #17855, #19814, #14176, #2971, #1389, #3086, #10506, #8556, #21993, #1254, #23815, #20169, #10268, #12458, #8675, #23709, #5275, #16002, #21635, #3192, #12572, #10400, #23594, #16131, #6872, #19919, #8808, #14295, #16252, #6980, #21866, #12706, #5146 ),
 ( #20044, #3325, #10747, #18216, #1141, #1506, #6744, #7089, #17724, #1027, #8448, #15896, #23355, #2076, #12931, #16957, #1732, #10856, #3909, #23941, #5500, #9033, #13286, #5859, #13170, #18324, #14875, #11090, #20386, #12817, #5755, #18794, #20525, #16482, #7214, #3678, #18574, #7431, #14657, #22351, #9373, #5395, #14998, #22127, #24, #3549, #20627, #10963, #7675, #7552, #22479, #11317, #5632, #13059, #9503, #1850, #272, #3798, #9270, #15113, #18443, #18679, #11207, #22578, #3445, #16717, #1609, #1951, #20274, #16825, #144, #9158, #16607, #24051, #7330, #14770, #22230, #17557, #15486, #21106, #23063, #13424, #20882, #18927, #745, #22696, #497, #15363, #2441, #4172, #9867, #4410, #859, #11451, #9988, #9629, #17324 ) ),
 .UNSPECIFIED., .F., .F., .T. ) 
 B_SPLINE_SURFACE_WITH_KNOTS ( ( 2, 2 ),
 ( 3, 2, 2, 2, 2, 2, 2, 2, 2, 2, 2, 2, 2, 2, 2, 2, 2, 2, 2, 2, 2, 2, 2, 2, 2, 2, 2, 2, 2, 2, 2, 2, 2, 2, 2, 2, 2, 2, 2, 2, 2, 2, 2, 2, 2, 2, 2, 2, 3 ),
 ( 0.000000000000000000, 1.000000000000000000 ),
 ( 0.000000000000000000, 0.02000000000000000042, 0.04000000000000000083, 0.05999999999999999778, 0.08000000000000000167, 0.1000000000000000056, 0.1199999999999999956, 0.1400000000000000133, 0.1600000000000000033, 0.1799999999999999933, 0.2000000000000000111, 0.2200000000000000011, 0.2399999999999999911, 0.2600000000000000089, 0.2800000000000000266, 0.2999999999999999889, 0.3200000000000000067, 0.3400000000000000244, 0.3599999999999999867, 0.3800000000000000044, 0.4000000000000000222, 0.4199999999999999845, 0.4400000000000000022, 0.4600000000000000200, 0.4799999999999999822, 0.5000000000000000000, 0.5200000000000000178, 0.5400000000000000355, 0.5600000000000000533, 0.5799999999999999600, 0.5999999999999999778, 0.6199999999999999956, 0.6400000000000000133, 0.6600000000000000311, 0.6800000000000000488, 0.6999999999999999556, 0.7199999999999999734, 0.7399999999999999911, 0.7600000000000000089, 0.7800000000000000266, 0.8000000000000000444, 0.8199999999999999512, 0.8399999999999999689, 0.8599999999999999867, 0.8800000000000000044, 0.9000000000000000222, 0.9200000000000000400, 0.9399999999999999467, 0.9500000000000000666 ),
 .UNSPECIFIED. ) 
 GEOMETRIC_REPRESENTATION_ITEM ( )  RATIONAL_B_SPLINE_SURFACE ( (
 ( 1.000000000000000000, 0.9510565162951535312, 1.000000000000000000, 0.9510565162951535312, 1.000000000000000000, 0.9510565162951535312, 1.000000000000000000, 0.9510565162951535312, 1.000000000000000000, 0.9510565162951535312, 1.000000000000000000, 0.9510565162951535312, 1.000000000000000000, 0.9510565162951535312, 1.000000000000000000, 0.9510565162951535312, 1.000000000000000000, 0.9510565162951535312, 1.000000000000000000, 0.9510565162951535312, 1.000000000000000000, 0.9510565162951535312, 1.000000000000000000, 0.9510565162951535312, 1.000000000000000000, 0.9510565162951535312, 1.000000000000000000, 0.9510565162951535312, 1.000000000000000000, 0.9510565162951535312, 1.000000000000000000, 0.9510565162951535312, 1.000000000000000000, 0.9510565162951535312, 1.000000000000000000, 0.9510565162951535312, 1.000000000000000000, 0.9510565162951535312, 1.000000000000000000, 0.9510565162951535312, 1.000000000000000000, 0.9510565162951535312, 1.000000000000000000, 0.9510565162951535312, 1.000000000000000000, 0.9510565162951535312, 1.000000000000000000, 0.9510565162951535312, 1.000000000000000000, 0.9510565162951535312, 1.000000000000000000, 0.9510565162951535312, 1.000000000000000000, 0.9510565162951535312, 1.000000000000000000, 0.9510565162951535312, 1.000000000000000000, 0.9510565162951535312, 1.000000000000000000, 0.9510565162951535312, 1.000000000000000000, 0.9510565162951535312, 1.000000000000000000, 0.9510565162951535312, 1.000000000000000000, 0.9510565162951535312, 1.000000000000000000, 0.9510565162951535312, 1.000000000000000000, 0.9510565162951535312, 1.000000000000000000, 0.9510565162951535312, 1.000000000000000000, 0.9510565162951535312, 1.000000000000000000, 0.9510565162951535312, 1.000000000000000000, 0.9510565162951535312, 1.000000000000000000, 0.9510565162951535312, 1.000000000000000000, 0.9510565162951535312, 1.000000000000000000, 0.9510565162951535312, 1.000000000000000000, 0.9510565162951535312, 1.000000000000000000, 0.9510565162951535312, 1.000000000000000000, 0.9510565162951535312, 1.000000000000000000, 0.9510565162951535312, 1.000000000000000000, 0.9510565162951535312, 1.000000000000000000, 0.9755282581475764880, 0.9755282581475768211),
 ( 1.000000000000000000, 0.9510565162951535312, 1.000000000000000000, 0.9510565162951535312, 1.000000000000000000, 0.9510565162951535312, 1.000000000000000000, 0.9510565162951535312, 1.000000000000000000, 0.9510565162951535312, 1.000000000000000000, 0.9510565162951535312, 1.000000000000000000, 0.9510565162951535312, 1.000000000000000000, 0.9510565162951535312, 1.000000000000000000, 0.9510565162951535312, 1.000000000000000000, 0.9510565162951535312, 1.000000000000000000, 0.9510565162951535312, 1.000000000000000000, 0.9510565162951535312, 1.000000000000000000, 0.9510565162951535312, 1.000000000000000000, 0.9510565162951535312, 1.000000000000000000, 0.9510565162951535312, 1.000000000000000000, 0.9510565162951535312, 1.000000000000000000, 0.9510565162951535312, 1.000000000000000000, 0.9510565162951535312, 1.000000000000000000, 0.9510565162951535312, 1.000000000000000000, 0.9510565162951535312, 1.000000000000000000, 0.9510565162951535312, 1.000000000000000000, 0.9510565162951535312, 1.000000000000000000, 0.9510565162951535312, 1.000000000000000000, 0.9510565162951535312, 1.000000000000000000, 0.9510565162951535312, 1.000000000000000000, 0.9510565162951535312, 1.000000000000000000, 0.9510565162951535312, 1.000000000000000000, 0.9510565162951535312, 1.000000000000000000, 0.9510565162951535312, 1.000000000000000000, 0.9510565162951535312, 1.000000000000000000, 0.9510565162951535312, 1.000000000000000000, 0.9510565162951535312, 1.000000000000000000, 0.9510565162951535312, 1.000000000000000000, 0.9510565162951535312, 1.000000000000000000, 0.9510565162951535312, 1.000000000000000000, 0.9510565162951535312, 1.000000000000000000, 0.9510565162951535312, 1.000000000000000000, 0.9510565162951535312, 1.000000000000000000, 0.9510565162951535312, 1.000000000000000000, 0.9510565162951535312, 1.000000000000000000, 0.9510565162951535312, 1.000000000000000000, 0.9510565162951535312, 1.000000000000000000, 0.9510565162951535312, 1.000000000000000000, 0.9510565162951535312, 1.000000000000000000, 0.9510565162951535312, 1.000000000000000000, 0.9510565162951535312, 1.000000000000000000, 0.9510565162951535312, 1.000000000000000000, 0.9755282581475764880, 0.9755282581475768211) ) ) 
 REPRESENTATION_ITEM ( '' )  SURFACE ( )  );
#13750=CARTESIAN_POINT ( 'NONE',  ( 5.871322893123448239, 8.081182679344781405, -11.50674201446023126 ) ) ;
#13753=CARTESIAN_POINT ( 'NONE',  ( 9.500000000000209610, -3.086737114211962396, -9.959589141758145914 ) ) ;
#13756=CARTESIAN_POINT ( 'NONE',  ( 7.524481829284360046, -4.467250836390474156, 12.50000000000000178 ) ) ;
#13757=CARTESIAN_POINT ( 'NONE',  ( -9.500000000000211386, 3.086737114211961064, 4.106742014460232681 ) ) ;
#13772=EDGE_LOOP ( 'NONE', ( #9458, #7567, #9684 ) ) ;
#13773=CARTESIAN_POINT ( 'NONE',  ( -7.022953521754877748, -5.102474405760673015, -5.833165578109188232 ) ) ;
#13783=CARTESIAN_POINT ( 'NONE',  ( 2.682529543900284974, -8.255977015246234174, -12.23316557810919036 ) ) ;
#13787=CIRCLE ( 'NONE', #4445, 8.000000000000000000 ) ;
#13793=VERTEX_POINT ( 'NONE', #21981 ) ;
#13796=CARTESIAN_POINT ( 'NONE',  ( -2.094119113047911540, -8.892932511210149826, 12.37200713923885687 ) ) ;
#13804=CARTESIAN_POINT ( 'NONE',  ( 4.029965094393306726E-41, -5.916456789157588541E-28, -21.49999999999996803 ) ) ;
#13808=CARTESIAN_POINT ( 'NONE',  ( -9.500000000000000000, -6.482511860946779655E-13, -6.206742014460234103 ) ) ;
#13812=CARTESIAN_POINT ( 'NONE',  ( 7.022953521755574080, -5.102474405759714671, 8.433165578109187877 ) ) ;
#13825=CARTESIAN_POINT ( 'NONE',  ( 6.809999908187194197E-13, -9.988891130263535700, -10.70674201446023233 ) ) ;
#13829=CARTESIAN_POINT ( 'NONE',  ( -3.577580068923903234, -8.440353260633020938, -12.34099035630368491 ) ) ;
#13832=CARTESIAN_POINT ( 'NONE',  ( -2.285357169336379446, -9.225016725403595075, -3.500112653623174364 ) ) ;
#13838=DIRECTION ( 'NONE',  ( 0.000000000000000000, 0.000000000000000000, -1.000000000000000000 ) ) ;
#13846=CARTESIAN_POINT ( 'NONE',  ( 2.935661446561383503, 9.035036904804158553, 8.459589141758144137 ) ) ;
#13872=CARTESIAN_POINT ( 'NONE',  ( 9.499999999999790390, 3.086737114213260025, 4.159589141758142539 ) ) ;
#13873=AXIS2_PLACEMENT_3D ( 'NONE', #20181, #14673, #16268 ) ;
#13877=CARTESIAN_POINT ( 'NONE',  ( 2.682529543899157876, 8.255977015246598327, -7.033165578109189298 ) ) ;
#13882=CARTESIAN_POINT ( 'NONE',  ( -2.935661446562617183, 9.035036904803758873, 3.806742014460233303 ) ) ;
#13883=VECTOR ( 'NONE', #11888, 1000.000000000000000 ) ;
#13894=CARTESIAN_POINT ( 'NONE',  ( 7.937578510445358226, -3.514536757623690999, 12.49999999999999112 ) ) ;
#13909=CARTESIAN_POINT ( 'NONE',  ( -2.935661446562617183, 9.035036904803758873, -11.80674201446023375 ) ) ;
#13910=( BOUNDED_CURVE ( )  B_SPLINE_CURVE ( 2, ( #21491, #4786, #19679, #11700, #6235, #13676, #757, #10001, #15609, #22112, #8655 ),
 .UNSPECIFIED., .F., .T. ) 
 B_SPLINE_CURVE_WITH_KNOTS ( ( 3, 2, 2, 2, 2, 3 ),
 ( 0.3000000000000000999, 0.3200000000000001177, 0.3400000000000000799, 0.3600000000000000422, 0.3800000000000000044, 0.4000000000000000222 ),
 .UNSPECIFIED. ) 
 CURVE ( )  GEOMETRIC_REPRESENTATION_ITEM ( )  RATIONAL_B_SPLINE_CURVE ( ( 0.9999999999999997780, 0.9510565162951537532, 1.000000000000000000, 0.9510565162951535312, 1.000000000000000000, 0.9510565162951535312, 1.000000000000000000, 0.9510565162951535312, 1.000000000000000000, 0.9510565162951535312, 1.000000000000000000 ) ) 
 REPRESENTATION_ITEM ( '' )  );
#13912=CARTESIAN_POINT ( 'NONE',  ( 5.871322893124553133, -8.081182679343980269, 3.759589141758144404 ) ) ;
#13913=FACE_OUTER_BOUND ( 'NONE', #20437, .T. ) ;
#13914=ORIENTED_EDGE ( 'NONE', *, *, #6012, .F. ) ;
#13917=CARTESIAN_POINT ( 'NONE',  ( -5.871322893124554021, 8.081182679343978492, 2.759589141758142627 ) ) ;
#13937=CARTESIAN_POINT ( 'NONE',  ( 9.499999999999790390, 3.086737114213260025, -7.306742014460234635 ) ) ;
#13940=CARTESIAN_POINT ( 'NONE',  ( -2.682529543899159208, -8.255977015246598327, 10.03316557810918930 ) ) ;
#13950=CARTESIAN_POINT ( 'NONE',  ( -9.500000000000000000, -6.482511860946779655E-13, -8.206742014460234103 ) ) ;
#13969=CARTESIAN_POINT ( 'NONE',  ( -7.685661446562381371, 5.583959896777970222, 4.859589141758143604 ) ) ;
#13986=CARTESIAN_POINT ( 'NONE',  ( -2.935661446562617183, 9.035036904803758873, 5.806742014460233747 ) ) ;
#13991=CARTESIAN_POINT ( 'NONE',  ( 0.000000000000000000, 0.000000000000000000, -2.500000000000000000 ) ) ;
#13993=CARTESIAN_POINT ( 'NONE',  ( 8.680847955711007202, 5.912916378492122225E-13, -10.63316557810918894 ) ) ;
#13997=CARTESIAN_POINT ( 'NONE',  ( -1.504652183083727168, 9.499999999999904077, 3.757996296007079184 ) ) ;
#13999=DIRECTION ( 'NONE',  ( 0.000000000000000000, 0.000000000000000000, 1.000000000000000000 ) ) ;
#14001=ORIENTED_EDGE ( 'NONE', *, *, #13087, .T. ) ;
#14002=DIRECTION ( 'NONE',  ( -0.000000000000000000, -0.000000000000000000, -1.000000000000000000 ) ) ;
#14019=VERTEX_POINT ( 'NONE', #22572 ) ;
#14020=CARTESIAN_POINT ( 'NONE',  ( -5.622572944242076564E-13, 8.680847955711007202, -3.133165578109187166 ) ) ;
#14023=CARTESIAN_POINT ( 'NONE',  ( -9.500000000000000000, -6.482511860946779655E-13, 3.059589141758143338 ) ) ;
#14028=DIRECTION ( 'NONE',  ( 0.5000000000000002220, -0.8660254037844384856, 0.000000000000000000 ) ) ;
#14029=CARTESIAN_POINT ( 'NONE',  ( -2.352265130537441795, -9.224593858590012019, 3.479461880036843535 ) ) ;
#14049=EDGE_LOOP ( 'NONE', ( #4068, #22740, #14001 ) ) ;
#14050=CARTESIAN_POINT ( 'NONE',  ( 2.682529543899157876, 8.255977015246598327, 5.033165578109189298 ) ) ;
#14055=STYLED_ITEM('',(#24169),#18256);
#14061=CARTESIAN_POINT ( 'NONE',  ( 7.685661446561619314, 5.583959896779020049, -7.406742014460233392 ) ) ;
#14064=CARTESIAN_POINT ( 'NONE',  ( -7.037334108778454222, -6.010000779825212192, -12.25356292181664131 ) ) ;
#14079=CARTESIAN_POINT ( 'NONE',  ( 7.685661446562381371, -5.583959896777971110, 9.859589141758144493 ) ) ;
#14090=CARTESIAN_POINT ( 'NONE',  ( 0.000000000000000000, 0.000000000000000000, 12.50000000000000000 ) ) ;
#14094=CARTESIAN_POINT ( 'NONE',  ( 6.809999908187194197E-13, -9.988891130263535700, 4.706742014460233214 ) ) ;
#14098=CYLINDRICAL_SURFACE ( 'NONE', #4894, 9.500000000000000000 ) ;
#14099=CARTESIAN_POINT ( 'NONE',  ( 8.680847955710813579, 2.820578480814259326, -10.73316557810918681 ) ) ;
#14105=AXIS2_PLACEMENT_3D ( 'NONE', #23305, #19639, #6320 ) ;
#14115=CARTESIAN_POINT ( 'NONE',  ( 2.935661446561383503, 9.035036904804158553, -4.459589141758144137 ) ) ;
#14118=LINE ( 'NONE', #8244, #16211 ) ;
#14132=CARTESIAN_POINT ( 'NONE',  ( -5.365059087799947335, 7.384370330706355290, -3.333165578109187344 ) ) ;
#14135=CARTESIAN_POINT ( 'NONE',  ( -9.500000000000211386, 3.086737114211961064, 6.959589141758143249 ) ) ;
#14136=CARTESIAN_POINT ( 'NONE',  ( -5.871322893123450015, -8.081182679344781405, 4.506742014460231260 ) ) ;
#14137=VERTEX_POINT ( 'NONE', #16087 ) ;
#14157=ORIENTED_EDGE ( 'NONE', *, *, #7649, .T. ) ;
#14163=CARTESIAN_POINT ( 'NONE',  ( -5.871322893124554021, 8.081182679343978492, -6.759589141758143072 ) ) ;
#14166=ADVANCED_FACE ( 'NONE', ( #6595 ), #19521, .F. ) ;
#14167=CARTESIAN_POINT ( 'NONE',  ( -1.374911245008260785, 8.680847955710920161, 3.184419859656034468 ) ) ;
#14176=CARTESIAN_POINT ( 'NONE',  ( -2.935661446561384391, -9.035036904804158553, -6.606742014460233570 ) ) ;
#14185=DIRECTION ( 'NONE',  ( 0.000000000000000000, 0.000000000000000000, 1.000000000000000000 ) ) ;
#14187=CARTESIAN_POINT ( 'NONE',  ( -9.499999999999998224, 1.163414459189985485E-15, 3.499999999999999556 ) ) ;
#14190=DIRECTION ( 'NONE',  ( -0.000000000000000000, -0.000000000000000000, -1.000000000000000000 ) ) ;
#14197=VERTEX_POINT ( 'NONE', #19656 ) ;
#14210=CARTESIAN_POINT ( 'NONE',  ( 7.685661446562381371, -5.583959896777971110, 5.006742014460233037 ) ) ;
#14226=CARTESIAN_POINT ( 'NONE',  ( -2.682529543900285862, 8.255977015246234174, 5.233165578109188587 ) ) ;
#14232=CARTESIAN_POINT ( 'NONE',  ( -9.500000000000211386, 3.086737114211961064, -6.959589141758143249 ) ) ;
#14241=ADVANCED_FACE ( 'NONE', ( #4649 ), #8825, .F. ) ;
#14251=CARTESIAN_POINT ( 'NONE',  ( -6.233975306307046963E-13, 9.127583699786111282, -5.133165578109188054 ) ) ;
#14257=CARTESIAN_POINT ( 'NONE',  ( 7.685661446562381371, -5.583959896777971110, 13.00674201446023304 ) ) ;
#14258=CARTESIAN_POINT ( 'NONE',  ( 7.685661446561619314, 5.583959896779020049, 7.406742014460233392 ) ) ;
#14275=DIRECTION ( 'NONE',  ( 0.000000000000000000, 0.000000000000000000, 1.000000000000000000 ) ) ;
#14277=CARTESIAN_POINT ( 'NONE',  ( -7.152444901921760412, 6.260001551030978995, -3.501211579454638123 ) ) ;
#14286=CARTESIAN_POINT ( 'NONE',  ( -8.680847955711007202, -5.923547351154968927E-13, 5.633165578109188942 ) ) ;
#14292=ORIENTED_EDGE ( 'NONE', *, *, #69, .F. ) ;
#14295=CARTESIAN_POINT ( 'NONE',  ( -9.500000000000211386, 3.086737114211961064, -4.106742014460232681 ) ) ;
#14313=ORIENTED_EDGE ( 'NONE', *, *, #19437, .F. ) ;
#14334=CARTESIAN_POINT ( 'NONE',  ( 0.000000000000000000, 0.000000000000000000, 12.50000000000000000 ) ) ;
#14335=CARTESIAN_POINT ( 'NONE',  ( 2.682529543900284974, -8.255977015246234174, -4.233165578109187699 ) ) ;
#14345=CARTESIAN_POINT ( 'NONE',  ( 9.500000000000000000, 6.470877716354879437E-13, -8.059589141758143782 ) ) ;
#14352=CYLINDRICAL_SURFACE ( 'NONE', #1885, 9.500000000000000000 ) ;
#14365=CARTESIAN_POINT ( 'NONE',  ( -9.499999999999790390, -3.086737114213257804, -10.30674201446023375 ) ) ;
#14369=CARTESIAN_POINT ( 'NONE',  ( -6.822232771736903637E-13, 9.988891130263535700, 6.559589141758143782 ) ) ;
#14370=CARTESIAN_POINT ( 'NONE',  ( -9.500000000000211386, 3.086737114211961064, 8.106742014460232681 ) ) ;
#14391=CARTESIAN_POINT ( 'NONE',  ( 8.680847955711007202, 5.912916378492122225E-13, -8.633165578109188942 ) ) ;
#14397=CARTESIAN_POINT ( 'NONE',  ( -8.680847955711200825, 2.820578480813073607, 5.533165578109187521 ) ) ;
#14398=ORIENTED_EDGE ( 'NONE', *, *, #21024, .T. ) ;
#14406=EDGE_CURVE ( 'NONE', #15773, #23710, #5682, .T. ) ;
#14419=CARTESIAN_POINT ( 'NONE',  ( -7.685661446562381371, 5.583959896777970222, -4.006742014460233925 ) ) ;
#14420=CARTESIAN_POINT ( 'NONE',  ( 6.809999908187194197E-13, -9.988891130263535700, 3.559589141758143338 ) ) ;
#14437=APPLICATION_CONTEXT ( 'automotive_design' ) ;
#14441=CARTESIAN_POINT ( 'NONE',  ( 8.680847955711199049, -2.820578480813074496, -4.533165578109188409 ) ) ;
#14451=CIRCLE ( 'NONE', #19551, 9.000000000000001776 ) ;
#14456=CARTESIAN_POINT ( 'NONE',  ( 9.499999999999790390, 3.086737114213260025, -4.159589141758141650 ) ) ;
#14474=( NAMED_UNIT ( * ) PLANE_ANGLE_UNIT ( ) SI_UNIT ( $, .RADIAN. ) );
#14477=CARTESIAN_POINT ( 'NONE',  ( -9.500000000000211386, 3.086737114211961064, 10.10674201446023446 ) ) ;
#14479=CARTESIAN_POINT ( 'NONE',  ( -5.871322893124554021, 8.081182679343978492, 9.906742014460235168 ) ) ;
#14501=CARTESIAN_POINT ( 'NONE',  ( 5.871322893124551356, -8.081182679343980269, -11.75958914175814485 ) ) ;
#14502=CARTESIAN_POINT ( 'NONE',  ( 0.000000000000000000, 0.000000000000000000, -12.50000000000000000 ) ) ;
#14503=CARTESIAN_POINT ( 'NONE',  ( 6.222797240145152671E-13, -9.127583699786111282, -8.133165578109188942 ) ) ;
#14520=DIRECTION ( 'NONE',  ( -0.000000000000000000, -0.000000000000000000, 1.000000000000000000 ) ) ;
#14524=( BOUNDED_CURVE ( )  B_SPLINE_CURVE ( 2, ( #11109, #22014, #14419, #18462, #14784, #5165, #9052 ),
 .UNSPECIFIED., .F., .F. ) 
 B_SPLINE_CURVE_WITH_KNOTS ( ( 3, 2, 2, 3 ),
 ( 0.9000000000000000222, 0.9200000000000000400, 0.9399999999999999467, 0.9500000000000000666 ),
 .UNSPECIFIED. ) 
 CURVE ( )  GEOMETRIC_REPRESENTATION_ITEM ( )  RATIONAL_B_SPLINE_CURVE ( ( 1.000000000000000000, 0.9510565162951535312, 1.000000000000000000, 0.9510565162951535312, 1.000000000000000000, 0.9755282581475764880, 0.9755282581475768211 ) ) 
 REPRESENTATION_ITEM ( '' )  );
#14526=B_SPLINE_CURVE_WITH_KNOTS ( 'NONE', 3,
 ( #21869, #7218, #1508, #5279 ),
 .UNSPECIFIED., .F., .F.,
 ( 4, 4 ),
 ( 0.8197781486845410193, 1.000000000000000000 ),
 .UNSPECIFIED. ) ;
#14528=CARTESIAN_POINT ( 'NONE',  ( 5.871322893123449127, 8.081182679344781405, -7.506742014460233037 ) ) ;
#14566=CARTESIAN_POINT ( 'NONE',  ( -8.778978273663913257, 3.506149232160788110, 12.05025702049722547 ) ) ;
#14567=CARTESIAN_POINT ( 'NONE',  ( -2.935661446561384391, -9.035036904804158553, 10.60674201446023446 ) ) ;
#14571=CARTESIAN_POINT ( 'NONE',  ( -1.374911245008260785, 8.680847955710920161, -3.184419859656034468 ) ) ;
#14573=AXIS2_PLACEMENT_3D ( 'NONE', #9191, #1641, #16642 ) ;
#14584=CARTESIAN_POINT ( 'NONE',  ( -8.595784692538620320, 3.983312405694302782, -12.03999298932260409 ) ) ;
#14585=CARTESIAN_POINT ( 'NONE',  ( -9.500000000000000000, -6.482511860946779655E-13, -5.059589141758143782 ) ) ;
#14589=CARTESIAN_POINT ( 'NONE',  ( -5.622572944242077574E-13, 8.680847955711007202, 3.133165578109187610 ) ) ;
#14611=CARTESIAN_POINT ( 'NONE',  ( -9.500000000000211386, 3.086737114211961064, 12.10674201446023091 ) ) ;
#14612=CARTESIAN_POINT ( 'NONE',  ( -9.500000000000000000, -6.482511860946779655E-13, 6.206742014460234103 ) ) ;
#14634=DIRECTION ( 'NONE',  ( -1.000000000000000000, 0.000000000000000000, 0.000000000000000000 ) ) ;
#14636=DIRECTION ( 'NONE',  ( -1.000000000000000000, 1.224646799147351482E-16, 0.000000000000000000 ) ) ;
#14644=ORIENTED_EDGE ( 'NONE', *, *, #677, .T. ) ;
#14657=CARTESIAN_POINT ( 'NONE',  ( 7.685661446561619314, 5.583959896779020049, -8.259589141758144848 ) ) ;
#14661=EDGE_CURVE ( 'NONE', #19085, #5096, #9664, .T. ) ;
#14673=DIRECTION ( 'NONE',  ( 0.000000000000000000, 0.000000000000000000, 1.000000000000000000 ) ) ;
#14676=( BOUNDED_CURVE ( )  B_SPLINE_CURVE ( 2, ( #18078, #18202, #15991, #14163, #15881, #12553, #4921, #1243, #8657, #8904, #12441 ),
 .UNSPECIFIED., .F., .T. ) 
 B_SPLINE_CURVE_WITH_KNOTS ( ( 3, 2, 2, 2, 2, 3 ),
 ( 0.5000000000000000000, 0.5200000000000000178, 0.5400000000000000355, 0.5600000000000001643, 0.5800000000000000711, 0.6000000000000000888 ),
 .UNSPECIFIED. ) 
 CURVE ( )  GEOMETRIC_REPRESENTATION_ITEM ( )  RATIONAL_B_SPLINE_CURVE ( ( 1.000000000000000000, 0.9510565162951535312, 1.000000000000000000, 0.9510565162951535312, 1.000000000000000000, 0.9510565162951535312, 1.000000000000000000, 0.9510565162951535312, 1.000000000000000000, 0.9510565162951533091, 1.000000000000000222 ) ) 
 REPRESENTATION_ITEM ( '' )  );
#14677=CARTESIAN_POINT ( 'NONE',  ( -7.022953521754877748, -5.102474405760673015, 3.833165578109188676 ) ) ;
#14680=ORIENTED_EDGE ( 'NONE', *, *, #14661, .F. ) ;
#14686=AXIS2_PLACEMENT_3D ( 'NONE', #1012, #23221, #8437 ) ;
#14696=DIRECTION ( 'NONE',  ( 1.000000000000000000, 0.000000000000000000, 0.000000000000000000 ) ) ;
#14704=CARTESIAN_POINT ( 'NONE',  ( -7.022953521754877748, -5.102474405760673015, 7.833165578109188232 ) ) ;
#14705=ORIENTED_EDGE ( 'NONE', *, *, #10913, .T. ) ;
#14712=CARTESIAN_POINT ( 'NONE',  ( -8.680847955710813579, -2.820578480814258437, -9.733165578109186811 ) ) ;
#14722=CARTESIAN_POINT ( 'NONE',  ( 5.871322893124551356, -8.081182679343980269, -6.906742014460233392 ) ) ;
#14733=CARTESIAN_POINT ( 'NONE',  ( 5.871322893123449127, 8.081182679344781405, 7.506742014460233037 ) ) ;
#14734=VERTEX_POINT ( 'NONE', #21896 ) ;
#14753=CARTESIAN_POINT ( 'NONE',  ( -8.680847955711200825, 2.820578480813073607, -9.533165578109187521 ) ) ;
#14756=FACE_OUTER_BOUND ( 'NONE', #6017, .T. ) ;
#14764=CARTESIAN_POINT ( 'NONE',  ( -5.871322893124554021, 8.081182679343978492, -2.759589141758142627 ) ) ;
#14770=CARTESIAN_POINT ( 'NONE',  ( -6.822232771736903637E-13, 9.988891130263535700, -4.559589141758142894 ) ) ;
#14783=CARTESIAN_POINT ( 'NONE',  ( 7.937578510445358226, -3.514536757623690999, 12.49999999999999112 ) ) ;
#14784=CARTESIAN_POINT ( 'NONE',  ( -2.935661446562617183, 9.035036904803758873, -3.806742014460233303 ) ) ;
#14815=CARTESIAN_POINT ( 'NONE',  ( -7.022953521754877748, -5.102474405760673015, -7.833165578109188232 ) ) ;
#14828=DIRECTION ( 'NONE',  ( 0.7071067811865487940, 0.000000000000000000, 0.7071067811865463515 ) ) ;
#14837=CARTESIAN_POINT ( 'NONE',  ( -5.871322893123450015, -8.081182679344781405, 10.50674201446023304 ) ) ;
#14852=CARTESIAN_POINT ( 'NONE',  ( 0.000000000000000000, 0.000000000000000000, -12.50000000000000000 ) ) ;
#14861=DIRECTION ( 'NONE',  ( -0.000000000000000000, -0.000000000000000000, -1.000000000000000000 ) ) ;
#14862=EDGE_CURVE ( 'NONE', #9263, #13492, #18603, .T. ) ;
#14875=CARTESIAN_POINT ( 'NONE',  ( -2.935661446561384391, -9.035036904804158553, -9.459589141758144137 ) ) ;
#14901=CARTESIAN_POINT ( 'NONE',  ( -8.680847955711007202, -5.923547351154968927E-13, 3.633165578109188054 ) ) ;
#14914=DIRECTION ( 'NONE',  ( -0.000000000000000000, -0.000000000000000000, -1.000000000000000000 ) ) ;
#14923=EDGE_LOOP ( 'NONE', ( #1081, #16518, #19382, #22465 ) ) ;
#14926=CARTESIAN_POINT ( 'NONE',  ( -2.682529543899159208, -8.255977015246598327, 4.033165578109189298 ) ) ;
#14927=VERTEX_POINT ( 'NONE', #15567 ) ;
#14935=CARTESIAN_POINT ( 'NONE',  ( -9.499999999999790390, -3.086737114213257804, -3.159589141758143871 ) ) ;
#14948=CIRCLE ( 'NONE', #19262, 1.000000000000000888 ) ;
#14951=CARTESIAN_POINT ( 'NONE',  ( -7.685661446561619314, -5.583959896779019161, -7.259589141758143960 ) ) ;
#14953=CIRCLE ( 'NONE', #3684, 10.49999999999999822 ) ;
#14955=CARTESIAN_POINT ( 'NONE',  ( 7.564539288232062120, -4.357045548396844659, -12.46583266205519713 ) ) ;
#14961=SHAPE_REPRESENTATION_RELATIONSHIP ( 'NONE' , 'NONE' ,  #23456, #20093 ) ;
#14982=AXIS2_PLACEMENT_3D ( 'NONE', #17738, #13838, #6525 ) ;
#14990=CARTESIAN_POINT ( 'NONE',  ( 5.871322893124551356, -8.081182679343980269, -9.759589141758143072 ) ) ;
#14997=EDGE_CURVE ( 'NONE', #17352, #105, #5267, .T. ) ;
#14998=CARTESIAN_POINT ( 'NONE',  ( 7.685661446562381371, -5.583959896777971110, -7.859589141758143604 ) ) ;
#15000=AXIS2_PLACEMENT_3D ( 'NONE', #17071, #16714, #17187 ) ;
#15002=CARTESIAN_POINT ( 'NONE',  ( -7.561939491010504000, 5.750397476200735269, 11.99999999999999822 ) ) ;
#15012=CYLINDRICAL_SURFACE ( 'NONE', #9452, 9.500000000000000000 ) ;
#15013=ORIENTED_EDGE ( 'NONE', *, *, #8968, .T. ) ;
#15017=CARTESIAN_POINT ( 'NONE',  ( 10.49999999999999822, 0.000000000000000000, -2.499999999999999556 ) ) ;
#15034=EDGE_CURVE ( 'NONE', #17358, #13793, #10450, .T. ) ;
#15043=LINE ( 'NONE', #5789, #9139 ) ;
#15049=CARTESIAN_POINT ( 'NONE',  ( -5.871322893124554021, 8.081182679343978492, 10.75958914175814130 ) ) ;
#15059=CARTESIAN_POINT ( 'NONE',  ( -8.680847955711007202, -5.923547351154968927E-13, -7.633165578109188942 ) ) ;
#15074=CARTESIAN_POINT ( 'NONE',  ( -8.680847955711200825, 2.820578480813073607, -11.53316557810918752 ) ) ;
#15092=FACE_OUTER_BOUND ( 'NONE', #12700, .T. ) ;
#15105=CARTESIAN_POINT ( 'NONE',  ( -9.500000000000211386, 3.086737114211961064, 8.959589141758140585 ) ) ;
#15113=CARTESIAN_POINT ( 'NONE',  ( 9.499999999999790390, 3.086737114213260025, -6.159589141758145203 ) ) ;
#15115=CARTESIAN_POINT ( 'NONE',  ( -5.762672935462116008, 8.116485190583384579, 11.90304097605235967 ) ) ;
#15123=CARTESIAN_POINT ( 'NONE',  ( 9.499999999999799272, 3.086737114213245370, -7.306742014460232859 ) ) ;
#15142=EDGE_LOOP ( 'NONE', ( #17126, #9055, #17570, #22219 ) ) ;
#15145=CARTESIAN_POINT ( 'NONE',  ( -8.103571562645766946, -4.965588994209959139, -3.501545554889576639 ) ) ;
#15156=CARTESIAN_POINT ( 'NONE',  ( -2.682529543900285862, 8.255977015246234174, 7.233165578109188587 ) ) ;
#15163=CARTESIAN_POINT ( 'NONE',  ( -9.500000000000000000, 0.000000000000000000, 12.50000000000000000 ) ) ;
#15164=CARTESIAN_POINT ( 'NONE',  ( -6.153822176767817416E-13, 9.500000000000000000, -2.559589141758142450 ) ) ;
#15175=EDGE_CURVE ( 'NONE', #105, #5101, #2200, .T. ) ;
#15178=CARTESIAN_POINT ( 'NONE',  ( -5.976739099259236459E-13, 9.226949318570335734, 2.750781287208490689 ) ) ;
#15195=CARTESIAN_POINT ( 'NONE',  ( 5.021738411795485746, -7.393327316361921753, 12.50000000000000178 ) ) ;
#15199=CARTESIAN_POINT ( 'NONE',  ( -9.500000000000000000, -6.482511860946779655E-13, 11.05958914175814556 ) ) ;
#15213=CARTESIAN_POINT ( 'NONE',  ( 2.935661446562616295, -9.035036904803758873, 9.659589141758143427 ) ) ;
#15229=CARTESIAN_POINT ( 'NONE',  ( -2.468715102574523534, -8.804291563376645868, 12.36424688184530396 ) ) ;
#15238=CARTESIAN_POINT ( 'NONE',  ( 0.000000000000000000, 0.000000000000000000, 12.50000000000000000 ) ) ;
#15244=CARTESIAN_POINT ( 'NONE',  ( -6.233975306307045953E-13, 9.127583699786111282, 9.133165578109188942 ) ) ;
#15253=CARTESIAN_POINT ( 'NONE',  ( 5.871322893123449127, 8.081182679344781405, -9.506742014460231260 ) ) ;
#15262=AXIS2_PLACEMENT_3D ( 'NONE', #1990, #60, #16649 ) ;
#15276=ORIENTED_EDGE ( 'NONE', *, *, #16614, .T. ) ;
#15277=CARTESIAN_POINT ( 'NONE',  ( 5.871322893124553133, -8.081182679343980269, 11.75958914175814485 ) ) ;
#15284=AXIS2_PLACEMENT_3D ( 'NONE', #11308, #14861, #7542 ) ;
#15312=CARTESIAN_POINT ( 'NONE',  ( 9.500000000000200728, -3.086737114211976607, -5.959589141758144137 ) ) ;
#15319=CARTESIAN_POINT ( 'NONE',  ( -5.365059087798939252, -7.384370330707086261, 11.93316557810918965 ) ) ;
#15323=CARTESIAN_POINT ( 'NONE',  ( -7.685661446562381371, 5.583959896777970222, -10.85958914175814449 ) ) ;
#15329=CARTESIAN_POINT ( 'NONE',  ( 7.685661446562381371, -5.583959896777971110, 7.006742014460233037 ) ) ;
#15330=CARTESIAN_POINT ( 'NONE',  ( 9.499999999999790390, 3.086737114213260025, -5.306742014460231971 ) ) ;
#15336=EDGE_CURVE ( 'NONE', #3116, #9659, #9432, .T. ) ;
#15348=CARTESIAN_POINT ( 'NONE',  ( -2.935661446561384391, -9.035036904804158553, 11.45958914175814414 ) ) ;
#15363=CARTESIAN_POINT ( 'NONE',  ( -5.871322893123450015, -8.081182679344781405, -3.359589141758143160 ) ) ;
#15365=ORIENTED_EDGE ( 'NONE', *, *, #20141, .T. ) ;
#15371=CARTESIAN_POINT ( 'NONE',  ( -8.866614027893694683, 3.263134433186268613, 12.05545359443210529 ) ) ;
#15380=CARTESIAN_POINT ( 'NONE',  ( -2.935661446561384391, -9.035036904804158553, -6.606742014460233570 ) ) ;
#15383=CARTESIAN_POINT ( 'NONE',  ( -5.365059087798940141, -7.384370330707086261, 11.93316557810918965 ) ) ;
#15396=CARTESIAN_POINT ( 'NONE',  ( 9.500000000000209610, -3.086737114211962396, -9.106742014460232681 ) ) ;
#15401=ORIENTED_EDGE ( 'NONE', *, *, #5537, .T. ) ;
#15402=CARTESIAN_POINT ( 'NONE',  ( -9.264724873483777046, -2.172114814696820329, -3.499867591578571968 ) ) ;
#15417=CARTESIAN_POINT ( 'NONE',  ( 8.680847955711007202, 5.912916378492122225E-13, 6.633165578109188942 ) ) ;
#15424=ADVANCED_FACE ( 'NONE', ( #557 ), #7978, .T. ) ;
#15426=CARTESIAN_POINT ( 'NONE',  ( -7.022953521755574080, 5.102474405759713783, -3.433165578109189209 ) ) ;
#15428=VECTOR ( 'NONE', #2635, 1000.000000000000227 ) ;
#15445=CARTESIAN_POINT ( 'NONE',  ( -9.499999999999799272, -3.086737114213243593, -5.159589141758141650 ) ) ;
#15446=CARTESIAN_POINT ( 'NONE',  ( 5.365059087798939252, 7.384370330707087149, -6.933165578109188765 ) ) ;
#15453=( BOUNDED_CURVE ( )  B_SPLINE_CURVE ( 2, ( #8128, #13757, #1089, #15571, #8509, #23034, #21206 ),
 .UNSPECIFIED., .F., .F. ) 
 B_SPLINE_CURVE_WITH_KNOTS ( ( 3, 2, 2, 3 ),
 ( 0.9000000000000000222, 0.9200000000000000400, 0.9399999999999999467, 0.9500000000000000666 ),
 .UNSPECIFIED. ) 
 CURVE ( )  GEOMETRIC_REPRESENTATION_ITEM ( )  RATIONAL_B_SPLINE_CURVE ( ( 1.000000000000000000, 0.9510565162951535312, 1.000000000000000000, 0.9510565162951535312, 1.000000000000000000, 0.9755282581475764880, 0.9755282581475768211 ) ) 
 REPRESENTATION_ITEM ( '' )  );
#15459=ADVANCED_FACE ( 'NONE', ( #3442 ), #17235, .F. ) ;
#15461=CARTESIAN_POINT ( 'NONE',  ( 8.840695694414906214, -0.6121865488561712976, 12.50000000000000000 ) ) ;
#15462=CARTESIAN_POINT ( 'NONE',  ( 9.500000000000000000, 6.470877716354879437E-13, 7.206742014460234103 ) ) ;
#15463=ORIENTED_EDGE ( 'NONE', *, *, #18349, .T. ) ;
#15464=CARTESIAN_POINT ( 'NONE',  ( 8.871028110654306076, 6.042456644462176420E-13, -12.50000000000000000 ) ) ;
#15473=CARTESIAN_POINT ( 'NONE',  ( -6.233975306307046963E-13, 9.127583699786111282, -7.133165578109187166 ) ) ;
#15483=CARTESIAN_POINT ( 'NONE',  ( 5.998136232247421873, -6.550536670409211837, -12.49999999999999289 ) ) ;
#15486=CARTESIAN_POINT ( 'NONE',  ( 7.685661446561619314, 5.583959896779020049, -4.259589141758143960 ) ) ;
#15487=ORIENTED_EDGE ( 'NONE', *, *, #16477, .T. ) ;
#15490=CARTESIAN_POINT ( 'NONE',  ( 0.9852835067608223252, -9.043392810604785836, 12.43634207785451196 ) ) ;
#15495=CARTESIAN_POINT ( 'NONE',  ( 0.000000000000000000, 0.000000000000000000, 12.50000000000000000 ) ) ;
#15498=CARTESIAN_POINT ( 'NONE',  ( -6.822232771736903637E-13, 9.988891130263535700, -5.706742014460234103 ) ) ;
#15503=CARTESIAN_POINT ( 'NONE',  ( 8.680847955711007202, 5.912916378492122225E-13, 6.633165578109188942 ) ) ;
#15513=CARTESIAN_POINT ( 'NONE',  ( 7.685661446562381371, -5.583959896777971110, -11.00674201446023304 ) ) ;
#15524=DIRECTION ( 'NONE',  ( -1.000000000000000000, 1.224646799147351482E-16, 0.000000000000000000 ) ) ;
#15530=CARTESIAN_POINT ( 'NONE',  ( -9.500000000000000000, -6.482511860946779655E-13, 5.059589141758143782 ) ) ;
#15537=CARTESIAN_POINT ( 'NONE',  ( 7.022953521754877748, 5.102474405760673903, -6.833165578109188232 ) ) ;
#15538=CARTESIAN_POINT ( 'NONE',  ( -9.500000000000216716, 3.086737114211953514, 8.106742014460232681 ) ) ;
#15551=CARTESIAN_POINT ( 'NONE',  ( -5.799656021750657521E-13, 8.953898637140671468, 2.941973432658839371 ) ) ;
#15556=CARTESIAN_POINT ( 'NONE',  ( -2.682529543900285862, 8.255977015246234174, -9.233165578109188587 ) ) ;
#15562=CARTESIAN_POINT ( 'NONE',  ( 5.365059087799946447, -7.384370330706356178, 12.33316557810918646 ) ) ;
#15565=CARTESIAN_POINT ( 'NONE',  ( -5.762672935462112456, 8.116485190583386355, -11.90304097605236144 ) ) ;
#15567=CARTESIAN_POINT ( 'NONE',  ( -12.50000000000000178, 1.672973214995343413E-15, -2.500000000000000000 ) ) ;
#15568=CARTESIAN_POINT ( 'NONE',  ( 9.500000000000209610, -3.086737114211962396, -11.95958914175814591 ) ) ;
#15571=CARTESIAN_POINT ( 'NONE',  ( -5.871322893124554021, 8.081182679343978492, 3.906742014460231616 ) ) ;
#15591=CARTESIAN_POINT ( 'NONE',  ( 7.022953521755574080, -5.102474405759714671, -12.43316557810918788 ) ) ;
#15608=CARTESIAN_POINT ( 'NONE',  ( -6.822232771736904647E-13, 9.988891130263535700, -7.706742014460232326 ) ) ;
#15609=CARTESIAN_POINT ( 'NONE',  ( 7.685661446561619314, 5.583959896779020049, 8.259589141758144848 ) ) ;
#15612=CARTESIAN_POINT ( 'NONE',  ( 2.935661446561383503, 9.035036904804158553, -5.606742014460233570 ) ) ;
#15615=CARTESIAN_POINT ( 'NONE',  ( 6.222797240145152671E-13, -9.127583699786111282, 12.13316557810918717 ) ) ;
#15624=CARTESIAN_POINT ( 'NONE',  ( 5.871322893124553133, -8.081182679343980269, -12.90674201446023517 ) ) ;
#15626=ORIENTED_EDGE ( 'NONE', *, *, #5629, .F. ) ;
#15627=CARTESIAN_POINT ( 'NONE',  ( -7.751616505663432299, -5.097168108095969430, -12.23076385528166909 ) ) ;
#15645=CARTESIAN_POINT ( 'NONE',  ( -6.822232771736904647E-13, 9.988891130263535700, -4.559589141758142894 ) ) ;
#15648=CARTESIAN_POINT ( 'NONE',  ( -9.500000000000000000, -6.482511860946779655E-13, 7.059589141758143782 ) ) ;
#15651=ORIENTED_EDGE ( 'NONE', *, *, #9722, .T. ) ;
#15659=EDGE_CURVE ( 'NONE', #566, #21243, #131, .T. ) ;
#15662=CARTESIAN_POINT ( 'NONE',  ( 0.000000000000000000, 0.000000000000000000, 3.499999999999999556 ) ) ;
#15678=CARTESIAN_POINT ( 'NONE',  ( 7.022953521754877748, 5.102474405760673903, -4.833165578109188232 ) ) ;
#15687=CARTESIAN_POINT ( 'NONE',  ( -7.022953521754877748, -5.102474405760673015, 7.833165578109188232 ) ) ;
#15697=CARTESIAN_POINT ( 'NONE',  ( -9.500000000000000000, -6.482511860946779655E-13, -10.20674201446023233 ) ) ;
#15715=CARTESIAN_POINT ( 'NONE',  ( -7.685661446562381371, 5.583959896777970222, -12.00674201446023481 ) ) ;
#15719=CARTESIAN_POINT ( 'NONE',  ( 7.685661446562381371, -5.583959896777971110, 5.859589141758143604 ) ) ;
#15728=AXIS2_PLACEMENT_3D ( 'NONE', #14334, #10783, #1541 ) ;
#15744=DIRECTION ( 'NONE',  ( -0.000000000000000000, -0.000000000000000000, 1.000000000000000000 ) ) ;
#15746=CARTESIAN_POINT ( 'NONE',  ( -9.500000000000000000, -6.482511860946779655E-13, -5.059589141758143782 ) ) ;
#15758=CARTESIAN_POINT ( 'NONE',  ( -5.365059087799948223, 7.384370330706355290, 11.33316557810918646 ) ) ;
#15763=CARTESIAN_POINT ( 'NONE',  ( -7.685661446561619314, -5.583959896779019161, 5.259589141758143960 ) ) ;
#15770=CARTESIAN_POINT ( 'NONE',  ( -2.935661446561384391, -9.035036904804158553, -8.606742014460234458 ) ) ;
#15773=VERTEX_POINT ( 'NONE', #23326 ) ;
#15774=CARTESIAN_POINT ( 'NONE',  ( -7.287171073162196144, -5.717079508223483764, -12.24592425542296148 ) ) ;
#15789=CARTESIAN_POINT ( 'NONE',  ( 7.685661446562381371, -5.583959896777971110, 5.859589141758143604 ) ) ;
#15790=ORIENTED_EDGE ( 'NONE', *, *, #21885, .T. ) ;
#15798=DIRECTION ( 'NONE',  ( 1.000000000000000000, 6.811450227741984732E-14, 0.000000000000000000 ) ) ;
#15814=CARTESIAN_POINT ( 'NONE',  ( 9.000000000000001776, 1.102182119232617911E-15, 12.50000000000000000 ) ) ;
#15817=DIRECTION ( 'NONE',  ( -0.000000000000000000, -0.000000000000000000, -1.000000000000000000 ) ) ;
#15818=CARTESIAN_POINT ( 'NONE',  ( 8.680847955711007202, 5.912916378492122225E-13, -6.633165578109188942 ) ) ;
#15824=CARTESIAN_POINT ( 'NONE',  ( 8.680847955711199049, -2.820578480813074496, 10.53316557810918752 ) ) ;
#15854=CARTESIAN_POINT ( 'NONE',  ( -5.871322893124554021, 8.081182679343978492, 4.759589141758144848 ) ) ;
#15862=CARTESIAN_POINT ( 'NONE',  ( -6.153822176767817416E-13, 9.500000000000000000, 2.559589141758142894 ) ) ;
#15876=CARTESIAN_POINT ( 'NONE',  ( 9.301232020971124115, 6.335487896752474877E-13, 12.19876797902887233 ) ) ;
#15881=CARTESIAN_POINT ( 'NONE',  ( -2.935661446562617183, 9.035036904803758873, -6.659589141758144315 ) ) ;
#15882=ORIENTED_EDGE ( 'NONE', *, *, #12548, .F. ) ;
#15883=CARTESIAN_POINT ( 'NONE',  ( -5.365059087799948223, 7.384370330706355290, 3.333165578109187344 ) ) ;
#15888=LINE ( 'NONE', #21266, #9040 ) ;
#15891=CARTESIAN_POINT ( 'NONE',  ( 3.934052222107162766, -8.094642247421043990, -12.50000000000000000 ) ) ;
#15893=ORIENTED_EDGE ( 'NONE', *, *, #8119, .F. ) ;
#15896=CARTESIAN_POINT ( 'NONE',  ( -9.500000000000211386, 3.086737114211961064, -10.95958914175814414 ) ) ;
#15899=CARTESIAN_POINT ( 'NONE',  ( 9.500000000000000000, 1.163414459189985485E-15, -3.499999999999999556 ) ) ;
#15907=DIRECTION ( 'NONE',  ( -0.000000000000000000, -0.000000000000000000, -1.000000000000000000 ) ) ;
#15915=CARTESIAN_POINT ( 'NONE',  ( 7.685661446562381371, -5.583959896777971110, 7.859589141758143604 ) ) ;
#15927=CARTESIAN_POINT ( 'NONE',  ( -5.871322893123449127, -8.081182679344781405, -8.506742014460233037 ) ) ;
#15929=CARTESIAN_POINT ( 'NONE',  ( 7.685661446561619314, 5.583959896779020049, 5.406742014460233392 ) ) ;
#15930=CARTESIAN_POINT ( 'NONE',  ( 9.500000000000000000, 6.470877716354879437E-13, 4.059589141758143782 ) ) ;
#15931=CARTESIAN_POINT ( 'NONE',  ( -7.685661446562381371, 5.583959896777970222, 4.859589141758143604 ) ) ;
#15933=DIRECTION ( 'NONE',  ( 1.000000000000000000, 0.000000000000000000, 0.000000000000000000 ) ) ;
#15935=CARTESIAN_POINT ( 'NONE',  ( -8.680847955710813579, -2.820578480814257549, -7.733165578109188587 ) ) ;
#15941=CARTESIAN_POINT ( 'NONE',  ( 2.682529543900284974, -8.255977015246234174, 4.233165578109187699 ) ) ;
#15944=CARTESIAN_POINT ( 'NONE',  ( 9.500000000000000000, 6.470877716354879437E-13, -11.20674201446023410 ) ) ;
#15947=CARTESIAN_POINT ( 'NONE',  ( -7.685661446561619314, -5.583959896779019161, -5.259589141758143960 ) ) ;
#15949=DIRECTION ( 'NONE',  ( 1.000000000000000000, 6.811450227741984732E-14, -0.000000000000000000 ) ) ;
#15962=CARTESIAN_POINT ( 'NONE',  ( 9.500000000000000000, 6.470877716354879437E-13, 5.206742014460234103 ) ) ;
#15964=CARTESIAN_POINT ( 'NONE',  ( 5.365059087799946447, -7.384370330706356178, -4.333165578109189120 ) ) ;
#15967=CARTESIAN_POINT ( 'NONE',  ( -2.935661446562617183, 9.035036904803758873, 4.659589141758143427 ) ) ;
#15968=CARTESIAN_POINT ( 'NONE',  ( 5.871322893123449127, 8.081182679344781405, 7.506742014460233037 ) ) ;
#15980=EDGE_CURVE ( 'NONE', #4813, #3733, #23728, .T. ) ;
#15986=FACE_OUTER_BOUND ( 'NONE', #18846, .T. ) ;
#15991=CARTESIAN_POINT ( 'NONE',  ( -7.685661446562381371, 5.583959896777970222, -6.859589141758143604 ) ) ;
#16002=CARTESIAN_POINT ( 'NONE',  ( 9.500000000000209610, -3.086737114211962396, -5.106742014460234458 ) ) ;
#16003=EDGE_LOOP ( 'NONE', ( #13481, #9931, #195, #2133 ) ) ;
#16014=CARTESIAN_POINT ( 'NONE',  ( 9.090423977855502713, 6.191897047423500831E-13, -12.34637735993366725 ) ) ;
#16018=CARTESIAN_POINT ( 'NONE',  ( -6.153822176767817416E-13, 9.500000000000000000, -2.559589141758142894 ) ) ;
#16022=CARTESIAN_POINT ( 'NONE',  ( -5.871322893123450015, -8.081182679344781405, 9.359589141758146269 ) ) ;
#16032=EDGE_CURVE ( 'NONE', #19051, #8084, #23869, .T. ) ;
#16051=CARTESIAN_POINT ( 'NONE',  ( -7.022953521755574080, 5.102474405759713783, 7.433165578109188765 ) ) ;
#16060=CARTESIAN_POINT ( 'NONE',  ( 7.685661446561619314, 5.583959896779020049, -4.259589141758143960 ) ) ;
#16061=CARTESIAN_POINT ( 'NONE',  ( -6.153822176767817416E-13, 9.500000000000000000, 3.499999999999999556 ) ) ;
#16066=CARTESIAN_POINT ( 'NONE',  ( 6.250000000000000000, 10.82531754730548279, 2.500000000000000000 ) ) ;
#16078=ORIENTED_EDGE ( 'NONE', *, *, #6558, .F. ) ;
#16079=CARTESIAN_POINT ( 'NONE',  ( -2.682529543900285862, 8.255977015246234174, -3.233165578109188587 ) ) ;
#16083=CARTESIAN_POINT ( 'NONE',  ( 9.500000000000000000, 6.470877716354879437E-13, 13.20674201446023410 ) ) ;
#16084=CARTESIAN_POINT ( 'NONE',  ( 9.500000000000000000, 6.470877716354879437E-13, 9.206742014460234103 ) ) ;
#16087=CARTESIAN_POINT ( 'NONE',  ( 9.500000000000000000, 6.470877716354879437E-13, -4.059589141758143782 ) ) ;
#16107=CARTESIAN_POINT ( 'NONE',  ( -8.534735993385114128, 4.219016916012935603, -3.499350572060046183 ) ) ;
#16119=CARTESIAN_POINT ( 'NONE',  ( 6.222797240145152671E-13, -9.127583699786111282, 4.133165578109187166 ) ) ;
#16131=CARTESIAN_POINT ( 'NONE',  ( -5.871322893123450015, -8.081182679344781405, -4.506742014460231260 ) ) ;
#16141=CARTESIAN_POINT ( 'NONE',  ( 2.935661446562616295, -9.035036904803758873, -3.659589141758142983 ) ) ;
#16146=CARTESIAN_POINT ( 'NONE',  ( -9.500000000000202505, 3.086737114211975275, -4.959589141758144137 ) ) ;
#16147=EDGE_CURVE ( 'NONE', #9633, #13492, #12347, .T. ) ;
#16155=AXIS2_PLACEMENT_3D ( 'NONE', #968, #6692, #2913 ) ;
#16167=CARTESIAN_POINT ( 'NONE',  ( 2.935661446562616295, -9.035036904803758873, 7.659589141758144315 ) ) ;
#16169=CIRCLE ( 'NONE', #14982, 9.500000000000000000 ) ;
#16181=AXIS2_PLACEMENT_3D ( 'NONE', #5380, #23576, #8790 ) ;
#16183=CARTESIAN_POINT ( 'NONE',  ( -6.233975306307046963E-13, 9.127583699786111282, 11.13316557810918894 ) ) ;
#16186=CARTESIAN_POINT ( 'NONE',  ( 6.222797240145152671E-13, -9.127583699786111282, 4.133165578109187166 ) ) ;
#16188=ADVANCED_FACE ( 'NONE', ( #16413 ), #8965, .T. ) ;
#16193=CARTESIAN_POINT ( 'NONE',  ( 9.500000000000000000, 6.470877716354879437E-13, -6.059589141758143782 ) ) ;
#16211=VECTOR ( 'NONE', #15949, 1000.000000000000000 ) ;
#16215=ORIENTED_EDGE ( 'NONE', *, *, #11117, .T. ) ;
#16216=CARTESIAN_POINT ( 'NONE',  ( -7.685661446561619314, -5.583959896779019161, 12.40674201446023339 ) ) ;
#16217=CARTESIAN_POINT ( 'NONE',  ( -5.871322893123450015, -8.081182679344781405, 6.506742014460233925 ) ) ;
#16233=CARTESIAN_POINT ( 'NONE',  ( -9.500000053420693646, 0.6115953479451512464, -3.501506748078538678 ) ) ;
#16234=LINE ( 'NONE', #12800, #20428 ) ;
#16238=ORIENTED_EDGE ( 'NONE', *, *, #23696, .T. ) ;
#16246=CARTESIAN_POINT ( 'NONE',  ( -1.504652183083727168, 9.499999999999904077, -2.610843423304989308 ) ) ;
#16248=( BOUNDED_CURVE ( )  B_SPLINE_CURVE ( 2, ( #1533, #8948, #16390, #20530, #7009, #3803, #22484, #18933, #5071, #3916, #3232 ),
 .UNSPECIFIED., .F., .T. ) 
 B_SPLINE_CURVE_WITH_KNOTS ( ( 3, 2, 2, 2, 2, 3 ),
 ( 0.7000000000000000666, 0.7200000000000000844, 0.7400000000000001021, 0.7600000000000000089, 0.7800000000000000266, 0.8000000000000000444 ),
 .UNSPECIFIED. ) 
 CURVE ( )  GEOMETRIC_REPRESENTATION_ITEM ( )  RATIONAL_B_SPLINE_CURVE ( ( 0.9999999999999997780, 0.9510565162951537532, 1.000000000000000000, 0.9510565162951535312, 1.000000000000000000, 0.9510565162951535312, 1.000000000000000000, 0.9510565162951535312, 1.000000000000000000, 0.9510565162951535312, 1.000000000000000000 ) ) 
 REPRESENTATION_ITEM ( '' )  );
#16252=CARTESIAN_POINT ( 'NONE',  ( -7.685661446562381371, 5.583959896777970222, -4.006742014460233925 ) ) ;
#16261=CARTESIAN_POINT ( 'NONE',  ( 5.871322893124551356, -8.081182679343980269, -3.759589141758144404 ) ) ;
#16268=DIRECTION ( 'NONE',  ( 1.000000000000000000, 0.000000000000000000, 0.000000000000000000 ) ) ;
#16269=CARTESIAN_POINT ( 'NONE',  ( -2.935661446562617183, 9.035036904803758873, 2.659589141758143871 ) ) ;
#16279=DIRECTION ( 'NONE',  ( -0.5000000000000001110, -0.8660254037844384856, 0.000000000000000000 ) ) ;
#16280=CARTESIAN_POINT ( 'NONE',  ( -9.500000000000000000, -6.482511860946779655E-13, 6.206742014460234103 ) ) ;
#16292=CARTESIAN_POINT ( 'NONE',  ( 7.022953521755574080, -5.102474405759714671, 10.43316557810918788 ) ) ;
#16298=CARTESIAN_POINT ( 'NONE',  ( -8.133158128751217575, 4.897985262767988068, -12.01970669115188350 ) ) ;
#16299=CARTESIAN_POINT ( 'NONE',  ( 6.809999908187194197E-13, -9.988891130263535700, -5.559589141758142894 ) ) ;
#16317=CARTESIAN_POINT ( 'NONE',  ( 9.500000000000209610, -3.086737114211962396, -9.106742014460232681 ) ) ;
#16321=CARTESIAN_POINT ( 'NONE',  ( -7.685661446562381371, 5.583959896777970222, 10.00674201446023481 ) ) ;
#16322=CARTESIAN_POINT ( 'NONE',  ( 7.685661446561619314, 5.583959896779020049, 5.406742014460233392 ) ) ;
#16340=CARTESIAN_POINT ( 'NONE',  ( -8.238183179803327150, 4.770819190637570983, -3.499164564451821224 ) ) ;
#16345=ORIENTED_EDGE ( 'NONE', *, *, #1849, .T. ) ;
#16357=CARTESIAN_POINT ( 'NONE',  ( 5.871322893124553133, -8.081182679343980269, -6.906742014460234280 ) ) ;
#16390=CARTESIAN_POINT ( 'NONE',  ( -7.685661446562381371, 5.583959896777970222, 6.006742014460233037 ) ) ;
#16394=CARTESIAN_POINT ( 'NONE',  ( 2.935661446562616295, -9.035036904803758873, 10.80674201446023197 ) ) ;
#16400=CARTESIAN_POINT ( 'NONE',  ( -8.680847955711200825, 2.820578480813073607, 11.53316557810918574 ) ) ;
#16411=CARTESIAN_POINT ( 'NONE',  ( -2.935661446561384391, -9.035036904804158553, -3.459589141758144137 ) ) ;
#16413=FACE_OUTER_BOUND ( 'NONE', #6472, .T. ) ;
#16417=CARTESIAN_POINT ( 'NONE',  ( 0.000000000000000000, 0.000000000000000000, 12.50000000000000000 ) ) ;
#16426=CARTESIAN_POINT ( 'NONE',  ( 9.500000000000209610, -3.086737114211962396, -11.10674201446023446 ) ) ;
#16431=CARTESIAN_POINT ( 'NONE',  ( 5.871322893124553133, -8.081182679343980269, 8.906742014460233392 ) ) ;
#16432=CARTESIAN_POINT ( 'NONE',  ( -2.935661446562617183, 9.035036904803758873, 7.806742014460233747 ) ) ;
#16438=CARTESIAN_POINT ( 'NONE',  ( -2.935661446561384391, -9.035036904804158553, -4.606742014460233570 ) ) ;
#16450=EDGE_LOOP ( 'NONE', ( #15882, #8971, #4311, #17964, #1996, #2038, #20731, #7177, #11683, #11250, #12299, #11359, #17156, #18531, #17572 ) ) ;
#16455=CARTESIAN_POINT ( 'NONE',  ( 6.250000000000000000, 10.82531754730548279, 2.500000000000000000 ) ) ;
#16457=EDGE_LOOP ( 'NONE', ( #9870, #15790, #182, #5639 ) ) ;
#16464=CIRCLE ( 'NONE', #7878, 1.000000000000000888 ) ;
#16467=ORIENTED_EDGE ( 'NONE', *, *, #8592, .T. ) ;
#16477=EDGE_CURVE ( 'NONE', #9290, #14927, #2510, .T. ) ;
#16482=CARTESIAN_POINT ( 'NONE',  ( -5.871322893124554021, 8.081182679343978492, -8.759589141758141295 ) ) ;
#16486=DIRECTION ( 'NONE',  ( 1.000000000000000000, 0.000000000000000000, 0.000000000000000000 ) ) ;
#16488=AXIS2_PLACEMENT_3D ( 'NONE', #23665, #18387, #8976 ) ;
#16501=DIRECTION ( 'NONE',  ( -1.000000000000000000, 0.000000000000000000, 0.000000000000000000 ) ) ;
#16518=ORIENTED_EDGE ( 'NONE', *, *, #16477, .F. ) ;
#16521=CARTESIAN_POINT ( 'NONE',  ( -9.383344417114237501, 0.2560680661589281315, 12.11665558288575184 ) ) ;
#16532=CARTESIAN_POINT ( 'NONE',  ( 5.365059087798938364, 7.384370330707087149, 8.933165578109186100 ) ) ;
#16541=CARTESIAN_POINT ( 'NONE',  ( 7.022953521755574080, -5.102474405759714671, -12.43316557810918788 ) ) ;
#16543=CARTESIAN_POINT ( 'NONE',  ( 9.090423977855502713, 6.191897047423500831E-13, 12.34637735993366725 ) ) ;
#16544=DIRECTION ( 'NONE',  ( -0.4999999999999998890, -0.8660254037844385966, 0.000000000000000000 ) ) ;
#16547=CYLINDRICAL_SURFACE ( 'NONE', #11369, 9.500000000000000000 ) ;
#16556=EDGE_CURVE ( 'NONE', #21563, #17766, #14953, .T. ) ;
#16558=CARTESIAN_POINT ( 'NONE',  ( -7.685661446561619314, -5.583959896779019161, -10.40674201446023339 ) ) ;
#16563=CARTESIAN_POINT ( 'NONE',  ( -2.935661446562617183, 9.035036904803758873, 7.806742014460233747 ) ) ;
#16581=CARTESIAN_POINT ( 'NONE',  ( 9.376681730866099684, -1.188761456322485532, -12.06692573382535016 ) ) ;
#16588=CARTESIAN_POINT ( 'NONE',  ( -2.682529543899159208, -8.255977015246598327, -10.03316557810918930 ) ) ;
#16591=CIRCLE ( 'NONE', #13873, 8.000000000000000000 ) ;
#16595=CARTESIAN_POINT ( 'NONE',  ( 2.935661446562616295, -9.035036904803758873, -9.659589141758143427 ) ) ;
#16605=TOROIDAL_SURFACE ( 'NONE', #22863, 10.49999999999999822, 1.000000000000000000 ) ;
#16607=CARTESIAN_POINT ( 'NONE',  ( -7.685661446562381371, 5.583959896777970222, -4.859589141758143604 ) ) ;
#16609=ORIENTED_EDGE ( 'NONE', *, *, #2189, .T. ) ;
#16614=EDGE_CURVE ( 'NONE', #5101, #21243, #4972, .T. ) ;
#16628=CARTESIAN_POINT ( 'NONE',  ( -2.682529543900285862, 8.255977015246234174, 3.233165578109188587 ) ) ;
#16635=DIRECTION ( 'NONE',  ( 0.8660254037844385966, -0.5000000000000003331, 0.000000000000000000 ) ) ;
#16642=DIRECTION ( 'NONE',  ( -1.000000000000000000, 0.000000000000000000, 0.000000000000000000 ) ) ;
#16649=DIRECTION ( 'NONE',  ( 1.000000000000000000, -6.750155989720951766E-14, 0.000000000000000000 ) ) ;
#16661=VERTEX_POINT ( 'NONE', #15899 ) ;
#16664=CARTESIAN_POINT ( 'NONE',  ( 2.682529543900284974, -8.255977015246234174, -10.23316557810918859 ) ) ;
#16667=DIRECTION ( 'NONE',  ( -1.000000000000000000, 0.000000000000000000, 0.000000000000000000 ) ) ;
#16669=VECTOR ( 'NONE', #22065, 1000.000000000000000 ) ;
#16671=ORIENTED_EDGE ( 'NONE', *, *, #13640, .T. ) ;
#16682=CARTESIAN_POINT ( 'NONE',  ( 2.935661446561383503, 9.035036904804158553, -9.606742014460232681 ) ) ;
#16684=ORIENTED_EDGE ( 'NONE', *, *, #11860, .T. ) ;
#16686=CARTESIAN_POINT ( 'NONE',  ( 9.500000000000000000, 6.470877716354879437E-13, 9.206742014460234103 ) ) ;
#16687=ORIENTED_EDGE ( 'NONE', *, *, #11929, .T. ) ;
#16689=EDGE_LOOP ( 'NONE', ( #2558, #22643, #1522, #10929 ) ) ;
#16693=CARTESIAN_POINT ( 'NONE',  ( -9.500000000000000000, -6.482511860946779655E-13, 9.059589141758143782 ) ) ;
#16701=CARTESIAN_POINT ( 'NONE',  ( 6.250000000000000000, 10.82531754730548279, 2.500000000000000000 ) ) ;
#16705=DIRECTION ( 'NONE',  ( -0.000000000000000000, -0.000000000000000000, -1.000000000000000000 ) ) ;
#16710=CIRCLE ( 'NONE', #21019, 9.500000000000000000 ) ;
#16714=DIRECTION ( 'NONE',  ( -0.000000000000000000, -0.000000000000000000, -1.000000000000000000 ) ) ;
#16717=CARTESIAN_POINT ( 'NONE',  ( 6.809999908187194197E-13, -9.988891130263535700, -5.559589141758142894 ) ) ;
#16733=CARTESIAN_POINT ( 'NONE',  ( 7.022953521755574080, -5.102474405759714671, 6.433165578109188765 ) ) ;
#16738=EDGE_CURVE ( 'NONE', #11511, #14734, #14526, .T. ) ;
#16754=CARTESIAN_POINT ( 'NONE',  ( 7.022953521754877748, 5.102474405760673903, 4.833165578109188232 ) ) ;
#16763=CARTESIAN_POINT ( 'NONE',  ( -5.365059087798939252, -7.384370330707086261, -9.933165578109189653 ) ) ;
#16767=DIRECTION ( 'NONE',  ( 1.000000000000000000, 6.811450227741984732E-14, 0.000000000000000000 ) ) ;
#16778=CARTESIAN_POINT ( 'NONE',  ( -5.871322893124554021, 8.081182679343978492, -8.759589141758144848 ) ) ;
#16782=CARTESIAN_POINT ( 'NONE',  ( 7.022953521755574080, -5.102474405759714671, -12.43316557810918788 ) ) ;
#16805=CARTESIAN_POINT ( 'NONE',  ( 5.871322893124551356, -8.081182679343980269, 4.906742014460232504 ) ) ;
#16806=ORIENTED_EDGE ( 'NONE', *, *, #2362, .F. ) ;
#16807=ORIENTED_EDGE ( 'NONE', *, *, #6203, .F. ) ;
#16808=CARTESIAN_POINT ( 'NONE',  ( -9.500000000000000000, 0.000000000000000000, 12.50000000000000000 ) ) ;
#16825=CARTESIAN_POINT ( 'NONE',  ( -9.499999999999790390, -3.086737114213257804, -5.159589141758141650 ) ) ;
#16852=VERTEX_POINT ( 'NONE', #15464 ) ;
#16862=ORIENTED_EDGE ( 'NONE', *, *, #5135, .F. ) ;
#16871=CARTESIAN_POINT ( 'NONE',  ( 9.500000000000000000, 1.163414459189985485E-15, 12.50000000000000000 ) ) ;
#16882=CARTESIAN_POINT ( 'NONE',  ( 9.500000000000000000, 6.470877716354879437E-13, 12.05958914175814378 ) ) ;
#16886=AXIS2_PLACEMENT_3D ( 'NONE', #9915, #2731, #786 ) ;
#16891=CARTESIAN_POINT ( 'NONE',  ( -5.365059087799947335, 7.384370330706355290, -11.33316557810918468 ) ) ;
#16901=CARTESIAN_POINT ( 'NONE',  ( 0.000000000000000000, 0.000000000000000000, 12.50000000000000000 ) ) ;
#16917=CARTESIAN_POINT ( 'NONE',  ( -9.500000000000000000, -6.482511860946779655E-13, 8.206742014460234103 ) ) ;
#16925=CARTESIAN_POINT ( 'NONE',  ( -7.685661446561619314, -5.583959896779019161, 9.259589141758143072 ) ) ;
#16932=CARTESIAN_POINT ( 'NONE',  ( 9.500000000000000000, 6.470877716354879437E-13, -10.05958914175814378 ) ) ;
#16935=CARTESIAN_POINT ( 'NONE',  ( 0.000000000000000000, 0.000000000000000000, 12.50000000000000000 ) ) ;
#16949=CARTESIAN_POINT ( 'NONE',  ( -7.685661446561619314, -5.583959896779019161, -9.259589141758143072 ) ) ;
#16950=ORIENTED_EDGE ( 'NONE', *, *, #18579, .T. ) ;
#16952=VECTOR ( 'NONE', #8748, 1000.000000000000000 ) ;
#16957=CARTESIAN_POINT ( 'NONE',  ( -6.822232771736903637E-13, 9.988891130263535700, -10.55958914175814378 ) ) ;
#16987=CARTESIAN_POINT ( 'NONE',  ( 5.871322893123448239, 8.081182679344781405, 9.506742014460231260 ) ) ;
#16990=CARTESIAN_POINT ( 'NONE',  ( -9.378401895172221003, -4.713374146359802882E-16, -12.12159810482778788 ) ) ;
#16995=CARTESIAN_POINT ( 'NONE',  ( -7.957653757147100215, -5.196064979199609191, -3.501362371312797706 ) ) ;
#16999=ORIENTED_EDGE ( 'NONE', *, *, #787, .F. ) ;
#17009=CARTESIAN_POINT ( 'NONE',  ( -5.365059087799947335, 7.384370330706355290, 5.333165578109189120 ) ) ;
#17017=CARTESIAN_POINT ( 'NONE',  ( 5.365059087798938364, 7.384370330707087149, -10.93316557810918788 ) ) ;
#17031=CARTESIAN_POINT ( 'NONE',  ( 2.935661446561383503, 9.035036904804158553, -8.459589141758144137 ) ) ;
#17035=CARTESIAN_POINT ( 'NONE',  ( -2.682529543900285862, 8.255977015246234174, -11.23316557810918859 ) ) ;
#17042=ORIENTED_EDGE ( 'NONE', *, *, #20070, .T. ) ;
#17044=CARTESIAN_POINT ( 'NONE',  ( -9.500000000000000000, 0.000000000000000000, 12.50000000000000000 ) ) ;
#17051=LINE ( 'NONE', #6542, #11768 ) ;
#17052=EDGE_CURVE ( 'NONE', #18218, #19938, #18886, .T. ) ;
#17071=CARTESIAN_POINT ( 'NONE',  ( 0.000000000000000000, 0.000000000000000000, 12.50000000000000000 ) ) ;
#17073=CARTESIAN_POINT ( 'NONE',  ( 4.379988124296556151, -7.836644668421599569, -12.50000000000000355 ) ) ;
#17091=CARTESIAN_POINT ( 'NONE',  ( 7.022953521754877748, 5.102474405760673903, 10.83316557810919001 ) ) ;
#17098=ORIENTED_EDGE ( 'NONE', *, *, #8255, .T. ) ;
#17104=CARTESIAN_POINT ( 'NONE',  ( -7.685661446562381371, 5.583959896777970222, -8.006742014460233037 ) ) ;
#17108=CARTESIAN_POINT ( 'NONE',  ( -5.733664283190738509, -7.594766265237401726, -3.500616659224041527 ) ) ;
#17119=ORIENTED_EDGE ( 'NONE', *, *, #3081, .T. ) ;
#17122=CARTESIAN_POINT ( 'NONE',  ( -5.365059087799947335, 7.384370330706355290, 3.333165578109187344 ) ) ;
#17126=ORIENTED_EDGE ( 'NONE', *, *, #17824, .T. ) ;
#17132=CARTESIAN_POINT ( 'NONE',  ( 2.682529543899157876, 8.255977015246598327, -7.033165578109189298 ) ) ;
#17133=EDGE_CURVE ( 'NONE', #22463, #22670, #8226, .T. ) ;
#17149=CARTESIAN_POINT ( 'NONE',  ( -5.365059087798940141, -7.384370330707086261, -11.93316557810918965 ) ) ;
#17152=ORIENTED_EDGE ( 'NONE', *, *, #6585, .T. ) ;
#17155=CARTESIAN_POINT ( 'NONE',  ( 2.682529543900284974, -8.255977015246234174, 8.233165578109190363 ) ) ;
#17156=ORIENTED_EDGE ( 'NONE', *, *, #6037, .F. ) ;
#17158=( BOUNDED_CURVE ( )  B_SPLINE_CURVE ( 2, ( #14783, #22244, #5516, #12949, #9645, #15615, #13443, #15383, #6128, #4559, #19065, #4302, #6369, #15758, #2224, #763, #395, #9888, #17091, #11704, #7802, #879, #9751, #18945, #11963, #19431, #13940, #19177, #6005, #2708, #2338, #10123, #21011, #8305, #17210, #15244, #17574, #23220, #21381, #2461, #22717, #8171, #13812, #20901, #6501, #11470, #4190, #6241, #11594, #10006, #517, #7933, #23082, #11842, #22853, #17345, #19311, #13569, #647, #8056, #15503, #22970, #13681, #21123, #21262, #4428, #2595, #17463, #10258, #18205, #14286, #14397, #12073, #17713, #12335, #8660, #14050, #8549, #21853, #10385, #1011, #21745, #1497, #12444, #19547, #16119, #19803, #21624, #21495, #6973, #20032, #5034, #8435, #15883, #4923, #14167, #23582 ),
 .UNSPECIFIED., .F., .F. ) 
 B_SPLINE_CURVE_WITH_KNOTS ( ( 3, 2, 2, 2, 2, 2, 2, 2, 2, 2, 2, 2, 2, 2, 2, 2, 2, 2, 2, 2, 2, 2, 2, 2, 2, 2, 2, 2, 2, 2, 2, 2, 2, 2, 2, 2, 2, 2, 2, 2, 2, 2, 2, 2, 2, 2, 2, 2, 3 ),
 ( 0.01324393663734861268, 0.02000000000000000042, 0.04000000000000000083, 0.05999999999999999778, 0.07999999999999998779, 0.1000000000000000056, 0.1199999999999999956, 0.1400000000000000133, 0.1600000000000000033, 0.1799999999999999933, 0.2000000000000000111, 0.2200000000000000011, 0.2399999999999999911, 0.2600000000000000089, 0.2800000000000000266, 0.2999999999999999889, 0.3200000000000000067, 0.3400000000000000244, 0.3599999999999999867, 0.3800000000000000044, 0.4000000000000000222, 0.4199999999999999845, 0.4400000000000000022, 0.4600000000000000200, 0.4799999999999999822, 0.5000000000000000000, 0.5200000000000000178, 0.5400000000000000355, 0.5600000000000000533, 0.5799999999999999600, 0.5999999999999999778, 0.6199999999999999956, 0.6400000000000000133, 0.6600000000000000311, 0.6800000000000000488, 0.6999999999999999556, 0.7199999999999999734, 0.7399999999999998801, 0.7600000000000000089, 0.7800000000000000266, 0.8000000000000000444, 0.8199999999999999512, 0.8399999999999999689, 0.8599999999999999867, 0.8800000000000000044, 0.9000000000000000222, 0.9200000000000000400, 0.9399999999999999467, 0.9500000000000000666 ),
 .UNSPECIFIED. ) 
 CURVE ( )  GEOMETRIC_REPRESENTATION_ITEM ( )  RATIONAL_B_SPLINE_CURVE ( ( 0.9781034501096583789, 0.9834667361450580847, 1.000000000000000000, 0.9510565162951535312, 1.000000000000000000, 0.9510565162951535312, 1.000000000000000000, 0.9510565162951535312, 1.000000000000000000, 0.9510565162951535312, 1.000000000000000000, 0.9510565162951535312, 1.000000000000000000, 0.9510565162951535312, 1.000000000000000000, 0.9510565162951535312, 1.000000000000000000, 0.9510565162951535312, 1.000000000000000000, 0.9510565162951535312, 1.000000000000000000, 0.9510565162951535312, 1.000000000000000000, 0.9510565162951535312, 1.000000000000000000, 0.9510565162951535312, 1.000000000000000000, 0.9510565162951535312, 1.000000000000000000, 0.9510565162951535312, 1.000000000000000000, 0.9510565162951535312, 1.000000000000000000, 0.9510565162951535312, 1.000000000000000000, 0.9510565162951535312, 1.000000000000000000, 0.9510565162951535312, 1.000000000000000000, 0.9510565162951535312, 1.000000000000000000, 0.9510565162951535312, 1.000000000000000000, 0.9510565162951535312, 1.000000000000000000, 0.9510565162951535312, 1.000000000000000000, 0.9510565162951535312, 1.000000000000000000, 0.9510565162951535312, 1.000000000000000000, 0.9510565162951535312, 1.000000000000000000, 0.9510565162951535312, 1.000000000000000000, 0.9510565162951535312, 1.000000000000000000, 0.9510565162951535312, 1.000000000000000000, 0.9510565162951535312, 1.000000000000000000, 0.9510565162951535312, 1.000000000000000000, 0.9510565162951535312, 1.000000000000000000, 0.9510565162951535312, 1.000000000000000000, 0.9510565162951535312, 1.000000000000000000, 0.9510565162951535312, 1.000000000000000000, 0.9510565162951535312, 1.000000000000000000, 0.9510565162951535312, 1.000000000000000000, 0.9510565162951535312, 1.000000000000000000, 0.9510565162951535312, 1.000000000000000000, 0.9510565162951535312, 1.000000000000000000, 0.9510565162951535312, 1.000000000000000000, 0.9510565162951535312, 1.000000000000000000, 0.9510565162951535312, 1.000000000000000000, 0.9510565162951535312, 1.000000000000000000, 0.9510565162951535312, 1.000000000000000000, 0.9510565162951535312, 1.000000000000000000, 0.9510565162951535312, 1.000000000000000000, 0.9755282581475764880, 0.9755282581475768211 ) ) 
 REPRESENTATION_ITEM ( '' )  );
#17160=AXIS2_PLACEMENT_3D ( 'NONE', #21261, #6126, #22852 ) ;
#17161=ORIENTED_EDGE ( 'NONE', *, *, #20141, .F. ) ;
#17173=CARTESIAN_POINT ( 'NONE',  ( -9.499999999999790390, -3.086737114213257804, 4.306742014460233747 ) ) ;
#17177=ORIENTED_EDGE ( 'NONE', *, *, #5462, .T. ) ;
#17179=CARTESIAN_POINT ( 'NONE',  ( 5.871322893123449127, 8.081182679344781405, 8.359589141758144493 ) ) ;
#17181=ADVANCED_FACE ( 'NONE', ( #9944 ), #14098, .T. ) ;
#17182=ORIENTED_EDGE ( 'NONE', *, *, #7021, .F. ) ;
#17187=DIRECTION ( 'NONE',  ( -1.000000000000000000, 0.000000000000000000, 0.000000000000000000 ) ) ;
#17197=CARTESIAN_POINT ( 'NONE',  ( 2.500152530714462085, -8.687388223084449024, 12.46832088299141716 ) ) ;
#17205=CARTESIAN_POINT ( 'NONE',  ( -5.871322893124554021, 8.081182679343978492, -5.906742014460233392 ) ) ;
#17210=CARTESIAN_POINT ( 'NONE',  ( -2.682529543900285862, 8.255977015246234174, 9.233165578109188587 ) ) ;
#17222=CARTESIAN_POINT ( 'NONE',  ( 9.499999999999790390, 3.086737114213260025, -9.306742014460233747 ) ) ;
#17223=VERTEX_POINT ( 'NONE', #4356 ) ;
#17231=AXIS2_PLACEMENT_3D ( 'NONE', #15495, #6121, #20895 ) ;
#17235=TOROIDAL_SURFACE ( 'NONE', #10234, 10.49999999999999822, 1.000000000000000000 ) ;
#17246=CARTESIAN_POINT ( 'NONE',  ( 7.022953521755574080, -5.102474405759714671, 6.433165578109188765 ) ) ;
#17252=CARTESIAN_POINT ( 'NONE',  ( 2.935661446562616295, -9.035036904803758873, 5.659589141758144315 ) ) ;
#17277=CARTESIAN_POINT ( 'NONE',  ( -8.680847955711007202, -5.923547351154968927E-13, -9.633165578109188942 ) ) ;
#17281=ORIENTED_EDGE ( 'NONE', *, *, #21264, .F. ) ;
#17282=CARTESIAN_POINT ( 'NONE',  ( -8.680847955711007202, -5.923547351154968927E-13, 9.633165578109188942 ) ) ;
#17284=CARTESIAN_POINT ( 'NONE',  ( -6.822232771736904647E-13, 9.988891130263535700, -11.70674201446023410 ) ) ;
#17290=CARTESIAN_POINT ( 'NONE',  ( 4.810877257134742457, -7.548248927254282314, 12.50000000000000000 ) ) ;
#17291=DIRECTION ( 'NONE',  ( -0.000000000000000000, -0.000000000000000000, 1.000000000000000000 ) ) ;
#17302=DIRECTION ( 'NONE',  ( -0.000000000000000000, -0.000000000000000000, -1.000000000000000000 ) ) ;
#17305=CARTESIAN_POINT ( 'NONE',  ( 8.000000000000000000, 0.000000000000000000, -12.50000000000000000 ) ) ;
#17308=CARTESIAN_POINT ( 'NONE',  ( 9.500000000000000000, 6.470877716354879437E-13, 5.206742014460234103 ) ) ;
#17310=CARTESIAN_POINT ( 'NONE',  ( 8.680847955711007202, 5.912916378492122225E-13, -6.633165578109188942 ) ) ;
#17314=CARTESIAN_POINT ( 'NONE',  ( 5.871322893124553133, -8.081182679343980269, 11.75958914175814485 ) ) ;
#17321=CARTESIAN_POINT ( 'NONE',  ( 3.934052222107162766, -8.094642247421043990, -12.50000000000000000 ) ) ;
#17324=CARTESIAN_POINT ( 'NONE',  ( -6.153822176767817416E-13, 9.500000000000000000, -2.559589141758142450 ) ) ;
#17329=ADVANCED_FACE ( 'NONE', ( #1775 ), #3478, .T. ) ;
#17345=CARTESIAN_POINT ( 'NONE',  ( -6.233975306307045953E-13, 9.127583699786111282, 7.133165578109187166 ) ) ;
#17352=VERTEX_POINT ( 'NONE', #23507 ) ;
#17354=AXIS2_PLACEMENT_3D ( 'NONE', #13991, #6432, #15933 ) ;
#17357=CARTESIAN_POINT ( 'NONE',  ( -7.685661446561619314, -5.583959896779019161, -8.406742014460233392 ) ) ;
#17358=VERTEX_POINT ( 'NONE', #20313 ) ;
#17380=CARTESIAN_POINT ( 'NONE',  ( -5.871322893123450015, -8.081182679344781405, 7.359589141758143604 ) ) ;
#17389=CARTESIAN_POINT ( 'NONE',  ( 7.022953521754877748, 5.102474405760673903, -4.833165578109188232 ) ) ;
#17398=DIRECTION ( 'NONE',  ( -1.000000000000000000, 0.000000000000000000, 0.000000000000000000 ) ) ;
#17406=CARTESIAN_POINT ( 'NONE',  ( -8.680847955710813579, -2.820578480814257549, -5.733165578109188587 ) ) ;
#17412=CARTESIAN_POINT ( 'NONE',  ( -5.365059087799947335, 7.384370330706355290, -11.33316557810918468 ) ) ;
#17413=CARTESIAN_POINT ( 'NONE',  ( 2.682529543900284974, -8.255977015246234174, 10.23316557810918859 ) ) ;
#17418=CARTESIAN_POINT ( 'NONE',  ( 9.499999999999790390, 3.086737114213260025, -10.15958914175814520 ) ) ;
#17424=EDGE_CURVE ( 'NONE', #17662, #9768, #20087, .T. ) ;
#17427=FACE_OUTER_BOUND ( 'NONE', #5907, .T. ) ;
#17432=CARTESIAN_POINT ( 'NONE',  ( 8.680847955711007202, 5.912916378492122225E-13, -4.633165578109188942 ) ) ;
#17435=CARTESIAN_POINT ( 'NONE',  ( 7.685661446562381371, -5.583959896777971110, 11.00674201446023304 ) ) ;
#17439=CARTESIAN_POINT ( 'NONE',  ( 8.680847955711199049, -2.820578480813074496, -12.53316557810918752 ) ) ;
#17442=CARTESIAN_POINT ( 'NONE',  ( -7.685661446562381371, 5.583959896777970222, 6.859589141758143604 ) ) ;
#17456=ORIENTED_EDGE ( 'NONE', *, *, #23282, .F. ) ;
#17460=CARTESIAN_POINT ( 'NONE',  ( 9.500000000000000000, 6.470877716354879437E-13, -7.206742014460234103 ) ) ;
#17463=CARTESIAN_POINT ( 'NONE',  ( -5.365059087798940141, -7.384370330707086261, 5.933165578109187877 ) ) ;
#17475=CARTESIAN_POINT ( 'NONE',  ( -8.835537148983579669, -3.054185505207691165, -12.18395005276799736 ) ) ;
#17483=AXIS2_PLACEMENT_3D ( 'NONE', #12435, #15744, #8539 ) ;
#17490=CARTESIAN_POINT ( 'NONE',  ( 9.499999999999790390, 3.086737114213260025, 4.159589141758141650 ) ) ;
#17500=CARTESIAN_POINT ( 'NONE',  ( -5.871322893124554021, 8.081182679343978492, 7.906742014460233392 ) ) ;
#17510=CARTESIAN_POINT ( 'NONE',  ( 2.935661446562616295, -9.035036904803758873, 3.659589141758142983 ) ) ;
#17514=CARTESIAN_POINT ( 'NONE',  ( -6.233975306307045953E-13, 9.127583699786111282, -7.133165578109187166 ) ) ;
#17520=CARTESIAN_POINT ( 'NONE',  ( 6.222797240145152671E-13, -9.127583699786111282, 12.13316557810918717 ) ) ;
#17521=EDGE_CURVE ( 'NONE', #18614, #3340, #13787, .T. ) ;
#17531=CARTESIAN_POINT ( 'NONE',  ( -2.935661446561384391, -9.035036904804158553, -10.60674201446023446 ) ) ;
#17536=CARTESIAN_POINT ( 'NONE',  ( -9.500000000000000000, 0.000000000000000000, 12.50000000000000000 ) ) ;
#17544=CARTESIAN_POINT ( 'NONE',  ( -7.022953521754877748, -5.102474405760673015, -3.833165578109188676 ) ) ;
#17555=CARTESIAN_POINT ( 'NONE',  ( 7.937578510445243651, -3.514536757623948127, -12.49999999999998046 ) ) ;
#17557=CARTESIAN_POINT ( 'NONE',  ( 5.871322893123449127, 8.081182679344781405, -4.359589141758143604 ) ) ;
#17570=ORIENTED_EDGE ( 'NONE', *, *, #2362, .T. ) ;
#17571=CARTESIAN_POINT ( 'NONE',  ( -2.935661446561384391, -9.035036904804158553, -8.606742014460234458 ) ) ;
#17572=ORIENTED_EDGE ( 'NONE', *, *, #24074, .F. ) ;
#17574=CARTESIAN_POINT ( 'NONE',  ( 2.682529543899157876, 8.255977015246598327, 9.033165578109187521 ) ) ;
#17576=CYLINDRICAL_SURFACE ( 'NONE', #14686, 8.000000000000000000 ) ;
#17583=VERTEX_POINT ( 'NONE', #2490 ) ;
#17585=CARTESIAN_POINT ( 'NONE',  ( -5.871322893124554021, 8.081182679343978492, -11.90674201446023339 ) ) ;
#17589=ADVANCED_FACE ( 'NONE', ( #4323 ), #6150, .F. ) ;
#17593=AXIS2_PLACEMENT_3D ( 'NONE', #605, #5841, #6089 ) ;
#17606=CARTESIAN_POINT ( 'NONE',  ( 9.499999999999790390, 3.086737114213260025, 6.159589141758145203 ) ) ;
#17614=CARTESIAN_POINT ( 'NONE',  ( 6.222797240145152671E-13, -9.127583699786111282, -6.133165578109188942 ) ) ;
#17619=CARTESIAN_POINT ( 'NONE',  ( -7.685661446562381371, 5.583959896777970222, -6.006742014460233037 ) ) ;
#17631=CARTESIAN_POINT ( 'NONE',  ( -2.935661446562617183, 9.035036904803758873, 4.659589141758143427 ) ) ;
#17635=CARTESIAN_POINT ( 'NONE',  ( -8.680847955711200825, 2.820578480813073607, -7.533165578109189298 ) ) ;
#17638=ORIENTED_EDGE ( 'NONE', *, *, #12455, .T. ) ;
#17644=CARTESIAN_POINT ( 'NONE',  ( 2.682529543900284974, -8.255977015246234174, 12.23316557810919036 ) ) ;
#17652=EDGE_CURVE ( 'NONE', #17850, #17766, #14948, .T. ) ;
#17662=VERTEX_POINT ( 'NONE', #1043 ) ;
#17674=CARTESIAN_POINT ( 'NONE',  ( -5.365059087798939252, -7.384370330707086261, -3.933165578109188321 ) ) ;
#17678=CARTESIAN_POINT ( 'NONE',  ( 2.935661446562616295, -9.035036904803758873, 3.659589141758142983 ) ) ;
#17679=CARTESIAN_POINT ( 'NONE',  ( 5.871322893124553133, -8.081182679343980269, 10.90674201446023339 ) ) ;
#17696=VERTEX_POINT ( 'NONE', #12098 ) ;
#17698=CARTESIAN_POINT ( 'NONE',  ( -9.378401895172215674, 3.550564238312661509E-15, 12.12159810482778077 ) ) ;
#17700=CARTESIAN_POINT ( 'NONE',  ( 9.366788983124298085, -0.5939584231415685478, 12.13321101687573922 ) ) ;
#17713=CARTESIAN_POINT ( 'NONE',  ( -5.365059087799948223, 7.384370330706355290, 5.333165578109190008 ) ) ;
#17724=CARTESIAN_POINT ( 'NONE',  ( -7.685661446561619314, -5.583959896779019161, -11.25958914175814307 ) ) ;
#17738=CARTESIAN_POINT ( 'NONE',  ( 0.000000000000000000, 0.000000000000000000, 11.99999999999999645 ) ) ;
#17746=CARTESIAN_POINT ( 'NONE',  ( 2.935661446562616295, -9.035036904803758873, 5.659589141758144315 ) ) ;
#17753=B_SPLINE_CURVE_WITH_KNOTS ( 'NONE', 3,
 ( #9871, #4290, #8046, #17197, #21110, #15490, #22957, #6354, #2811, #13796, #15229, #21245, #6227, #4413, #13556, #23204, #10241, #11952, #11581, #19056, #2328, #19419, #20998, #11822, #2696, #17698 ),
 .UNSPECIFIED., .F., .F.,
 ( 4, 2, 2, 2, 2, 2, 2, 2, 2, 2, 2, 2, 4 ),
 ( 0.000000000000000000, 0.001163219550936220315, 0.002326439101872440629, 0.004652878203744879523, 0.005816097754681098971, 0.006979317305617317550, 0.008142536856553536997, 0.009305756407489757312, 0.01163219550936219794, 0.01395863461123463684, 0.01512185416217085715, 0.01628507371310707399, 0.01861151281497951115 ),
 .UNSPECIFIED. ) ;
#17766=VERTEX_POINT ( 'NONE', #3212 ) ;
#17775=CARTESIAN_POINT ( 'NONE',  ( 7.022953521754877748, 5.102474405760673903, -10.83316557810919001 ) ) ;
#17779=CARTESIAN_POINT ( 'NONE',  ( 5.365059087799947335, -7.384370330706356178, -10.33316557810918823 ) ) ;
#17783=CARTESIAN_POINT ( 'NONE',  ( -5.622572944242076564E-13, 8.680847955711007202, 3.133165578109187166 ) ) ;
#17788=CARTESIAN_POINT ( 'NONE',  ( 2.935661446561383503, 9.035036904804158553, -11.60674201446023268 ) ) ;
#17794=EDGE_CURVE ( 'NONE', #8782, #21563, #18468, .T. ) ;
#17796=CARTESIAN_POINT ( 'NONE',  ( -6.153822176767817416E-13, 9.500000000000000000, 2.873059427838761781 ) ) ;
#17800=DIRECTION ( 'NONE',  ( -0.000000000000000000, -0.000000000000000000, -1.000000000000000000 ) ) ;
#17810=CARTESIAN_POINT ( 'NONE',  ( -2.682529543900285862, 8.255977015246234174, -5.233165578109188587 ) ) ;
#17815=CARTESIAN_POINT ( 'NONE',  ( -9.500000000000000000, -6.482511860946779655E-13, 5.059589141758143782 ) ) ;
#17816=CARTESIAN_POINT ( 'NONE',  ( -9.499999999999790390, -3.086737114213257804, 10.30674201446023375 ) ) ;
#17823=CARTESIAN_POINT ( 'NONE',  ( 9.500000000000000000, 6.470877716354879437E-13, 6.059589141758143782 ) ) ;
#17824=EDGE_CURVE ( 'NONE', #14019, #11511, #244, .T. ) ;
#17830=( BOUNDED_CURVE ( )  B_SPLINE_CURVE ( 2, ( #13509, #19118, #22434, #3871, #13622, #20957, #11276, #11540, #4240, #18879, #16917 ),
 .UNSPECIFIED., .F., .T. ) 
 B_SPLINE_CURVE_WITH_KNOTS ( ( 3, 2, 2, 2, 2, 3 ),
 ( 0.4000000000000000222, 0.4199999999999999845, 0.4400000000000000022, 0.4599999999999999645, 0.4799999999999999267, 0.4999999999999999445 ),
 .UNSPECIFIED. ) 
 CURVE ( )  GEOMETRIC_REPRESENTATION_ITEM ( )  RATIONAL_B_SPLINE_CURVE ( ( 1.000000000000000000, 0.9510565162951535312, 1.000000000000000000, 0.9510565162951535312, 1.000000000000000000, 0.9510565162951535312, 1.000000000000000000, 0.9510565162951535312, 1.000000000000000000, 0.9510565162951536422, 0.9999999999999998890 ) ) 
 REPRESENTATION_ITEM ( '' )  );
#17834=CARTESIAN_POINT ( 'NONE',  ( -7.685661446562381371, 5.583959896777970222, 10.85958914175814449 ) ) ;
#17840=EDGE_LOOP ( 'NONE', ( #21612, #3468, #444, #5545 ) ) ;
#17850=VERTEX_POINT ( 'NONE', #14187 ) ;
#17855=CARTESIAN_POINT ( 'NONE',  ( 2.935661446562616295, -9.035036904803758873, -6.806742014460233747 ) ) ;
#17858=CARTESIAN_POINT ( 'NONE',  ( -3.213650742982549602, -8.577201891241250209, -12.34882418652165548 ) ) ;
#17872=ORIENTED_EDGE ( 'NONE', *, *, #17876, .F. ) ;
#17874=CARTESIAN_POINT ( 'NONE',  ( -5.871322893124554021, 8.081182679343978492, 6.759589141758143072 ) ) ;
#17876=EDGE_CURVE ( 'NONE', #8084, #19085, #22952, .T. ) ;
#17884=CARTESIAN_POINT ( 'NONE',  ( 0.000000000000000000, 0.000000000000000000, 2.500000000000000000 ) ) ;
#17888=CONICAL_SURFACE ( 'NONE', #17483, 9.500000000000000000, 0.7853981633974500554 ) ;
#17889=CARTESIAN_POINT ( 'NONE',  ( 5.871322893124551356, -8.081182679343980269, 7.759589141758143072 ) ) ;
#17898=CARTESIAN_POINT ( 'NONE',  ( -5.365059087798940141, -7.384370330707086261, -3.933165578109187877 ) ) ;
#17902=VERTEX_POINT ( 'NONE', #20540 ) ;
#17911=CARTESIAN_POINT ( 'NONE',  ( 7.685661446561619314, 5.583959896779020049, -8.259589141758144848 ) ) ;
#17928=CARTESIAN_POINT ( 'NONE',  ( -8.680847955711200825, 2.820578480813073607, -3.533165578109187965 ) ) ;
#17931=CARTESIAN_POINT ( 'NONE',  ( -6.153822176767817416E-13, 9.500000000000000000, 2.559589141758142450 ) ) ;
#17932=CARTESIAN_POINT ( 'NONE',  ( -6.822232771736903637E-13, 9.988891130263535700, 7.706742014460232326 ) ) ;
#17956=CARTESIAN_POINT ( 'NONE',  ( -9.500000000000000000, -6.482511860946779655E-13, -8.206742014460234103 ) ) ;
#17960=LINE ( 'NONE', #5388, #2217 ) ;
#17961=CARTESIAN_POINT ( 'NONE',  ( 9.500000000000000000, 1.163414459189985485E-15, 12.50000000000000000 ) ) ;
#17964=ORIENTED_EDGE ( 'NONE', *, *, #9085, .T. ) ;
#17967=CARTESIAN_POINT ( 'NONE',  ( -5.871322893124554021, 8.081182679343978492, -7.906742014460233392 ) ) ;
#17973=ADVANCED_FACE ( 'NONE', ( #9644 ), #3811, .F. ) ;
#17977=ADVANCED_FACE ( 'NONE', ( #13185 ), #394, .T. ) ;
#17986=CIRCLE ( 'NONE', #7430, 8.000000000000000000 ) ;
#17987=CARTESIAN_POINT ( 'NONE',  ( -7.685661446562381371, 5.583959896777970222, 2.859589141758144493 ) ) ;
#18000=CARTESIAN_POINT ( 'NONE',  ( -7.685661446562381371, 5.583959896777970222, 4.006742014460233925 ) ) ;
#18008=ORIENTED_EDGE ( 'NONE', *, *, #23393, .F. ) ;
#18021=CARTESIAN_POINT ( 'NONE',  ( -5.871322893124554021, 8.081182679343978492, -8.759589141758141295 ) ) ;
#18024=CARTESIAN_POINT ( 'NONE',  ( -6.153822176767817416E-13, 9.500000000000000000, 3.706742014460231882 ) ) ;
#18041=ORIENTED_EDGE ( 'NONE', *, *, #16556, .T. ) ;
#18045=ORIENTED_EDGE ( 'NONE', *, *, #17794, .F. ) ;
#18046=CARTESIAN_POINT ( 'NONE',  ( 6.809999908187194197E-13, -9.988891130263535700, 12.70674201446023410 ) ) ;
#18060=LINE ( 'NONE', #23561, #5320 ) ;
#18068=DIRECTION ( 'NONE',  ( 0.5000000000000001110, -0.8660254037844384856, 0.000000000000000000 ) ) ;
#18078=CARTESIAN_POINT ( 'NONE',  ( -9.500000000000000000, -6.482511860946779655E-13, -7.059589141758143782 ) ) ;
#18088=CARTESIAN_POINT ( 'NONE',  ( -2.935661446561384391, -9.035036904804158553, -3.459589141758144137 ) ) ;
#18095=AXIS2_PLACEMENT_3D ( 'NONE', #15238, #9281, #11590 ) ;
#18096=CARTESIAN_POINT ( 'NONE',  ( 9.500000000000000000, 6.470877716354879437E-13, -7.206742014460234103 ) ) ;
#18101=AXIS2_PLACEMENT_3D ( 'NONE', #10636, #6989, #12359 ) ;
#18102=VECTOR ( 'NONE', #19723, 1000.000000000000000 ) ;
#18106=CARTESIAN_POINT ( 'NONE',  ( 9.500000000000209610, -3.086737114211962396, -3.959589141758144581 ) ) ;
#18112=CARTESIAN_POINT ( 'NONE',  ( -7.685661446561619314, -5.583959896779019161, 3.259589141758143516 ) ) ;
#18113=( BOUNDED_CURVE ( )  B_SPLINE_CURVE ( 2, ( #4734, #15565, #12144, #17284, #17788, #13750, #1083, #4505, #15944 ),
 .UNSPECIFIED., .F., .T. ) 
 B_SPLINE_CURVE_WITH_KNOTS ( ( 3, 2, 2, 2, 3 ),
 ( 0.1207052568533188708, 0.1400000000000000133, 0.1600000000000000033, 0.1799999999999999933, 0.2000000000000000111 ),
 .UNSPECIFIED. ) 
 CURVE ( )  GEOMETRIC_REPRESENTATION_ITEM ( )  RATIONAL_B_SPLINE_CURVE ( ( 0.9966699465879109709, 0.9527824026605606900, 1.000000000000000000, 0.9510565162951535312, 1.000000000000000000, 0.9510565162951535312, 1.000000000000000000, 0.9510565162951535312, 1.000000000000000000 ) ) 
 REPRESENTATION_ITEM ( '' )  );
#18131=CARTESIAN_POINT ( 'NONE',  ( 9.000000000000001776, 6.130305204967781210E-13, 12.50000000000000000 ) ) ;
#18133=CARTESIAN_POINT ( 'NONE',  ( 5.871322893124551356, -8.081182679343980269, -8.906742014460233392 ) ) ;
#18140=CARTESIAN_POINT ( 'NONE',  ( -5.365059087799948223, 7.384370330706355290, -3.333165578109187344 ) ) ;
#18142=CARTESIAN_POINT ( 'NONE',  ( -2.682529543900285862, 8.255977015246234174, 9.233165578109188587 ) ) ;
#18143=EDGE_CURVE ( 'NONE', #11511, #16661, #21845, .T. ) ;
#18147=PLANE ( 'NONE',  #10875 ) ;
#18152=CARTESIAN_POINT ( 'NONE',  ( -2.935661446561384391, -9.035036904804158553, -7.459589141758144137 ) ) ;
#18156=LINE ( 'NONE', #10908, #23243 ) ;
#18161=DIRECTION ( 'NONE',  ( -1.000000000000000000, 0.000000000000000000, 0.000000000000000000 ) ) ;
#18170=CARTESIAN_POINT ( 'NONE',  ( 9.499999999999790390, 3.086737114213260025, -9.306742014460233747 ) ) ;
#18177=CARTESIAN_POINT ( 'NONE',  ( 6.809999908187194197E-13, -9.988891130263535700, 5.559589141758142894 ) ) ;
#18178=CARTESIAN_POINT ( 'NONE',  ( -2.935661446561384391, -9.035036904804158553, 8.606742014460234458 ) ) ;
#18186=CARTESIAN_POINT ( 'NONE',  ( -7.685661446561619314, -5.583959896779019161, 3.259589141758143516 ) ) ;
#18191=CARTESIAN_POINT ( 'NONE',  ( 12.50000000000000178, 5.755434930044642846E-15, -2.500000000000000000 ) ) ;
#18195=CYLINDRICAL_SURFACE ( 'NONE', #19139, 9.500000000000000000 ) ;
#18197=CARTESIAN_POINT ( 'NONE',  ( -3.342360423240396727, 8.897987090007918098, -3.499485096983522059 ) ) ;
#18202=CARTESIAN_POINT ( 'NONE',  ( -9.500000000000211386, 3.086737114211961064, -6.959589141758143249 ) ) ;
#18205=CARTESIAN_POINT ( 'NONE',  ( -8.680847955710813579, -2.820578480814257549, 5.733165578109188587 ) ) ;
#18216=CARTESIAN_POINT ( 'NONE',  ( 5.871322893124553133, -8.081182679343980269, -11.75958914175814485 ) ) ;
#18218=VERTEX_POINT ( 'NONE', #878 ) ;
#18224=CARTESIAN_POINT ( 'NONE',  ( 9.500000000000000000, 6.470877716354879437E-13, -4.059589141758143782 ) ) ;
#18227=CARTESIAN_POINT ( 'NONE',  ( -6.153822176767817416E-13, 9.500000000000000000, -3.500000000000014211 ) ) ;
#18255=CARTESIAN_POINT ( 'NONE',  ( 5.365059087798938364, 7.384370330707087149, 10.93316557810918788 ) ) ;
#18256=MANIFOLD_SOLID_BREP ( 'Mirror1', #9279 ) ;
#18263=CARTESIAN_POINT ( 'NONE',  ( 6.809999908187194197E-13, -9.988891130263535700, -3.559589141758143338 ) ) ;
#18288=CARTESIAN_POINT ( 'NONE',  ( 9.500000000000209610, -3.086737114211962396, 11.10674201446023446 ) ) ;
#18289=CARTESIAN_POINT ( 'NONE',  ( -5.871322893123450015, -8.081182679344781405, 8.506742014460233037 ) ) ;
#18304=CARTESIAN_POINT ( 'NONE',  ( -9.440377765553483513, 1.232704728397706839, -3.501569427774944732 ) ) ;
#18305=CARTESIAN_POINT ( 'NONE',  ( -7.685661446561619314, -5.583959896779019161, -11.25958914175814307 ) ) ;
#18308=CARTESIAN_POINT ( 'NONE',  ( -5.365059087798939252, -7.384370330707086261, -7.933165578109187877 ) ) ;
#18313=DIRECTION ( 'NONE',  ( 0.000000000000000000, -1.000000000000000000, 0.000000000000000000 ) ) ;
#18322=CARTESIAN_POINT ( 'NONE',  ( 0.000000000000000000, 0.000000000000000000, 3.499999999999999556 ) ) ;
#18324=CARTESIAN_POINT ( 'NONE',  ( 6.809999908187194197E-13, -9.988891130263535700, -9.559589141758145558 ) ) ;
#18349=EDGE_CURVE ( 'NONE', #13485, #1630, #17830, .T. ) ;
#18350=CYLINDRICAL_SURFACE ( 'NONE', #14573, 9.500000000000000000 ) ;
#18363=CARTESIAN_POINT ( 'NONE',  ( 8.680847955711007202, 5.912916378492122225E-13, 8.633165578109188942 ) ) ;
#18374=CARTESIAN_POINT ( 'NONE',  ( -5.871322893124554021, 8.081182679343978492, -6.759589141758143072 ) ) ;
#18378=CARTESIAN_POINT ( 'NONE',  ( 6.250000000000000000, -10.82531754730548279, 2.500000000000000000 ) ) ;
#18381=CARTESIAN_POINT ( 'NONE',  ( -8.000000000000000000, 9.797174393178825657E-16, -12.50000000000000000 ) ) ;
#18387=DIRECTION ( 'NONE',  ( 0.000000000000000000, 0.000000000000000000, 1.000000000000000000 ) ) ;
#18396=CARTESIAN_POINT ( 'NONE',  ( -9.500000000000000000, -6.482511860946779655E-13, 8.206742014460234103 ) ) ;
#18397=CARTESIAN_POINT ( 'NONE',  ( 5.871322893124553133, -8.081182679343980269, 4.906742014460232504 ) ) ;
#18422=CARTESIAN_POINT ( 'NONE',  ( -6.233975306307046963E-13, 9.127583699786111282, -9.133165578109188942 ) ) ;
#18443=CARTESIAN_POINT ( 'NONE',  ( 9.500000000000000000, 6.470877716354879437E-13, -6.059589141758143782 ) ) ;
#18451=CARTESIAN_POINT ( 'NONE',  ( 8.999999999999996447, 6.130305204967778181E-13, -12.50000000000000000 ) ) ;
#18462=CARTESIAN_POINT ( 'NONE',  ( -5.871322893124554021, 8.081182679343978492, -3.906742014460231616 ) ) ;
#18463=CARTESIAN_POINT ( 'NONE',  ( 6.222797240145152671E-13, -9.127583699786111282, 6.133165578109188942 ) ) ;
#18468=CIRCLE ( 'NONE', #18101, 1.000000000000000000 ) ;
#18470=PLANE ( 'NONE',  #4109 ) ;
#18491=CARTESIAN_POINT ( 'NONE',  ( 2.682529543900284974, -8.255977015246234174, 12.23316557810919036 ) ) ;
#18502=CARTESIAN_POINT ( 'NONE',  ( 2.682529543900284974, -8.255977015246234174, -8.233165578109190363 ) ) ;
#18524=CARTESIAN_POINT ( 'NONE',  ( 5.871322893124553133, -8.081182679343980269, -10.90674201446023339 ) ) ;
#18529=CARTESIAN_POINT ( 'NONE',  ( 7.685661446562381371, -5.583959896777971110, 7.006742014460233037 ) ) ;
#18531=ORIENTED_EDGE ( 'NONE', *, *, #6931, .F. ) ;
#18549=CARTESIAN_POINT ( 'NONE',  ( 9.330908268522616567, -1.784418920661929642, -11.99999999999998934 ) ) ;
#18553=CARTESIAN_POINT ( 'NONE',  ( 8.680847955711199049, -2.820578480813074496, -10.53316557810918752 ) ) ;
#18560=PLANE ( 'NONE',  #21224 ) ;
#18563=ADVANCED_FACE ( 'NONE', ( #1307 ), #21386, .F. ) ;
#18574=CARTESIAN_POINT ( 'NONE',  ( 2.935661446561383503, 9.035036904804158553, -8.459589141758144137 ) ) ;
#18579=EDGE_CURVE ( 'NONE', #10046, #5101, #8826, .T. ) ;
#18581=AXIS2_PLACEMENT_3D ( 'NONE', #7447, #4192, #18948 ) ;
#18590=CARTESIAN_POINT ( 'NONE',  ( 6.809999908187194197E-13, -9.988891130263535700, -8.706742014460230550 ) ) ;
#18593=CYLINDRICAL_SURFACE ( 'NONE', #18581, 9.500000000000000000 ) ;
#18594=CARTESIAN_POINT ( 'NONE',  ( -8.680847955710813579, -2.820578480814258437, 3.733165578109188587 ) ) ;
#18596=ORIENTED_EDGE ( 'NONE', *, *, #21726, .T. ) ;
#18603=( BOUNDED_CURVE ( )  B_SPLINE_CURVE ( 2, ( #20007, #14029, #3287, #1352, #18186, #21475, #6476, #1479, #2802, #13917, #21360, #8411, #15862 ),
 .UNSPECIFIED., .F., .T. ) 
 B_SPLINE_CURVE_WITH_KNOTS ( ( 3, 2, 2, 2, 2, 2, 3 ),
 ( 0.8558632199373861216, 0.8599999999999999867, 0.8800000000000000044, 0.9000000000000000222, 0.9200000000000000400, 0.9399999999999999467, 0.9500000000000000666 ),
 .UNSPECIFIED. ) 
 CURVE ( )  GEOMETRIC_REPRESENTATION_ITEM ( )  RATIONAL_B_SPLINE_CURVE ( ( 0.9839409940142059829, 0.9898765786207461836, 1.000000000000000000, 0.9510565162951535312, 1.000000000000000000, 0.9510565162951535312, 1.000000000000000000, 0.9510565162951535312, 1.000000000000000000, 0.9510565162951535312, 1.000000000000000000, 0.9755282581475764880, 0.9755282581475768211 ) ) 
 REPRESENTATION_ITEM ( '' )  );
#18614=VERTEX_POINT ( 'NONE', #10873 ) ;
#18616=CARTESIAN_POINT ( 'NONE',  ( -2.935661446562617183, 9.035036904803758873, 10.65958914175814343 ) ) ;
#18622=CARTESIAN_POINT ( 'NONE',  ( -5.871322893123450015, -8.081182679344781405, -3.359589141758143160 ) ) ;
#18645=CARTESIAN_POINT ( 'NONE',  ( -7.685661446561619314, -5.583959896779019161, 10.40674201446023339 ) ) ;
#18651=VERTEX_POINT ( 'NONE', #21244 ) ;
#18658=CARTESIAN_POINT ( 'NONE',  ( -5.871322893124554021, 8.081182679343978492, -10.75958914175814130 ) ) ;
#18679=CARTESIAN_POINT ( 'NONE',  ( 9.500000000000209610, -3.086737114211962396, -5.959589141758143249 ) ) ;
#18682=CARTESIAN_POINT ( 'NONE',  ( 5.871322893123448239, 8.081182679344781405, 11.50674201446023126 ) ) ;
#18693=VERTEX_POINT ( 'NONE', #4908 ) ;
#18700=EDGE_LOOP ( 'NONE', ( #7320, #15651, #3406, #862 ) ) ;
#18723=CARTESIAN_POINT ( 'NONE',  ( 6.222797240145152671E-13, -9.127583699786111282, 4.133165578109187166 ) ) ;
#18730=CARTESIAN_POINT ( 'NONE',  ( 8.680847955711199049, -2.820578480813074496, -12.53316557810918752 ) ) ;
#18731=( BOUNDED_CURVE ( )  B_SPLINE_CURVE ( 2, ( #11941, #8530, #17442, #13658, #8276, #6477, #19155, #21096, #11684, #21606, #17823 ),
 .UNSPECIFIED., .F., .T. ) 
 B_SPLINE_CURVE_WITH_KNOTS ( ( 3, 2, 2, 2, 2, 3 ),
 ( 0.5000000000000000000, 0.5200000000000000178, 0.5400000000000000355, 0.5600000000000001643, 0.5800000000000000711, 0.6000000000000000888 ),
 .UNSPECIFIED. ) 
 CURVE ( )  GEOMETRIC_REPRESENTATION_ITEM ( )  RATIONAL_B_SPLINE_CURVE ( ( 1.000000000000000000, 0.9510565162951535312, 1.000000000000000000, 0.9510565162951535312, 1.000000000000000000, 0.9510565162951535312, 1.000000000000000000, 0.9510565162951535312, 1.000000000000000000, 0.9510565162951533091, 1.000000000000000222 ) ) 
 REPRESENTATION_ITEM ( '' )  );
#18748=CARTESIAN_POINT ( 'NONE',  ( 9.500000000000000000, 6.470877716354879437E-13, -6.059589141758143782 ) ) ;
#18754=ORIENTED_EDGE ( 'NONE', *, *, #5308, .F. ) ;
#18761=EDGE_CURVE ( 'NONE', #3993, #22463, #14451, .T. ) ;
#18771=VERTEX_POINT ( 'NONE', #21735 ) ;
#18778=ORIENTED_EDGE ( 'NONE', *, *, #17652, .F. ) ;
#18783=AXIS2_PLACEMENT_3D ( 'NONE', #2576, #6110, #6482 ) ;
#18790=ADVANCED_FACE ( 'NONE', ( #9008 ), #18195, .T. ) ;
#18792=EDGE_CURVE ( 'NONE', #9278, #17662, #5481, .T. ) ;
#18794=CARTESIAN_POINT ( 'NONE',  ( -9.500000000000211386, 3.086737114211961064, -8.959589141758140585 ) ) ;
#18797=ORIENTED_EDGE ( 'NONE', *, *, #11117, .F. ) ;
#18803=LINE ( 'NONE', #22962, #10479 ) ;
#18834=CARTESIAN_POINT ( 'NONE',  ( -7.485396084480734125, -5.856027100821079578, -3.500200866489544538 ) ) ;
#18839=CARTESIAN_POINT ( 'NONE',  ( 9.500000000000000000, 6.470877716354879437E-13, 11.20674201446023410 ) ) ;
#18846=EDGE_LOOP ( 'NONE', ( #9018, #10635, #72 ) ) ;
#18847=CARTESIAN_POINT ( 'NONE',  ( -7.022953521755574080, 5.102474405759713783, 5.433165578109188765 ) ) ;
#18859=CARTESIAN_POINT ( 'NONE',  ( -7.022953521754877748, -5.102474405760673015, -11.83316557810918823 ) ) ;
#18879=CARTESIAN_POINT ( 'NONE',  ( -9.499999999999786837, -3.086737114213265354, 8.306742014460233747 ) ) ;
#18882=EDGE_CURVE ( 'NONE', #9290, #17358, #20255, .T. ) ;
#18886=( BOUNDED_CURVE ( )  B_SPLINE_CURVE ( 2, ( #18748, #15312, #2027, #19116, #7997, #5817, #2160, #13244, #2390, #15445, #9807 ),
 .UNSPECIFIED., .F., .T. ) 
 B_SPLINE_CURVE_WITH_KNOTS ( ( 3, 2, 2, 2, 2, 3 ),
 ( 0.6000000000000000888, 0.6200000000000001066, 0.6400000000000001243, 0.6600000000000001421, 0.6800000000000001599, 0.7000000000000000666 ),
 .UNSPECIFIED. ) 
 CURVE ( )  GEOMETRIC_REPRESENTATION_ITEM ( )  RATIONAL_B_SPLINE_CURVE ( ( 0.9999999999999997780, 0.9510565162951537532, 1.000000000000000000, 0.9510565162951535312, 1.000000000000000000, 0.9510565162951535312, 1.000000000000000000, 0.9510565162951535312, 1.000000000000000000, 0.9510565162951533091, 1.000000000000000222 ) ) 
 REPRESENTATION_ITEM ( '' )  );
#18912=VECTOR ( 'NONE', #20809, 1000.000000000000000 ) ;
#18927=CARTESIAN_POINT ( 'NONE',  ( 5.871322893124553133, -8.081182679343980269, -3.759589141758144404 ) ) ;
#18928=VERTEX_POINT ( 'NONE', #20492 ) ;
#18933=CARTESIAN_POINT ( 'NONE',  ( 5.871322893123448239, 8.081182679344781405, 5.506742014460233925 ) ) ;
#18937=ADVANCED_FACE ( 'NONE', ( #1935 ), #22559, .F. ) ;
#18945=CARTESIAN_POINT ( 'NONE',  ( 5.365059087799947335, -7.384370330706356178, 10.33316557810918823 ) ) ;
#18948=DIRECTION ( 'NONE',  ( -1.000000000000000000, 0.000000000000000000, 0.000000000000000000 ) ) ;
#18972=DIRECTION ( 'NONE',  ( 1.000000000000000000, 6.811450227741984732E-14, -0.000000000000000000 ) ) ;
#18980=ORIENTED_EDGE ( 'NONE', *, *, #7021, .T. ) ;
#18981=CARTESIAN_POINT ( 'NONE',  ( 2.682529543899157876, 8.255977015246598327, 7.033165578109189298 ) ) ;
#19010=CARTESIAN_POINT ( 'NONE',  ( 8.680847955711199049, -2.820578480813074496, 12.53316557810918752 ) ) ;
#19022=DIRECTION ( 'NONE',  ( -0.000000000000000000, -0.000000000000000000, -1.000000000000000000 ) ) ;
#19033=CARTESIAN_POINT ( 'NONE',  ( -7.685661446561619314, -5.583959896779019161, 4.406742014460233392 ) ) ;
#19051=VERTEX_POINT ( 'NONE', #23417 ) ;
#19053=ADVANCED_FACE ( 'NONE', ( #17427 ), #5528, .T. ) ;
#19056=CARTESIAN_POINT ( 'NONE',  ( -8.354078656939378789, -4.088315676896441708, 12.20717083813929271 ) ) ;
#19057=CARTESIAN_POINT ( 'NONE',  ( -9.378401895172215674, 3.550564238312661509E-15, 12.12159810482778077 ) ) ;
#19062=CARTESIAN_POINT ( 'NONE',  ( -7.685661446561619314, -5.583959896779019161, -4.406742014460233392 ) ) ;
#19063=ORIENTED_EDGE ( 'NONE', *, *, #17521, .T. ) ;
#19065=CARTESIAN_POINT ( 'NONE',  ( -8.680847955711007202, -5.923547351154968927E-13, 11.63316557810919072 ) ) ;
#19068=ORIENTED_EDGE ( 'NONE', *, *, #9904, .T. ) ;
#19073=CARTESIAN_POINT ( 'NONE',  ( 9.500000000000000000, 6.470877716354879437E-13, -11.20674201446023410 ) ) ;
#19079=CARTESIAN_POINT ( 'NONE',  ( -1.749335460928132413, -9.337549220493531976, -3.500000000000076383 ) ) ;
#19085=VERTEX_POINT ( 'NONE', #836 ) ;
#19091=CARTESIAN_POINT ( 'NONE',  ( -9.500000000000211386, 3.086737114211961064, 10.95958914175814414 ) ) ;
#19096=CARTESIAN_POINT ( 'NONE',  ( 0.000000000000000000, 0.000000000000000000, 11.99999999999999645 ) ) ;
#19101=CARTESIAN_POINT ( 'NONE',  ( 7.022953521755574080, -5.102474405759714671, -6.433165578109188765 ) ) ;
#19111=CARTESIAN_POINT ( 'NONE',  ( -9.499999999999799272, -3.086737114213243593, -6.306742014460231083 ) ) ;
#19116=CARTESIAN_POINT ( 'NONE',  ( 5.871322893124551356, -8.081182679343980269, -5.759589141758143960 ) ) ;
#19117=CARTESIAN_POINT ( 'NONE',  ( -7.022953521754877748, -5.102474405760673015, -9.833165578109188232 ) ) ;
#19118=CARTESIAN_POINT ( 'NONE',  ( 9.500000000000209610, -3.086737114211962396, 9.106742014460232681 ) ) ;
#19121=CARTESIAN_POINT ( 'NONE',  ( -2.682529543899159208, -8.255977015246598327, 10.03316557810918930 ) ) ;
#19129=CARTESIAN_POINT ( 'NONE',  ( 4.159489978096769569, -7.970633069177189611, 12.50000000000000000 ) ) ;
#19132=ORIENTED_EDGE ( 'NONE', *, *, #21971, .F. ) ;
#19139=AXIS2_PLACEMENT_3D ( 'NONE', #12678, #7189, #14634 ) ;
#19142=CARTESIAN_POINT ( 'NONE',  ( 7.022953521754877748, 5.102474405760673903, -6.833165578109188232 ) ) ;
#19146=CARTESIAN_POINT ( 'NONE',  ( -5.871322893124554021, 8.081182679343978492, 10.75958914175814130 ) ) ;
#19155=CARTESIAN_POINT ( 'NONE',  ( 2.935661446561383503, 9.035036904804158553, 6.459589141758144137 ) ) ;
#19174=VERTEX_POINT ( 'NONE', #19984 ) ;
#19177=CARTESIAN_POINT ( 'NONE',  ( -5.365059087798940141, -7.384370330707086261, 9.933165578109189653 ) ) ;
#19189=FACE_OUTER_BOUND ( 'NONE', #10699, .T. ) ;
#19211=CARTESIAN_POINT ( 'NONE',  ( 2.935661446561383503, 9.035036904804158553, 4.459589141758144137 ) ) ;
#19224=CARTESIAN_POINT ( 'NONE',  ( -7.022953521755574080, 5.102474405759713783, -5.433165578109188765 ) ) ;
#19245=CARTESIAN_POINT ( 'NONE',  ( -8.680847955711007202, -5.923547351154968927E-13, -5.633165578109188942 ) ) ;
#19251=CARTESIAN_POINT ( 'NONE',  ( 8.680847955711007202, 5.912916378492122225E-13, 10.63316557810918894 ) ) ;
#19256=CARTESIAN_POINT ( 'NONE',  ( -9.499999999999790390, -3.086737114213257804, -11.15958914175814520 ) ) ;
#19259=CARTESIAN_POINT ( 'NONE',  ( -5.871322893123449127, -8.081182679344781405, -10.50674201446023304 ) ) ;
#19261=CARTESIAN_POINT ( 'NONE',  ( -9.499999999999799272, -3.086737114213243593, 6.306742014460231083 ) ) ;
#19262=AXIS2_PLACEMENT_3D ( 'NONE', #8079, #10286, #15524 ) ;
#19275=CARTESIAN_POINT ( 'NONE',  ( -5.365059087799947335, 7.384370330706355290, -5.333165578109189120 ) ) ;
#19278=CARTESIAN_POINT ( 'NONE',  ( 9.500000000000000000, 6.470877716354879437E-13, 12.05958914175814378 ) ) ;
#19295=FACE_OUTER_BOUND ( 'NONE', #4955, .T. ) ;
#19308=CARTESIAN_POINT ( 'NONE',  ( 5.871322893123449127, 8.081182679344781405, -7.506742014460233037 ) ) ;
#19311=CARTESIAN_POINT ( 'NONE',  ( 2.682529543899157876, 8.255977015246598327, 7.033165578109189298 ) ) ;
#19324=CARTESIAN_POINT ( 'NONE',  ( -9.500000000000000000, -6.482511860946779655E-13, -12.20674201446023410 ) ) ;
#19349=CARTESIAN_POINT ( 'NONE',  ( 9.500000000000000000, 6.470877716354879437E-13, 6.059589141758143782 ) ) ;
#19355=CARTESIAN_POINT ( 'NONE',  ( 5.365059087798938364, 7.384370330707087149, -6.933165578109188765 ) ) ;
#19356=AXIS2_PLACEMENT_3D ( 'NONE', #18378, #23527, #16544 ) ;
#19360=EDGE_LOOP ( 'NONE', ( #12738, #16609, #16807 ) ) ;
#19374=CARTESIAN_POINT ( 'NONE',  ( 6.222797240145152671E-13, -9.127583699786111282, -8.133165578109188942 ) ) ;
#19382=ORIENTED_EDGE ( 'NONE', *, *, #9879, .F. ) ;
#19385=CARTESIAN_POINT ( 'NONE',  ( 6.809999908187194197E-13, -9.988891130263535700, -10.70674201446023410 ) ) ;
#19399=CARTESIAN_POINT ( 'NONE',  ( -5.871322893123450015, -8.081182679344781405, -12.50674201446023481 ) ) ;
#19402=CARTESIAN_POINT ( 'NONE',  ( -7.685661446561619314, -5.583959896779019161, 9.259589141758143072 ) ) ;
#19403=CARTESIAN_POINT ( 'NONE',  ( 7.685661446562381371, -5.583959896777971110, 13.00674201446023304 ) ) ;
#19405=CARTESIAN_POINT ( 'NONE',  ( -7.022953521754877748, -5.102474405760673015, -11.83316557810918823 ) ) ;
#19419=CARTESIAN_POINT ( 'NONE',  ( -8.818858540945930358, -3.028632380371159449, 12.18357898287954733 ) ) ;
#19421=CARTESIAN_POINT ( 'NONE',  ( -2.935661446561384391, -9.035036904804158553, 11.45958914175814414 ) ) ;
#19427=VERTEX_POINT ( 'NONE', #92 ) ;
#19428=CARTESIAN_POINT ( 'NONE',  ( -9.500000000000000000, -6.482511860946779655E-13, -8.206742014460234103 ) ) ;
#19431=CARTESIAN_POINT ( 'NONE',  ( 6.222797240145152671E-13, -9.127583699786111282, 10.13316557810918894 ) ) ;
#19437=EDGE_CURVE ( 'NONE', #11621, #9659, #3629, .T. ) ;
#19443=CARTESIAN_POINT ( 'NONE',  ( 3.934052222107162766, -8.094642247421043990, -12.50000000000000000 ) ) ;
#19450=FACE_OUTER_BOUND ( 'NONE', #9310, .T. ) ;
#19455=CARTESIAN_POINT ( 'NONE',  ( 9.500000000000000000, 6.470877716354879437E-13, 9.206742014460234103 ) ) ;
#19458=CARTESIAN_POINT ( 'NONE',  ( -7.685661446562381371, 5.583959896777970222, 6.859589141758143604 ) ) ;
#19467=CARTESIAN_POINT ( 'NONE',  ( 5.365059087798938364, 7.384370330707087149, -4.933165578109187877 ) ) ;
#19486=CARTESIAN_POINT ( 'NONE',  ( 2.682529543899157876, 8.255977015246598327, -9.033165578109187521 ) ) ;
#19490=CARTESIAN_POINT ( 'NONE',  ( -8.680847955711200825, 2.820578480813073607, 9.533165578109187521 ) ) ;
#19497=CARTESIAN_POINT ( 'NONE',  ( -5.871322893123450015, -8.081182679344781405, -11.35958914175814272 ) ) ;
#19498=EDGE_CURVE ( 'NONE', #5066, #9263, #10467, .T. ) ;
#19499=AXIS2_PLACEMENT_3D ( 'NONE', #14502, #20259, #1711 ) ;
#19512=CARTESIAN_POINT ( 'NONE',  ( 2.935661446561383503, 9.035036904804158553, -11.60674201446023268 ) ) ;
#19516=B_SPLINE_CURVE_WITH_KNOTS ( 'NONE', 3,
 ( #5674, #13097, #13211, #3717 ),
 .UNSPECIFIED., .F., .F.,
 ( 4, 4 ),
 ( 0.000000000000000000, 1.000000000000000000 ),
 .UNSPECIFIED. ) ;
#19517=CARTESIAN_POINT ( 'NONE',  ( -5.871322893123450015, -8.081182679344781405, 5.359589141758144493 ) ) ;
#19518=CARTESIAN_POINT ( 'NONE',  ( 9.500000000000000000, 6.470877716354879437E-13, 11.20674201446023410 ) ) ;
#19521=PLANE ( 'NONE',  #7220 ) ;
#19528=( BOUNDED_CURVE ( )  B_SPLINE_CURVE ( 2, ( #13007, #1915, #9333, #16778, #20587, #93, #17031, #21059, #2520, #7746, #4234 ),
 .UNSPECIFIED., .F., .F. ) 
 B_SPLINE_CURVE_WITH_KNOTS ( ( 3, 2, 2, 2, 2, 3 ),
 ( 0.3000000000000000999, 0.3200000000000001177, 0.3400000000000000799, 0.3600000000000000422, 0.3800000000000000044, 0.4000000000000000222 ),
 .UNSPECIFIED. ) 
 CURVE ( )  GEOMETRIC_REPRESENTATION_ITEM ( )  RATIONAL_B_SPLINE_CURVE ( ( 0.9999999999999997780, 0.9510565162951537532, 1.000000000000000000, 0.9510565162951535312, 1.000000000000000000, 0.9510565162951535312, 1.000000000000000000, 0.9510565162951535312, 1.000000000000000000, 0.9510565162951535312, 1.000000000000000000 ) ) 
 REPRESENTATION_ITEM ( '' )  );
#19534=PLANE ( 'NONE',  #20021 ) ;
#19537=CARTESIAN_POINT ( 'NONE',  ( 9.330908268522556170, -1.784418920662232289, 11.99999999999997691 ) ) ;
#19547=CARTESIAN_POINT ( 'NONE',  ( 2.682529543900284974, -8.255977015246234174, 4.233165578109187699 ) ) ;
#19551=AXIS2_PLACEMENT_3D ( 'NONE', #10484, #14275, #8158 ) ;
#19557=CARTESIAN_POINT ( 'NONE',  ( -7.685661446562381371, 5.583959896777970222, -12.00674201446023481 ) ) ;
#19581=CARTESIAN_POINT ( 'NONE',  ( 5.871322893123449127, 8.081182679344781405, 6.359589141758142716 ) ) ;
#19593=CARTESIAN_POINT ( 'NONE',  ( 9.500000000000000000, 6.470877716354879437E-13, -5.206742014460234103 ) ) ;
#19601=CARTESIAN_POINT ( 'NONE',  ( -7.685661446562381371, 5.583959896777970222, 6.006742014460233037 ) ) ;
#19609=CARTESIAN_POINT ( 'NONE',  ( -5.365059087798940141, -7.384370330707086261, -7.933165578109187877 ) ) ;
#19638=PLANE ( 'NONE',  #16155 ) ;
#19639=DIRECTION ( 'NONE',  ( -0.000000000000000000, -0.000000000000000000, 1.000000000000000000 ) ) ;
#19641=CARTESIAN_POINT ( 'NONE',  ( -9.500000000000000000, -6.482511860946779655E-13, 6.206742014460234103 ) ) ;
#19646=ADVANCED_FACE ( 'NONE', ( #20198 ), #10779, .F. ) ;
#19647=ORIENTED_EDGE ( 'NONE', *, *, #22025, .T. ) ;
#19652=CARTESIAN_POINT ( 'NONE',  ( -9.500000000000211386, 3.086737114211961064, 2.959589141758143249 ) ) ;
#19656=CARTESIAN_POINT ( 'NONE',  ( 12.50000000000000178, 5.755434930044642846E-15, -2.500000000000000000 ) ) ;
#19679=CARTESIAN_POINT ( 'NONE',  ( -7.685661446562381371, 5.583959896777970222, 8.859589141758144493 ) ) ;
#19686=( BOUNDED_SURFACE ( )  B_SPLINE_SURFACE ( 1, 2, ( 
 ( #19278, #9975, #733, #17314, #6214, #23052, #15348, #21226, #9851, #20984, #4530, #5974, #13653, #19146, #10094, #11936, #4273, #22567, #21090, #11438, #4390, #22820, #7899, #7776, #15213, #13539, #11676, #5852, #19402, #2562, #846, #15105, #22683, #13408, #13277, #20734, #20871, #17179, #2425, #4021, #4160, #9619, #11570, #12527, #23184, #21719, #21354, #6703, #6467, #1103, #4644, #14135, #19999, #21826, #12045, #14369, #3278, #8525, #8405, #2925, #5006, #3157, #15719, #5107, #10705, #18177, #3049, #19517, #10352, #8630, #17815, #2796, #6947, #15854, #15967, #12171, #10217, #23545, #23428, #21597, #6592, #8267, #4892, #13912, #17678, #979, #19774, #12304, #12420, #23315, #14023, #19652, #1219, #10581, #21469, #10470, #17931 ),
 ( #16083, #6827, #14257, #19880, #4762, #18046, #1344, #8768, #16216, #23676, #6898, #14611, #1922, #20474, #23895, #3763, #11050, #11171, #21948, #12659, #22309, #18288, #5587, #5354, #13017, #1572, #1471, #14837, #18645, #8884, #10924, #14477, #16321, #23776, #7399, #12779, #7048, #9239, #22196, #20239, #16686, #5232, #20127, #16431, #3403, #10819, #3516, #8986, #7174, #22081, #18396, #1691, #12893, #9115, #16563, #24018, #7293, #14733, #5469, #20349, #1817, #3633, #18529, #8842, #6550, #12124, #6781, #3114, #8484, #3012, #16280, #4847, #19601, #6663, #13986, #3233, #1065, #2877, #15929, #10430, #10778, #23390, #14210, #21898, #8590, #14094, #5072, #10662, #21549, #12380, #21674, #10538, #18000, #5183, #3359, #23744, #21430 ) ),
 .UNSPECIFIED., .F., .F., .F. ) 
 B_SPLINE_SURFACE_WITH_KNOTS ( ( 2, 2 ),
 ( 3, 2, 2, 2, 2, 2, 2, 2, 2, 2, 2, 2, 2, 2, 2, 2, 2, 2, 2, 2, 2, 2, 2, 2, 2, 2, 2, 2, 2, 2, 2, 2, 2, 2, 2, 2, 2, 2, 2, 2, 2, 2, 2, 2, 2, 2, 2, 2, 3 ),
 ( 0.000000000000000000, 1.000000000000000000 ),
 ( 0.000000000000000000, 0.02000000000000000042, 0.04000000000000000083, 0.05999999999999999778, 0.08000000000000000167, 0.1000000000000000056, 0.1199999999999999956, 0.1400000000000000133, 0.1600000000000000033, 0.1799999999999999933, 0.2000000000000000111, 0.2200000000000000011, 0.2399999999999999911, 0.2600000000000000089, 0.2800000000000000266, 0.2999999999999999889, 0.3200000000000000067, 0.3400000000000000244, 0.3599999999999999867, 0.3800000000000000044, 0.4000000000000000222, 0.4199999999999999845, 0.4400000000000000022, 0.4600000000000000200, 0.4799999999999999822, 0.5000000000000000000, 0.5200000000000000178, 0.5400000000000000355, 0.5600000000000000533, 0.5799999999999999600, 0.5999999999999999778, 0.6199999999999999956, 0.6400000000000000133, 0.6600000000000000311, 0.6800000000000000488, 0.6999999999999999556, 0.7199999999999999734, 0.7399999999999999911, 0.7600000000000000089, 0.7800000000000000266, 0.8000000000000000444, 0.8199999999999999512, 0.8399999999999999689, 0.8599999999999999867, 0.8800000000000000044, 0.9000000000000000222, 0.9200000000000000400, 0.9399999999999999467, 0.9500000000000000666 ),
 .UNSPECIFIED. ) 
 GEOMETRIC_REPRESENTATION_ITEM ( )  RATIONAL_B_SPLINE_SURFACE ( (
 ( 1.000000000000000000, 0.9510565162951535312, 1.000000000000000000, 0.9510565162951535312, 1.000000000000000000, 0.9510565162951535312, 1.000000000000000000, 0.9510565162951535312, 1.000000000000000000, 0.9510565162951535312, 1.000000000000000000, 0.9510565162951535312, 1.000000000000000000, 0.9510565162951535312, 1.000000000000000000, 0.9510565162951535312, 1.000000000000000000, 0.9510565162951535312, 1.000000000000000000, 0.9510565162951535312, 1.000000000000000000, 0.9510565162951535312, 1.000000000000000000, 0.9510565162951535312, 1.000000000000000000, 0.9510565162951535312, 1.000000000000000000, 0.9510565162951535312, 1.000000000000000000, 0.9510565162951535312, 1.000000000000000000, 0.9510565162951535312, 1.000000000000000000, 0.9510565162951535312, 1.000000000000000000, 0.9510565162951535312, 1.000000000000000000, 0.9510565162951535312, 1.000000000000000000, 0.9510565162951535312, 1.000000000000000000, 0.9510565162951535312, 1.000000000000000000, 0.9510565162951535312, 1.000000000000000000, 0.9510565162951535312, 1.000000000000000000, 0.9510565162951535312, 1.000000000000000000, 0.9510565162951535312, 1.000000000000000000, 0.9510565162951535312, 1.000000000000000000, 0.9510565162951535312, 1.000000000000000000, 0.9510565162951535312, 1.000000000000000000, 0.9510565162951535312, 1.000000000000000000, 0.9510565162951535312, 1.000000000000000000, 0.9510565162951535312, 1.000000000000000000, 0.9510565162951535312, 1.000000000000000000, 0.9510565162951535312, 1.000000000000000000, 0.9510565162951535312, 1.000000000000000000, 0.9510565162951535312, 1.000000000000000000, 0.9510565162951535312, 1.000000000000000000, 0.9510565162951535312, 1.000000000000000000, 0.9510565162951535312, 1.000000000000000000, 0.9510565162951535312, 1.000000000000000000, 0.9510565162951535312, 1.000000000000000000, 0.9510565162951535312, 1.000000000000000000, 0.9510565162951535312, 1.000000000000000000, 0.9510565162951535312, 1.000000000000000000, 0.9510565162951535312, 1.000000000000000000, 0.9510565162951535312, 1.000000000000000000, 0.9510565162951535312, 1.000000000000000000, 0.9510565162951535312, 1.000000000000000000, 0.9755282581475764880, 0.9755282581475768211),
 ( 1.000000000000000000, 0.9510565162951535312, 1.000000000000000000, 0.9510565162951535312, 1.000000000000000000, 0.9510565162951535312, 1.000000000000000000, 0.9510565162951535312, 1.000000000000000000, 0.9510565162951535312, 1.000000000000000000, 0.9510565162951535312, 1.000000000000000000, 0.9510565162951535312, 1.000000000000000000, 0.9510565162951535312, 1.000000000000000000, 0.9510565162951535312, 1.000000000000000000, 0.9510565162951535312, 1.000000000000000000, 0.9510565162951535312, 1.000000000000000000, 0.9510565162951535312, 1.000000000000000000, 0.9510565162951535312, 1.000000000000000000, 0.9510565162951535312, 1.000000000000000000, 0.9510565162951535312, 1.000000000000000000, 0.9510565162951535312, 1.000000000000000000, 0.9510565162951535312, 1.000000000000000000, 0.9510565162951535312, 1.000000000000000000, 0.9510565162951535312, 1.000000000000000000, 0.9510565162951535312, 1.000000000000000000, 0.9510565162951535312, 1.000000000000000000, 0.9510565162951535312, 1.000000000000000000, 0.9510565162951535312, 1.000000000000000000, 0.9510565162951535312, 1.000000000000000000, 0.9510565162951535312, 1.000000000000000000, 0.9510565162951535312, 1.000000000000000000, 0.9510565162951535312, 1.000000000000000000, 0.9510565162951535312, 1.000000000000000000, 0.9510565162951535312, 1.000000000000000000, 0.9510565162951535312, 1.000000000000000000, 0.9510565162951535312, 1.000000000000000000, 0.9510565162951535312, 1.000000000000000000, 0.9510565162951535312, 1.000000000000000000, 0.9510565162951535312, 1.000000000000000000, 0.9510565162951535312, 1.000000000000000000, 0.9510565162951535312, 1.000000000000000000, 0.9510565162951535312, 1.000000000000000000, 0.9510565162951535312, 1.000000000000000000, 0.9510565162951535312, 1.000000000000000000, 0.9510565162951535312, 1.000000000000000000, 0.9510565162951535312, 1.000000000000000000, 0.9510565162951535312, 1.000000000000000000, 0.9510565162951535312, 1.000000000000000000, 0.9510565162951535312, 1.000000000000000000, 0.9510565162951535312, 1.000000000000000000, 0.9510565162951535312, 1.000000000000000000, 0.9510565162951535312, 1.000000000000000000, 0.9755282581475764880, 0.9755282581475768211) ) ) 
 REPRESENTATION_ITEM ( '' )  SURFACE ( )  );
#19702=ORIENTED_EDGE ( 'NONE', *, *, #7649, .F. ) ;
#19703=LINE ( 'NONE', #4578, #2031 ) ;
#19711=CYLINDRICAL_SURFACE ( 'NONE', #5683, 9.500000000000000000 ) ;
#19713=CARTESIAN_POINT ( 'NONE',  ( -5.871322893124554021, 8.081182679343978492, 8.759589141758141295 ) ) ;
#19717=ORIENTED_EDGE ( 'NONE', *, *, #10149, .T. ) ;
#19720=DIRECTION ( 'NONE',  ( 0.000000000000000000, 0.000000000000000000, 1.000000000000000000 ) ) ;
#19723=DIRECTION ( 'NONE',  ( -0.000000000000000000, -0.000000000000000000, -1.000000000000000000 ) ) ;
#19733=CARTESIAN_POINT ( 'NONE',  ( 0.000000000000000000, 0.000000000000000000, -12.50000000000000000 ) ) ;
#19743=CARTESIAN_POINT ( 'NONE',  ( -8.680847955711007202, -5.923547351154968927E-13, 5.633165578109188942 ) ) ;
#19753=CARTESIAN_POINT ( 'NONE',  ( -5.871322893123450015, -8.081182679344781405, -5.359589141758144493 ) ) ;
#19770=EDGE_LOOP ( 'NONE', ( #330, #360, #10338, #19063 ) ) ;
#19771=CARTESIAN_POINT ( 'NONE',  ( 5.365059087798938364, 7.384370330707087149, -4.933165578109187877 ) ) ;
#19774=CARTESIAN_POINT ( 'NONE',  ( -2.935661446561384391, -9.035036904804158553, 3.459589141758144137 ) ) ;
#19775=CARTESIAN_POINT ( 'NONE',  ( 2.935661446561383503, 9.035036904804158553, 9.606742014460232681 ) ) ;
#19803=CARTESIAN_POINT ( 'NONE',  ( -2.682529543899159208, -8.255977015246598327, 4.033165578109189298 ) ) ;
#19814=CARTESIAN_POINT ( 'NONE',  ( 6.809999908187194197E-13, -9.988891130263535700, -6.706742014460232326 ) ) ;
#19830=CARTESIAN_POINT ( 'NONE',  ( -5.871322893123450015, -8.081182679344781405, 3.359589141758143160 ) ) ;
#19835=B_SPLINE_CURVE_WITH_KNOTS ( 'NONE', 3,
 ( #14589, #1319, #22061, #5449 ),
 .UNSPECIFIED., .F., .F.,
 ( 4, 4 ),
 ( 0.000000000000000000, 1.000000000000000000 ),
 .UNSPECIFIED. ) ;
#19844=CARTESIAN_POINT ( 'NONE',  ( -9.499999999999790390, -3.086737114213257804, 7.159589141758144315 ) ) ;
#19862=CARTESIAN_POINT ( 'NONE',  ( 5.871322893124553133, -8.081182679343980269, -3.759589141758144404 ) ) ;
#19876=CARTESIAN_POINT ( 'NONE',  ( 6.809999908187194197E-13, -9.988891130263535700, -10.70674201446023233 ) ) ;
#19880=CARTESIAN_POINT ( 'NONE',  ( 5.871322893124553133, -8.081182679343980269, 12.90674201446023517 ) ) ;
#19882=CARTESIAN_POINT ( 'NONE',  ( -9.499999999999790390, -3.086737114213257804, 6.306742014460231971 ) ) ;
#19891=DIRECTION ( 'NONE',  ( -1.000000000000000000, 0.000000000000000000, 0.000000000000000000 ) ) ;
#19900=MECHANICAL_DESIGN_GEOMETRIC_PRESENTATION_REPRESENTATION('',(#14055),#20670);
#19919=CARTESIAN_POINT ( 'NONE',  ( -9.499999999999790390, -3.086737114213257804, -4.306742014460233747 ) ) ;
#19938=VERTEX_POINT ( 'NONE', #15746 ) ;
#19952=B_SPLINE_CURVE_WITH_KNOTS ( 'NONE', 3,
 ( #13034, #5125, #10838, #7312 ),
 .UNSPECIFIED., .F., .F.,
 ( 4, 4 ),
 ( 0.000000000000000000, 1.000000000000000000 ),
 .UNSPECIFIED. ) ;
#19961=CARTESIAN_POINT ( 'NONE',  ( -7.022953521754877748, -5.102474405760673015, 11.83316557810918823 ) ) ;
#19962=EDGE_LOOP ( 'NONE', ( #21141, #14157, #9476, #12047, #9563, #9065, #12125, #1512, #7024, #21524, #3990, #21482, #15893, #13120, #2763 ) ) ;
#19970=FACE_BOUND ( 'NONE', #4880, .T. ) ;
#19974=CARTESIAN_POINT ( 'NONE',  ( -2.935661446561384391, -9.035036904804158553, -9.459589141758144137 ) ) ;
#19979=CARTESIAN_POINT ( 'NONE',  ( 0.000000000000000000, 0.000000000000000000, 12.50000000000000000 ) ) ;
#19980=DIRECTION ( 'NONE',  ( 1.000000000000000000, 0.000000000000000000, 0.000000000000000000 ) ) ;
#19981=CONICAL_SURFACE ( 'NONE', #4809, 9.500000000000000000, 0.7853981633974500554 ) ;
#19984=CARTESIAN_POINT ( 'NONE',  ( -9.500000000000000000, -6.482511860946779655E-13, -11.05958914175814556 ) ) ;
#19995=AXIS2_PLACEMENT_3D ( 'NONE', #13600, #20574, #15798 ) ;
#19997=ORIENTED_EDGE ( 'NONE', *, *, #7778, .T. ) ;
#19999=CARTESIAN_POINT ( 'NONE',  ( -7.685661446562381371, 5.583959896777970222, 6.859589141758143604 ) ) ;
#20000=CARTESIAN_POINT ( 'NONE',  ( 6.809999908187194197E-13, -9.988891130263535700, 4.706742014460233214 ) ) ;
#20001=EDGE_LOOP ( 'NONE', ( #15401, #22053, #8245 ) ) ;
#20007=CARTESIAN_POINT ( 'NONE',  ( -1.749335460929532182, -9.337549220493269075, 3.500000000000028866 ) ) ;
#20020=CARTESIAN_POINT ( 'NONE',  ( -9.499999999999783284, -3.086737114213268018, -11.15958914175814698 ) ) ;
#20021=AXIS2_PLACEMENT_3D ( 'NONE', #2584, #23070, #8290 ) ;
#20023=CARTESIAN_POINT ( 'NONE',  ( 5.365059087799946447, -7.384370330706356178, -8.333165578109190008 ) ) ;
#20032=CARTESIAN_POINT ( 'NONE',  ( -8.680847955711007202, -5.923547351154968927E-13, 3.633165578109188054 ) ) ;
#20038=CARTESIAN_POINT ( 'NONE',  ( -9.499999999999790390, -3.086737114213257804, -3.159589141758143871 ) ) ;
#20044=CARTESIAN_POINT ( 'NONE',  ( 9.500000000000000000, 6.470877716354879437E-13, -12.05958914175814378 ) ) ;
#20061=CARTESIAN_POINT ( 'NONE',  ( 2.935661446562616295, -9.035036904803758873, 3.659589141758142983 ) ) ;
#20064=VECTOR ( 'NONE', #23399, 1000.000000000000000 ) ;
#20070=EDGE_CURVE ( 'NONE', #21243, #10046, #8952, .T. ) ;
#20087=LINE ( 'NONE', #21902, #7158 ) ;
#20092=ORIENTED_EDGE ( 'NONE', *, *, #4485, .F. ) ;
#20093=ADVANCED_BREP_SHAPE_REPRESENTATION ( '', ( #18256, #8005 ), #10756 ) ;
#20102=CARTESIAN_POINT ( 'NONE',  ( -9.388305250079428177, 0.5130848116249094870, -12.11169474992057005 ) ) ;
#20103=CARTESIAN_POINT ( 'NONE',  ( 7.685661446562381371, -5.583959896777971110, -3.859589141758143604 ) ) ;
#20111=CARTESIAN_POINT ( 'NONE',  ( -9.500000000000000000, -6.482511860946779655E-13, 7.059589141758143782 ) ) ;
#20127=CARTESIAN_POINT ( 'NONE',  ( 7.685661446562381371, -5.583959896777971110, 9.006742014460233037 ) ) ;
#20128=CARTESIAN_POINT ( 'NONE',  ( -6.822232771736903637E-13, 9.988891130263535700, 9.706742014460232326 ) ) ;
#20138=DIRECTION ( 'NONE',  ( 0.5000000000000001110, -0.8660254037844384856, 0.000000000000000000 ) ) ;
#20141=EDGE_CURVE ( 'NONE', #9278, #12486, #22331, .T. ) ;
#20143=CARTESIAN_POINT ( 'NONE',  ( -2.935661446562617183, 9.035036904803758873, -10.65958914175814343 ) ) ;
#20148=CARTESIAN_POINT ( 'NONE',  ( -9.500000000000220268, 3.086737114211950406, 10.95958914175814236 ) ) ;
#20150=CARTESIAN_POINT ( 'NONE',  ( -2.935661446561384391, -9.035036904804158553, -11.45958914175814414 ) ) ;
#20161=CARTESIAN_POINT ( 'NONE',  ( 7.937578510445243651, -3.514536757623948127, -12.49999999999998046 ) ) ;
#20169=CARTESIAN_POINT ( 'NONE',  ( -6.822232771736903637E-13, 9.988891130263535700, -5.706742014460234103 ) ) ;
#20179=CARTESIAN_POINT ( 'NONE',  ( 2.935661446561383503, 9.035036904804158553, -9.606742014460232681 ) ) ;
#20181=CARTESIAN_POINT ( 'NONE',  ( 0.000000000000000000, 0.000000000000000000, 12.50000000000000000 ) ) ;
#20192=ORIENTED_EDGE ( 'NONE', *, *, #11612, .F. ) ;
#20198=FACE_OUTER_BOUND ( 'NONE', #19770, .T. ) ;
#20210=CARTESIAN_POINT ( 'NONE',  ( 7.022953521755574080, -5.102474405759714671, 8.433165578109187877 ) ) ;
#20211=ORIENTED_EDGE ( 'NONE', *, *, #11342, .F. ) ;
#20212=EDGE_CURVE ( 'NONE', #20510, #12845, #5485, .T. ) ;
#20220=CARTESIAN_POINT ( 'NONE',  ( -7.685661446562381371, 5.583959896777970222, -8.859589141758144493 ) ) ;
#20234=CARTESIAN_POINT ( 'NONE',  ( 2.935661446562616295, -9.035036904803758873, -10.80674201446023197 ) ) ;
#20239=CARTESIAN_POINT ( 'NONE',  ( 9.499999999999790390, 3.086737114213260025, 9.306742014460233747 ) ) ;
#20240=CARTESIAN_POINT ( 'NONE',  ( 2.935661446561383503, 9.035036904804158553, 5.606742014460233570 ) ) ;
#20247=CARTESIAN_POINT ( 'NONE',  ( -9.499999999999790390, -3.086737114213257804, -4.306742014460233747 ) ) ;
#20255=LINE ( 'NONE', #23793, #1988 ) ;
#20259=DIRECTION ( 'NONE',  ( -0.000000000000000000, -0.000000000000000000, -1.000000000000000000 ) ) ;
#20271=CARTESIAN_POINT ( 'NONE',  ( -2.352265130537804616, -9.224593858589891227, -3.479461880036829768 ) ) ;
#20274=CARTESIAN_POINT ( 'NONE',  ( -7.685661446561619314, -5.583959896779019161, -5.259589141758143960 ) ) ;
#20291=CARTESIAN_POINT ( 'NONE',  ( 2.682529543900284974, -8.255977015246234174, 6.233165578109188587 ) ) ;
#20304=( BOUNDED_CURVE ( )  B_SPLINE_CURVE ( 2, ( #11180, #9475, #21961, #18658, #20143, #12903, #7187, #22207, #12794, #3650, #16932 ),
 .UNSPECIFIED., .F., .F. ) 
 B_SPLINE_CURVE_WITH_KNOTS ( ( 3, 2, 2, 2, 2, 3 ),
 ( 0.09999999999999992228, 0.1199999999999999262, 0.1399999999999999578, 0.1599999999999999756, 0.1799999999999999656, 0.2000000000000000111 ),
 .UNSPECIFIED. ) 
 CURVE ( )  GEOMETRIC_REPRESENTATION_ITEM ( )  RATIONAL_B_SPLINE_CURVE ( ( 1.000000000000000222, 0.9510565162951533091, 1.000000000000000000, 0.9510565162951535312, 1.000000000000000000, 0.9510565162951535312, 1.000000000000000000, 0.9510565162951535312, 1.000000000000000000, 0.9510565162951535312, 1.000000000000000000 ) ) 
 REPRESENTATION_ITEM ( '' )  );
#20313=CARTESIAN_POINT ( 'NONE',  ( -6.249999999999999112, -10.82531754730548279, 2.500000000000000000 ) ) ;
#20317=CARTESIAN_POINT ( 'NONE',  ( -8.680847955710813579, -2.820578480814258437, 7.733165578109187699 ) ) ;
#20325=CARTESIAN_POINT ( 'NONE',  ( 5.365059087798938364, 7.384370330707087149, -8.933165578109186100 ) ) ;
#20345=CARTESIAN_POINT ( 'NONE',  ( -9.500000000000000000, -6.482511860946779655E-13, -10.20674201446023233 ) ) ;
#20349=CARTESIAN_POINT ( 'NONE',  ( 9.499999999999790390, 3.086737114213260025, 7.306742014460234635 ) ) ;
#20350=CARTESIAN_POINT ( 'NONE',  ( -5.871322893124554021, 8.081182679343978492, 3.906742014460231616 ) ) ;
#20375=AXIS2_PLACEMENT_3D ( 'NONE', #16901, #214, #7626 ) ;
#20386=CARTESIAN_POINT ( 'NONE',  ( -7.685661446561619314, -5.583959896779019161, -9.259589141758143072 ) ) ;
#20401=DIRECTION ( 'NONE',  ( -0.000000000000000000, -0.000000000000000000, -1.000000000000000000 ) ) ;
#20406=CARTESIAN_POINT ( 'NONE',  ( -8.680847955710813579, -2.820578480814258437, 5.733165578109188587 ) ) ;
#20428=VECTOR ( 'NONE', #3534, 1000.000000000000000 ) ;
#20436=CARTESIAN_POINT ( 'NONE',  ( -2.682529543900285862, 8.255977015246234174, 11.23316557810918859 ) ) ;
#20437=EDGE_LOOP ( 'NONE', ( #4100, #11993, #12891, #1735, #16215, #6717, #15463, #20938, #17119, #19068, #10583, #11386, #18008, #19702 ) ) ;
#20446=CARTESIAN_POINT ( 'NONE',  ( -1.504652183083727168, 9.499999999999904077, -2.610843423304989308 ) ) ;
#20447=( BOUNDED_CURVE ( )  B_SPLINE_CURVE ( 2, ( #9147, #23928, #133, #14990, #16595, #3543, #9488, #24044, #16949, #7665, #21979 ),
 .UNSPECIFIED., .F., .T. ) 
 B_SPLINE_CURVE_WITH_KNOTS ( ( 3, 2, 2, 2, 2, 3 ),
 ( 0.2000000000000000111, 0.2200000000000000289, 0.2400000000000000466, 0.2600000000000000644, 0.2800000000000001377, 0.3000000000000000999 ),
 .UNSPECIFIED. ) 
 CURVE ( )  GEOMETRIC_REPRESENTATION_ITEM ( )  RATIONAL_B_SPLINE_CURVE ( ( 1.000000000000000000, 0.9510565162951535312, 1.000000000000000000, 0.9510565162951535312, 1.000000000000000000, 0.9510565162951535312, 1.000000000000000000, 0.9510565162951535312, 1.000000000000000000, 0.9510565162951533091, 1.000000000000000222 ) ) 
 REPRESENTATION_ITEM ( '' )  );
#20474=CARTESIAN_POINT ( 'NONE',  ( -5.871322893124554021, 8.081182679343978492, 11.90674201446023339 ) ) ;
#20491=AXIS2_PLACEMENT_3D ( 'NONE', #2660, #17291, #10078 ) ;
#20492=CARTESIAN_POINT ( 'NONE',  ( 9.500000000000000000, 6.470877716354879437E-13, 6.059589141758143782 ) ) ;
#20501=CARTESIAN_POINT ( 'NONE',  ( -7.022953521755574080, 5.102474405759713783, -9.433165578109189653 ) ) ;
#20510=VERTEX_POINT ( 'NONE', #15962 ) ;
#20525=CARTESIAN_POINT ( 'NONE',  ( -7.685661446562381371, 5.583959896777970222, -8.859589141758144493 ) ) ;
#20526=ORIENTED_EDGE ( 'NONE', *, *, #11828, .T. ) ;
#20530=CARTESIAN_POINT ( 'NONE',  ( -5.871322893124554021, 8.081182679343978492, 5.906742014460232504 ) ) ;
#20536=CARTESIAN_POINT ( 'NONE',  ( -2.682529543899159208, -8.255977015246598327, -8.033165578109189298 ) ) ;
#20540=CARTESIAN_POINT ( 'NONE',  ( 8.871028110654306076, 6.042456644462176420E-13, 12.50000000000000000 ) ) ;
#20568=CARTESIAN_POINT ( 'NONE',  ( -8.680847955711007202, -5.923547351154968927E-13, 5.633165578109188942 ) ) ;
#20574=DIRECTION ( 'NONE',  ( 6.811450227741984732E-14, -1.000000000000000000, 0.000000000000000000 ) ) ;
#20575=CARTESIAN_POINT ( 'NONE',  ( 2.682529543899157876, 8.255977015246598327, -9.033165578109187521 ) ) ;
#20587=CARTESIAN_POINT ( 'NONE',  ( -2.935661446562617183, 9.035036904803758873, -8.659589141758143427 ) ) ;
#20599=ORIENTED_EDGE ( 'NONE', *, *, #9085, .F. ) ;
#20619=DIRECTION ( 'NONE',  ( 0.000000000000000000, -0.000000000000000000, -1.000000000000000000 ) ) ;
#20627=CARTESIAN_POINT ( 'NONE',  ( -2.935661446561384391, -9.035036904804158553, -7.459589141758144137 ) ) ;
#20670=( GEOMETRIC_REPRESENTATION_CONTEXT ( 3 ) GLOBAL_UNCERTAINTY_ASSIGNED_CONTEXT ( ( #2538 ) ) GLOBAL_UNIT_ASSIGNED_CONTEXT ( ( #11166, #14474, #8833 ) ) REPRESENTATION_CONTEXT ( 'NONE', 'WORKASPACE' ) );
#20672=DIRECTION ( 'NONE',  ( 1.000000000000000000, 0.000000000000000000, 0.000000000000000000 ) ) ;
#20676=CARTESIAN_POINT ( 'NONE',  ( 5.365059087798938364, 7.384370330707087149, 6.933165578109188765 ) ) ;
#20682=CARTESIAN_POINT ( 'NONE',  ( -7.022953521755574080, 5.102474405759713783, -7.433165578109188765 ) ) ;
#20695=ADVANCED_FACE ( 'NONE', ( #23303 ), #19638, .F. ) ;
#20703=VERTEX_POINT ( 'NONE', #4878 ) ;
#20706=VECTOR ( 'NONE', #6911, 1000.000000000000000 ) ;
#20713=CARTESIAN_POINT ( 'NONE',  ( -7.685661446561619314, -5.583959896779019161, -10.40674201446023339 ) ) ;
#20716=CARTESIAN_POINT ( 'NONE',  ( -6.822232771736904647E-13, 9.988891130263535700, -5.706742014460233214 ) ) ;
#20718=DIRECTION ( 'NONE',  ( -1.000000000000000000, 0.000000000000000000, 0.000000000000000000 ) ) ;
#20727=B_SPLINE_CURVE_WITH_KNOTS ( 'NONE', 3,
 ( #13633, #15461, #718, #2777, #6687, #21578, #2906, #13894 ),
 .UNSPECIFIED., .F., .F.,
 ( 4, 2, 2, 4 ),
 ( 0.000000000000000000, 0.001825626494867649361, 0.002738439742301474258, 0.003651252989735298722 ),
 .UNSPECIFIED. ) ;
#20729=ORIENTED_EDGE ( 'NONE', *, *, #15336, .T. ) ;
#20731=ORIENTED_EDGE ( 'NONE', *, *, #19437, .T. ) ;
#20734=CARTESIAN_POINT ( 'NONE',  ( -6.822232771736903637E-13, 9.988891130263535700, 8.559589141758145558 ) ) ;
#20767=B_SPLINE_CURVE_WITH_KNOTS ( 'NONE', 3,
 ( #18024, #23656, #1201, #4873 ),
 .UNSPECIFIED., .F., .F.,
 ( 4, 4 ),
 ( 0.000000000000000000, 0.1802218513154718038 ),
 .UNSPECIFIED. ) ;
#20791=CARTESIAN_POINT ( 'NONE',  ( -9.500000000000000000, -6.482511860946779655E-13, 10.20674201446023233 ) ) ;
#20802=CARTESIAN_POINT ( 'NONE',  ( -8.680847955711200825, 2.820578480813073607, 5.533165578109187521 ) ) ;
#20809=DIRECTION ( 'NONE',  ( 1.000000000000000000, 0.000000000000000000, 0.000000000000000000 ) ) ;
#20816=CARTESIAN_POINT ( 'NONE',  ( 6.222797240145152671E-13, -9.127583699786111282, -12.13316557810918717 ) ) ;
#20822=FACE_OUTER_BOUND ( 'NONE', #20001, .T. ) ;
#20844=( NAMED_UNIT ( * ) PLANE_ANGLE_UNIT ( ) SI_UNIT ( $, .RADIAN. ) );
#20849=CARTESIAN_POINT ( 'NONE',  ( 2.935661446562616295, -9.035036904803758873, 9.659589141758143427 ) ) ;
#20871=CARTESIAN_POINT ( 'NONE',  ( 2.935661446561383503, 9.035036904804158553, 8.459589141758144137 ) ) ;
#20882=CARTESIAN_POINT ( 'NONE',  ( 7.685661446562381371, -5.583959896777971110, -3.859589141758143604 ) ) ;
#20891=( BOUNDED_CURVE ( )  B_SPLINE_CURVE ( 2, ( #15002, #15115, #274, #13173, #9631, #18682, #5862, #9376, #7556 ),
 .UNSPECIFIED., .F., .T. ) 
 B_SPLINE_CURVE_WITH_KNOTS ( ( 3, 2, 2, 2, 3 ),
 ( 0.1207052568533188430, 0.1400000000000000133, 0.1600000000000000033, 0.1799999999999999933, 0.2000000000000000111 ),
 .UNSPECIFIED. ) 
 CURVE ( )  GEOMETRIC_REPRESENTATION_ITEM ( )  RATIONAL_B_SPLINE_CURVE ( ( 0.9966699465879109709, 0.9527824026605606900, 1.000000000000000000, 0.9510565162951535312, 1.000000000000000000, 0.9510565162951535312, 1.000000000000000000, 0.9510565162951535312, 1.000000000000000000 ) ) 
 REPRESENTATION_ITEM ( '' )  );
#20895=DIRECTION ( 'NONE',  ( -1.000000000000000000, 0.000000000000000000, 0.000000000000000000 ) ) ;
#20901=CARTESIAN_POINT ( 'NONE',  ( 5.365059087799947335, -7.384370330706356178, 8.333165578109188232 ) ) ;
#20902=AXIS2_PLACEMENT_3D ( 'NONE', #13232, #9438, #16667 ) ;
#20910=CARTESIAN_POINT ( 'NONE',  ( -2.935661446561384391, -9.035036904804158553, -12.60674201446023446 ) ) ;
#20920=AXIS2_PLACEMENT_3D ( 'NONE', #10222, #21095, #4396 ) ;
#20933=CARTESIAN_POINT ( 'NONE',  ( -5.365059087799947335, 7.384370330706355290, 7.333165578109188232 ) ) ;
#20934=ORIENTED_EDGE ( 'NONE', *, *, #69, .T. ) ;
#20938=ORIENTED_EDGE ( 'NONE', *, *, #4432, .T. ) ;
#20940=CARTESIAN_POINT ( 'NONE',  ( 6.222797240145152671E-13, -9.127583699786111282, -4.133165578109187166 ) ) ;
#20944=LINE ( 'NONE', #9933, #15428 ) ;
#20950=CARTESIAN_POINT ( 'NONE',  ( 6.809999908187194197E-13, -9.988891130263535700, -7.559589141758143782 ) ) ;
#20957=CARTESIAN_POINT ( 'NONE',  ( 6.809999908187194197E-13, -9.988891130263535700, 8.706742014460232326 ) ) ;
#20959=CARTESIAN_POINT ( 'NONE',  ( -7.022953521754877748, -5.102474405760673015, 11.83316557810918823 ) ) ;
#20964=CARTESIAN_POINT ( 'NONE',  ( -2.935661446562617183, 9.035036904803758873, -10.65958914175814343 ) ) ;
#20984=CARTESIAN_POINT ( 'NONE',  ( -9.499999999999790390, -3.086737114213257804, 11.15958914175814520 ) ) ;
#20985=CARTESIAN_POINT ( 'NONE',  ( -5.871322893123450015, -8.081182679344781405, 12.50674201446023481 ) ) ;
#20998=CARTESIAN_POINT ( 'NONE',  ( -8.945956657690407710, -2.657973477511877736, 12.17557883498289506 ) ) ;
#21008=CARTESIAN_POINT ( 'NONE',  ( 9.499999999999790390, 3.086737114213260025, -5.306742014460231971 ) ) ;
#21011=CARTESIAN_POINT ( 'NONE',  ( -7.022953521755574080, 5.102474405759713783, 9.433165578109189653 ) ) ;
#21013=LINE ( 'NONE', #4305, #5938 ) ;
#21019=AXIS2_PLACEMENT_3D ( 'NONE', #1925, #13999, #8502 ) ;
#21021=CARTESIAN_POINT ( 'NONE',  ( -7.685661446562381371, 5.583959896777970222, -10.00674201446023481 ) ) ;
#21024=EDGE_CURVE ( 'NONE', #8523, #23486, #1391, .T. ) ;
#21039=AXIS2_PLACEMENT_3D ( 'NONE', #12395, #21800, #5082 ) ;
#21040=ORIENTED_EDGE ( 'NONE', *, *, #17133, .T. ) ;
#21041=CARTESIAN_POINT ( 'NONE',  ( 6.809999908187194197E-13, -9.988891130263535700, 5.559589141758142894 ) ) ;
#21046=CARTESIAN_POINT ( 'NONE',  ( 8.680847955711007202, 5.912916378492122225E-13, -6.633165578109188942 ) ) ;
#21056=AXIS2_PLACEMENT_3D ( 'NONE', #35, #9522, #22242 ) ;
#21059=CARTESIAN_POINT ( 'NONE',  ( 5.871322893123448239, 8.081182679344781405, -8.359589141758144493 ) ) ;
#21061=CARTESIAN_POINT ( 'NONE',  ( -2.682529543899159208, -8.255977015246598327, -6.033165578109189298 ) ) ;
#21064=ORIENTED_EDGE ( 'NONE', *, *, #8968, .F. ) ;
#21065=CARTESIAN_POINT ( 'NONE',  ( -5.365059087798939252, -7.384370330707086261, 7.933165578109187877 ) ) ;
#21083=( BOUNDED_CURVE ( )  B_SPLINE_CURVE ( 2, ( #7643, #7403, #4133, #9597, #20849, #3880, #11057, #2040, #16925, #9245, #16693 ),
 .UNSPECIFIED., .F., .T. ) 
 B_SPLINE_CURVE_WITH_KNOTS ( ( 3, 2, 2, 2, 2, 3 ),
 ( 0.2000000000000000111, 0.2200000000000000289, 0.2400000000000000466, 0.2600000000000000644, 0.2800000000000001377, 0.3000000000000000999 ),
 .UNSPECIFIED. ) 
 CURVE ( )  GEOMETRIC_REPRESENTATION_ITEM ( )  RATIONAL_B_SPLINE_CURVE ( ( 1.000000000000000000, 0.9510565162951535312, 1.000000000000000000, 0.9510565162951535312, 1.000000000000000000, 0.9510565162951535312, 1.000000000000000000, 0.9510565162951535312, 1.000000000000000000, 0.9510565162951533091, 1.000000000000000222 ) ) 
 REPRESENTATION_ITEM ( '' )  );
#21085=CARTESIAN_POINT ( 'NONE',  ( -2.935661446561384391, -9.035036904804158553, 4.606742014460233570 ) ) ;
#21090=CARTESIAN_POINT ( 'NONE',  ( 7.685661446561619314, 5.583959896779020049, 10.25958914175814485 ) ) ;
#21091=CARTESIAN_POINT ( 'NONE',  ( -2.935661446562617183, 9.035036904803758873, 11.80674201446023375 ) ) ;
#21095=DIRECTION ( 'NONE',  ( 0.000000000000000000, 0.000000000000000000, 1.000000000000000000 ) ) ;
#21096=CARTESIAN_POINT ( 'NONE',  ( 5.871322893123448239, 8.081182679344781405, 6.359589141758142716 ) ) ;
#21099=CARTESIAN_POINT ( 'NONE',  ( 6.669109785867858520, -5.768629174198284915, -12.49999999999999645 ) ) ;
#21106=CARTESIAN_POINT ( 'NONE',  ( 9.499999999999790390, 3.086737114213260025, -4.159589141758141650 ) ) ;
#21110=CARTESIAN_POINT ( 'NONE',  ( 2.124376461992584897, -8.795015941986886077, 12.46040265135714975 ) ) ;
#21118=CARTESIAN_POINT ( 'NONE',  ( 9.500000000000000000, 6.470877716354879437E-13, -5.206742014460234103 ) ) ;
#21123=CARTESIAN_POINT ( 'NONE',  ( 5.365059087799947335, -7.384370330706356178, 6.333165578109188232 ) ) ;
#21135=CARTESIAN_POINT ( 'NONE',  ( -9.250591143756309975, -1.553302072574070714, -12.15226205728695064 ) ) ;
#21141=ORIENTED_EDGE ( 'NONE', *, *, #23128, .T. ) ;
#21155=CARTESIAN_POINT ( 'NONE',  ( -5.871322893123450015, -8.081182679344781405, 5.359589141758144493 ) ) ;
#21169=CARTESIAN_POINT ( 'NONE',  ( -8.680847955710813579, -2.820578480814258437, -5.733165578109188587 ) ) ;
#21177=CARTESIAN_POINT ( 'NONE',  ( -9.500000000000000000, -6.482511860946779655E-13, -9.059589141758143782 ) ) ;
#21188=DIRECTION ( 'NONE',  ( -1.000000000000000000, 0.000000000000000000, 0.000000000000000000 ) ) ;
#21190=CARTESIAN_POINT ( 'NONE',  ( 2.682529543899157876, 8.255977015246598327, -5.033165578109189298 ) ) ;
#21195=ADVANCED_FACE ( 'NONE', ( #9838 ), #9966, .T. ) ;
#21196=CARTESIAN_POINT ( 'NONE',  ( 5.365059087798938364, 7.384370330707087149, 8.933165578109186100 ) ) ;
#21203=CARTESIAN_POINT ( 'NONE',  ( -7.685661446561619314, -5.583959896779019161, -11.25958914175814307 ) ) ;
#21205=CARTESIAN_POINT ( 'NONE',  ( 6.669109785867946449, -5.768629174198188103, 12.50000000000000533 ) ) ;
#21206=CARTESIAN_POINT ( 'NONE',  ( -6.153822176767817416E-13, 9.500000000000000000, 3.706742014460231882 ) ) ;
#21221=CARTESIAN_POINT ( 'NONE',  ( -7.022953521755574080, 5.102474405759713783, -3.433165578109189209 ) ) ;
#21224=AXIS2_PLACEMENT_3D ( 'NONE', #5383, #18313, #20619 ) ;
#21226=CARTESIAN_POINT ( 'NONE',  ( -5.871322893123450015, -8.081182679344781405, 11.35958914175814272 ) ) ;
#21231=CARTESIAN_POINT ( 'NONE',  ( 6.222797240145152671E-13, -9.127583699786111282, -12.13316557810918717 ) ) ;
#21233=DIRECTION ( 'NONE',  ( -0.8660254037844385966, -0.5000000000000003331, 0.000000000000000000 ) ) ;
#21243=VERTEX_POINT ( 'NONE', #15891 ) ;
#21244=CARTESIAN_POINT ( 'NONE',  ( -9.500000000000000000, -6.482511860946779655E-13, 9.059589141758143782 ) ) ;
#21245=CARTESIAN_POINT ( 'NONE',  ( -3.205182335425767803, -8.579959099472988626, 12.34900154096814795 ) ) ;
#21259=CARTESIAN_POINT ( 'NONE',  ( -2.935661446561384391, -9.035036904804158553, -4.606742014460233570 ) ) ;
#21261=CARTESIAN_POINT ( 'NONE',  ( 0.000000000000000000, 0.000000000000000000, -3.499999999999999556 ) ) ;
#21262=CARTESIAN_POINT ( 'NONE',  ( 2.682529543900284974, -8.255977015246234174, 6.233165578109188587 ) ) ;
#21264=EDGE_CURVE ( 'NONE', #13793, #23301, #4674, .T. ) ;
#21266=CARTESIAN_POINT ( 'NONE',  ( 6.250000000000000000, -10.82531754730548279, 2.500000000000000000 ) ) ;
#21274=CARTESIAN_POINT ( 'NONE',  ( -9.500000000000000000, -6.482511860946779655E-13, -10.20674201446023233 ) ) ;
#21276=CARTESIAN_POINT ( 'NONE',  ( -5.294811499230706708, -7.532409217682791258, -12.30101643041108872 ) ) ;
#21284=DIRECTION ( 'NONE',  ( -1.000000000000000000, 0.000000000000000000, 0.000000000000000000 ) ) ;
#21290=EDGE_CURVE ( 'NONE', #19427, #20703, #4896, .T. ) ;
#21296=CARTESIAN_POINT ( 'NONE',  ( -7.685661446561619314, -5.583959896779019161, 7.259589141758143960 ) ) ;
#21300=ORIENTED_EDGE ( 'NONE', *, *, #23128, .F. ) ;
#21302=CARTESIAN_POINT ( 'NONE',  ( -5.365059087799947335, 7.384370330706355290, -5.333165578109189120 ) ) ;
#21314=CARTESIAN_POINT ( 'NONE',  ( 9.500000000000000000, 6.470877716354879437E-13, 8.059589141758143782 ) ) ;
#21315=VERTEX_POINT ( 'NONE', #12341 ) ;
#21316=CARTESIAN_POINT ( 'NONE',  ( 0.6317332097108555589, -9.783628567664221620, 3.581108421866209479 ) ) ;
#21317=CARTESIAN_POINT ( 'NONE',  ( 7.685661446561619314, 5.583959896779020049, 4.259589141758143960 ) ) ;
#21321=CARTESIAN_POINT ( 'NONE',  ( 8.680847955710813579, 2.820578480814259326, -6.733165578109188587 ) ) ;
#21327=EDGE_LOOP ( 'NONE', ( #11673, #2424, #21945, #15487 ) ) ;
#21334=FACE_OUTER_BOUND ( 'NONE', #16450, .T. ) ;
#21341=CARTESIAN_POINT ( 'NONE',  ( 0.000000000000000000, 0.000000000000000000, -12.00000000000000000 ) ) ;
#21351=CARTESIAN_POINT ( 'NONE',  ( -7.022953521755574080, 5.102474405759713783, -5.433165578109188765 ) ) ;
#21354=CARTESIAN_POINT ( 'NONE',  ( -2.935661446561384391, -9.035036904804158553, 7.459589141758144137 ) ) ;
#21355=CARTESIAN_POINT ( 'NONE',  ( -5.871322893124554021, 8.081182679343978492, 11.90674201446023339 ) ) ;
#21360=CARTESIAN_POINT ( 'NONE',  ( -2.935661446562617183, 9.035036904803758873, 2.659589141758143871 ) ) ;
#21365=EDGE_CURVE ( 'NONE', #18928, #17223, #7957, .T. ) ;
#21372=CARTESIAN_POINT ( 'NONE',  ( 9.330908268522556170, -1.784418920662232289, 11.99999999999997691 ) ) ;
#21377=ORIENTED_EDGE ( 'NONE', *, *, #17824, .F. ) ;
#21378=CARTESIAN_POINT ( 'NONE',  ( -9.499999999999790390, -3.086737114213257804, -6.306742014460231971 ) ) ;
#21381=CARTESIAN_POINT ( 'NONE',  ( 7.022953521754877748, 5.102474405760673903, 8.833165578109190008 ) ) ;
#21386=( BOUNDED_SURFACE ( )  B_SPLINE_SURFACE ( 1, 2, ( 
 ( #22272, #11017, #22048, #12496, #18491, #3368, #21906, #23985, #19961, #5325, #8956, #16400, #8852, #7369, #20436, #16183, #6916, #18255, #12748, #3245, #5194, #3595, #16292, #12859, #23752, #1780, #5546, #12628, #23852, #10788, #24094, #10548, #9209, #10673, #18142, #1545, #1440, #16532, #22163, #7140, #18363, #5437, #20210, #3484, #10897, #1653, #9082, #7265, #14704, #20317, #71, #5795, #4212, #20933, #15156, #5685, #18981, #20676, #22520, #1997, #15417, #13222, #17246, #425, #548, #22887, #13108, #5908, #9559, #7474, #20568, #20802, #18847, #17009, #13341, #6158, #7723, #22403, #16754, #22628, #315, #4091, #3957, #11509, #2254, #18723, #14926, #11366, #2132, #7968, #9420, #3845, #9672, #17122, #11140, #11251, #3729 ),
 ( #16882, #2365, #7834, #15277, #22754, #198, #6036, #13478, #9779, #7604, #11623, #19091, #13596, #15049, #18616, #1897, #9311, #9921, #4591, #914, #6267, #793, #14079, #2625, #23376, #10034, #21528, #16022, #23117, #10153, #6403, #2992, #23482, #19713, #4831, #10417, #13846, #22997, #2858, #8469, #11989, #4699, #15915, #4328, #676, #12241, #12102, #17380, #21296, #21413, #15648, #8085, #19458, #17874, #1163, #8337, #13707, #19581, #2736, #17606, #19349, #8577, #15789, #6761, #17746, #21041, #11734, #21155, #23256, #6534, #15530, #4460, #13969, #10289, #1047, #6645, #19211, #2497, #11877, #17490, #8202, #23724, #6992, #3215, #20061, #14420, #6893, #19830, #18112, #1407, #9053, #21774, #17987, #21883, #16269, #21657, #10524 ) ),
 .UNSPECIFIED., .F., .F., .T. ) 
 B_SPLINE_SURFACE_WITH_KNOTS ( ( 2, 2 ),
 ( 3, 2, 2, 2, 2, 2, 2, 2, 2, 2, 2, 2, 2, 2, 2, 2, 2, 2, 2, 2, 2, 2, 2, 2, 2, 2, 2, 2, 2, 2, 2, 2, 2, 2, 2, 2, 2, 2, 2, 2, 2, 2, 2, 2, 2, 2, 2, 2, 3 ),
 ( 0.000000000000000000, 1.000000000000000000 ),
 ( 0.000000000000000000, 0.02000000000000000042, 0.04000000000000000083, 0.05999999999999999778, 0.08000000000000000167, 0.1000000000000000056, 0.1199999999999999956, 0.1400000000000000133, 0.1600000000000000033, 0.1799999999999999933, 0.2000000000000000111, 0.2200000000000000011, 0.2399999999999999911, 0.2600000000000000089, 0.2800000000000000266, 0.2999999999999999889, 0.3200000000000000067, 0.3400000000000000244, 0.3599999999999999867, 0.3800000000000000044, 0.4000000000000000222, 0.4199999999999999845, 0.4400000000000000022, 0.4600000000000000200, 0.4799999999999999822, 0.5000000000000000000, 0.5200000000000000178, 0.5400000000000000355, 0.5600000000000000533, 0.5799999999999999600, 0.5999999999999999778, 0.6199999999999999956, 0.6400000000000000133, 0.6600000000000000311, 0.6800000000000000488, 0.6999999999999999556, 0.7199999999999999734, 0.7399999999999999911, 0.7600000000000000089, 0.7800000000000000266, 0.8000000000000000444, 0.8199999999999999512, 0.8399999999999999689, 0.8599999999999999867, 0.8800000000000000044, 0.9000000000000000222, 0.9200000000000000400, 0.9399999999999999467, 0.9500000000000000666 ),
 .UNSPECIFIED. ) 
 GEOMETRIC_REPRESENTATION_ITEM ( )  RATIONAL_B_SPLINE_SURFACE ( (
 ( 1.000000000000000000, 0.9510565162951535312, 1.000000000000000000, 0.9510565162951535312, 1.000000000000000000, 0.9510565162951535312, 1.000000000000000000, 0.9510565162951535312, 1.000000000000000000, 0.9510565162951535312, 1.000000000000000000, 0.9510565162951535312, 1.000000000000000000, 0.9510565162951535312, 1.000000000000000000, 0.9510565162951535312, 1.000000000000000000, 0.9510565162951535312, 1.000000000000000000, 0.9510565162951535312, 1.000000000000000000, 0.9510565162951535312, 1.000000000000000000, 0.9510565162951535312, 1.000000000000000000, 0.9510565162951535312, 1.000000000000000000, 0.9510565162951535312, 1.000000000000000000, 0.9510565162951535312, 1.000000000000000000, 0.9510565162951535312, 1.000000000000000000, 0.9510565162951535312, 1.000000000000000000, 0.9510565162951535312, 1.000000000000000000, 0.9510565162951535312, 1.000000000000000000, 0.9510565162951535312, 1.000000000000000000, 0.9510565162951535312, 1.000000000000000000, 0.9510565162951535312, 1.000000000000000000, 0.9510565162951535312, 1.000000000000000000, 0.9510565162951535312, 1.000000000000000000, 0.9510565162951535312, 1.000000000000000000, 0.9510565162951535312, 1.000000000000000000, 0.9510565162951535312, 1.000000000000000000, 0.9510565162951535312, 1.000000000000000000, 0.9510565162951535312, 1.000000000000000000, 0.9510565162951535312, 1.000000000000000000, 0.9510565162951535312, 1.000000000000000000, 0.9510565162951535312, 1.000000000000000000, 0.9510565162951535312, 1.000000000000000000, 0.9510565162951535312, 1.000000000000000000, 0.9510565162951535312, 1.000000000000000000, 0.9510565162951535312, 1.000000000000000000, 0.9510565162951535312, 1.000000000000000000, 0.9510565162951535312, 1.000000000000000000, 0.9510565162951535312, 1.000000000000000000, 0.9510565162951535312, 1.000000000000000000, 0.9510565162951535312, 1.000000000000000000, 0.9510565162951535312, 1.000000000000000000, 0.9510565162951535312, 1.000000000000000000, 0.9510565162951535312, 1.000000000000000000, 0.9510565162951535312, 1.000000000000000000, 0.9510565162951535312, 1.000000000000000000, 0.9510565162951535312, 1.000000000000000000, 0.9755282581475764880, 0.9755282581475768211),
 ( 1.000000000000000000, 0.9510565162951535312, 1.000000000000000000, 0.9510565162951535312, 1.000000000000000000, 0.9510565162951535312, 1.000000000000000000, 0.9510565162951535312, 1.000000000000000000, 0.9510565162951535312, 1.000000000000000000, 0.9510565162951535312, 1.000000000000000000, 0.9510565162951535312, 1.000000000000000000, 0.9510565162951535312, 1.000000000000000000, 0.9510565162951535312, 1.000000000000000000, 0.9510565162951535312, 1.000000000000000000, 0.9510565162951535312, 1.000000000000000000, 0.9510565162951535312, 1.000000000000000000, 0.9510565162951535312, 1.000000000000000000, 0.9510565162951535312, 1.000000000000000000, 0.9510565162951535312, 1.000000000000000000, 0.9510565162951535312, 1.000000000000000000, 0.9510565162951535312, 1.000000000000000000, 0.9510565162951535312, 1.000000000000000000, 0.9510565162951535312, 1.000000000000000000, 0.9510565162951535312, 1.000000000000000000, 0.9510565162951535312, 1.000000000000000000, 0.9510565162951535312, 1.000000000000000000, 0.9510565162951535312, 1.000000000000000000, 0.9510565162951535312, 1.000000000000000000, 0.9510565162951535312, 1.000000000000000000, 0.9510565162951535312, 1.000000000000000000, 0.9510565162951535312, 1.000000000000000000, 0.9510565162951535312, 1.000000000000000000, 0.9510565162951535312, 1.000000000000000000, 0.9510565162951535312, 1.000000000000000000, 0.9510565162951535312, 1.000000000000000000, 0.9510565162951535312, 1.000000000000000000, 0.9510565162951535312, 1.000000000000000000, 0.9510565162951535312, 1.000000000000000000, 0.9510565162951535312, 1.000000000000000000, 0.9510565162951535312, 1.000000000000000000, 0.9510565162951535312, 1.000000000000000000, 0.9510565162951535312, 1.000000000000000000, 0.9510565162951535312, 1.000000000000000000, 0.9510565162951535312, 1.000000000000000000, 0.9510565162951535312, 1.000000000000000000, 0.9510565162951535312, 1.000000000000000000, 0.9510565162951535312, 1.000000000000000000, 0.9510565162951535312, 1.000000000000000000, 0.9510565162951535312, 1.000000000000000000, 0.9510565162951535312, 1.000000000000000000, 0.9510565162951535312, 1.000000000000000000, 0.9755282581475764880, 0.9755282581475768211) ) ) 
 REPRESENTATION_ITEM ( '' )  SURFACE ( )  );
#21405=LINE ( 'NONE', #16014, #13387 ) ;
#21411=CARTESIAN_POINT ( 'NONE',  ( 2.935661446561383503, 9.035036904804158553, -4.459589141758144137 ) ) ;
#21413=CARTESIAN_POINT ( 'NONE',  ( -9.499999999999790390, -3.086737114213257804, 7.159589141758144315 ) ) ;
#21417=CARTESIAN_POINT ( 'NONE',  ( -5.365059087798939252, -7.384370330707086261, -3.933165578109188321 ) ) ;
#21427=ORIENTED_EDGE ( 'NONE', *, *, #13542, .F. ) ;
#21428=CARTESIAN_POINT ( 'NONE',  ( 9.500000000000209610, -3.086737114211962396, -9.106742014460232681 ) ) ;
#21430=CARTESIAN_POINT ( 'NONE',  ( -6.153822176767817416E-13, 9.500000000000000000, 3.706742014460232326 ) ) ;
#21437=CARTESIAN_POINT ( 'NONE',  ( -7.022953521755574080, 5.102474405759713783, -9.433165578109189653 ) ) ;
#21441=CARTESIAN_POINT ( 'NONE',  ( 8.680847955711199049, -2.820578480813074496, 8.533165578109187521 ) ) ;
#21449=CARTESIAN_POINT ( 'NONE',  ( 7.685661446562381371, -5.583959896777971110, -11.85958914175814449 ) ) ;
#21465=CARTESIAN_POINT ( 'NONE',  ( -2.935661446561384391, -9.035036904804158553, -12.60674201446023446 ) ) ;
#21469=CARTESIAN_POINT ( 'NONE',  ( -2.935661446562617183, 9.035036904803758873, 2.659589141758143871 ) ) ;
#21475=CARTESIAN_POINT ( 'NONE',  ( -9.499999999999790390, -3.086737114213257804, 3.159589141758143871 ) ) ;
#21482=ORIENTED_EDGE ( 'NONE', *, *, #10149, .F. ) ;
#21491=CARTESIAN_POINT ( 'NONE',  ( -9.500000000000000000, -6.482511860946779655E-13, 9.059589141758143782 ) ) ;
#21495=CARTESIAN_POINT ( 'NONE',  ( -7.022953521754877748, -5.102474405760673015, 3.833165578109188676 ) ) ;
#21502=CARTESIAN_POINT ( 'NONE',  ( 6.809999908187194197E-13, -9.988891130263535700, 5.559589141758142894 ) ) ;
#21508=CARTESIAN_POINT ( 'NONE',  ( 7.685661446562381371, -5.583959896777971110, -7.006742014460233037 ) ) ;
#21509=ORIENTED_EDGE ( 'NONE', *, *, #18143, .T. ) ;
#21510=CARTESIAN_POINT ( 'NONE',  ( 3.239832068448452951, -8.450089895365024972, -12.48376408781543034 ) ) ;
#21524=ORIENTED_EDGE ( 'NONE', *, *, #12997, .F. ) ;
#21528=CARTESIAN_POINT ( 'NONE',  ( -2.935661446561384391, -9.035036904804158553, 9.459589141758144137 ) ) ;
#21548=CARTESIAN_POINT ( 'NONE',  ( -6.250000000000000888, 10.82531754730548279, -2.500000000000000000 ) ) ;
#21549=CARTESIAN_POINT ( 'NONE',  ( -7.685661446561619314, -5.583959896779019161, 4.406742014460233392 ) ) ;
#21550=CARTESIAN_POINT ( 'NONE',  ( 9.500000000000209610, -3.086737114211962396, 3.959589141758144581 ) ) ;
#21551=DIRECTION ( 'NONE',  ( 1.000000000000000000, 0.000000000000000000, 0.000000000000000000 ) ) ;
#21563=VERTEX_POINT ( 'NONE', #4032 ) ;
#21565=CARTESIAN_POINT ( 'NONE',  ( 5.365059087798938364, 7.384370330707087149, 6.933165578109188765 ) ) ;
#21576=CARTESIAN_POINT ( 'NONE',  ( -9.500000000000000000, -6.482511860946779655E-13, -7.059589141758143782 ) ) ;
#21578=CARTESIAN_POINT ( 'NONE',  ( 8.199992213793651175, -2.961991314798469332, 12.49999999999999467 ) ) ;
#21592=ADVANCED_FACE ( 'NONE', ( #1948 ), #22831, .T. ) ;
#21597=CARTESIAN_POINT ( 'NONE',  ( 9.499999999999790390, 3.086737114213260025, 4.159589141758141650 ) ) ;
#21606=CARTESIAN_POINT ( 'NONE',  ( 9.499999999999799272, 3.086737114213245370, 6.159589141758142539 ) ) ;
#21612=ORIENTED_EDGE ( 'NONE', *, *, #10865, .F. ) ;
#21614=CARTESIAN_POINT ( 'NONE',  ( 7.685661446562381371, -5.583959896777971110, 11.85958914175814449 ) ) ;
#21624=CARTESIAN_POINT ( 'NONE',  ( -5.365059087798940141, -7.384370330707086261, 3.933165578109187877 ) ) ;
#21626=DIRECTION ( 'NONE',  ( -0.000000000000000000, -0.000000000000000000, -1.000000000000000000 ) ) ;
#21635=CARTESIAN_POINT ( 'NONE',  ( 7.685661446562381371, -5.583959896777971110, -5.006742014460233037 ) ) ;
#21637=AXIS2_PLACEMENT_3D ( 'NONE', #14852, #10941, #22325 ) ;
#21657=CARTESIAN_POINT ( 'NONE',  ( -1.504652183083727168, 9.499999999999904077, 2.610843423304989308 ) ) ;
#21674=CARTESIAN_POINT ( 'NONE',  ( -9.500000000000000000, -6.482511860946779655E-13, 4.206742014460233214 ) ) ;
#21683=CARTESIAN_POINT ( 'NONE',  ( -2.682529543900285862, 8.255977015246234174, -3.233165578109188587 ) ) ;
#21686=CARTESIAN_POINT ( 'NONE',  ( 8.680847955711007202, 5.912916378492122225E-13, 4.633165578109188942 ) ) ;
#21693=DIRECTION ( 'NONE',  ( 1.000000000000000000, 0.000000000000000000, 0.000000000000000000 ) ) ;
#21694=CARTESIAN_POINT ( 'NONE',  ( 7.685661446562381371, -5.583959896777971110, -5.859589141758143604 ) ) ;
#21701=LINE ( 'NONE', #17536, #23876 ) ;
#21716=CARTESIAN_POINT ( 'NONE',  ( 7.022953521754877748, 5.102474405760673903, -4.833165578109188232 ) ) ;
#21719=CARTESIAN_POINT ( 'NONE',  ( 6.809999908187194197E-13, -9.988891130263535700, 7.559589141758143782 ) ) ;
#21720=CARTESIAN_POINT ( 'NONE',  ( -2.935661446561384391, -9.035036904804158553, 6.606742014460233570 ) ) ;
#21724=CARTESIAN_POINT ( 'NONE',  ( -5.871322893123449127, -8.081182679344781405, -4.506742014460232149 ) ) ;
#21726=EDGE_CURVE ( 'NONE', #3425, #18928, #18731, .T. ) ;
#21735=CARTESIAN_POINT ( 'NONE',  ( 9.500000000000000000, 6.470877716354879437E-13, 10.05958914175814378 ) ) ;
#21737=CARTESIAN_POINT ( 'NONE',  ( -2.466888520469390222, 9.179244532860076689, -3.500783152383143193 ) ) ;
#21744=EDGE_LOOP ( 'NONE', ( #20526, #8945, #12818, #15365 ) ) ;
#21745=CARTESIAN_POINT ( 'NONE',  ( 8.680847955711199049, -2.820578480813074496, 4.533165578109188409 ) ) ;
#21756=CARTESIAN_POINT ( 'NONE',  ( -2.935661446562617183, 9.035036904803758873, -7.806742014460233747 ) ) ;
#21770=CARTESIAN_POINT ( 'NONE',  ( -9.500000000000202505, 3.086737114211975275, -10.10674201446023268 ) ) ;
#21771=DIRECTION ( 'NONE',  ( 0.000000000000000000, 0.000000000000000000, -1.000000000000000000 ) ) ;
#21772=CARTESIAN_POINT ( 'NONE',  ( 9.499999999999790390, 3.086737114213260025, -4.159589141758142539 ) ) ;
#21774=CARTESIAN_POINT ( 'NONE',  ( -9.500000000000211386, 3.086737114211961064, 2.959589141758143249 ) ) ;
#21784=CARTESIAN_POINT ( 'NONE',  ( -12.50000000000000178, 1.672973214995343413E-15, 2.500000000000000000 ) ) ;
#21800=DIRECTION ( 'NONE',  ( 0.000000000000000000, 0.000000000000000000, 1.000000000000000000 ) ) ;
#21801=ORIENTED_EDGE ( 'NONE', *, *, #1849, .F. ) ;
#21806=CARTESIAN_POINT ( 'NONE',  ( 6.809999908187194197E-13, -9.988891130263535700, -7.559589141758143782 ) ) ;
#21810=DIRECTION ( 'NONE',  ( -1.000000000000000000, 0.000000000000000000, 0.000000000000000000 ) ) ;
#21823=CARTESIAN_POINT ( 'NONE',  ( 5.871322893123449127, 8.081182679344781405, -9.506742014460231260 ) ) ;
#21826=CARTESIAN_POINT ( 'NONE',  ( -5.871322893124554021, 8.081182679343978492, 6.759589141758143072 ) ) ;
#21827=CARTESIAN_POINT ( 'NONE',  ( 2.935661446561383503, 9.035036904804158553, 7.606742014460233570 ) ) ;
#21842=CARTESIAN_POINT ( 'NONE',  ( -5.871322893124554021, 8.081182679343978492, 10.75958914175814130 ) ) ;
#21845=CIRCLE ( 'NONE', #17160, 9.500000000000000000 ) ;
#21847=CARTESIAN_POINT ( 'NONE',  ( 8.680847955711199049, -2.820578480813074496, -8.533165578109187521 ) ) ;
#21853=CARTESIAN_POINT ( 'NONE',  ( 7.022953521754877748, 5.102474405760673903, 4.833165578109188232 ) ) ;
#21866=CARTESIAN_POINT ( 'NONE',  ( -2.935661446562617183, 9.035036904803758873, -3.806742014460233303 ) ) ;
#21869=CARTESIAN_POINT ( 'NONE',  ( -6.153822176767817416E-13, 9.500000000000000000, -3.500000000000014211 ) ) ;
#21880=CARTESIAN_POINT ( 'NONE',  ( -5.871322893124554021, 8.081182679343978492, -9.906742014460235168 ) ) ;
#21883=CARTESIAN_POINT ( 'NONE',  ( -5.871322893124554021, 8.081182679343978492, 2.759589141758142627 ) ) ;
#21885=EDGE_CURVE ( 'NONE', #1372, #1207, #3782, .T. ) ;
#21896=CARTESIAN_POINT ( 'NONE',  ( -6.153822176767817416E-13, 9.500000000000000000, -3.706742014460231882 ) ) ;
#21898=CARTESIAN_POINT ( 'NONE',  ( 5.871322893124553133, -8.081182679343980269, 4.906742014460232504 ) ) ;
#21902=CARTESIAN_POINT ( 'NONE',  ( -6.250000000000000888, 10.82531754730548279, 2.500000000000000000 ) ) ;
#21906=CARTESIAN_POINT ( 'NONE',  ( -2.682529543899159208, -8.255977015246598327, 12.03316557810918930 ) ) ;
#21917=DIRECTION ( 'NONE',  ( 0.000000000000000000, 0.000000000000000000, 1.000000000000000000 ) ) ;
#21921=CARTESIAN_POINT ( 'NONE',  ( 9.500000000000209610, -3.086737114211962396, -3.959589141758145026 ) ) ;
#21923=FACE_OUTER_BOUND ( 'NONE', #11336, .T. ) ;
#21926=ORIENTED_EDGE ( 'NONE', *, *, #23492, .T. ) ;
#21945=ORIENTED_EDGE ( 'NONE', *, *, #18882, .F. ) ;
#21948=CARTESIAN_POINT ( 'NONE',  ( 7.685661446561619314, 5.583959896779020049, 11.40674201446023517 ) ) ;
#21949=CARTESIAN_POINT ( 'NONE',  ( 5.871322893124553133, -8.081182679343980269, 6.906742014460234280 ) ) ;
#21959=LINE ( 'NONE', #18191, #22710 ) ;
#21961=CARTESIAN_POINT ( 'NONE',  ( -7.685661446562381371, 5.583959896777970222, -10.85958914175814449 ) ) ;
#21966=CARTESIAN_POINT ( 'NONE',  ( -6.944120675781903174, 6.490472247601844380, -3.501262065910452748 ) ) ;
#21967=CARTESIAN_POINT ( 'NONE',  ( 2.935661446562616295, -9.035036904803758873, -11.65958914175814520 ) ) ;
#21971=EDGE_CURVE ( 'NONE', #17223, #12845, #2172, .T. ) ;
#21979=CARTESIAN_POINT ( 'NONE',  ( -9.500000000000000000, -6.482511860946779655E-13, -9.059589141758143782 ) ) ;
#21981=CARTESIAN_POINT ( 'NONE',  ( -6.249999999999999112, -10.82531754730548279, -2.500000000000000000 ) ) ;
#21993=CARTESIAN_POINT ( 'NONE',  ( -7.685661446562381371, 5.583959896777970222, -6.006742014460233037 ) ) ;
#22014=CARTESIAN_POINT ( 'NONE',  ( -9.500000000000211386, 3.086737114211961064, -4.106742014460232681 ) ) ;
#22025=EDGE_CURVE ( 'NONE', #18771, #18651, #21083, .T. ) ;
#22033=CARTESIAN_POINT ( 'NONE',  ( -9.319542265568680151, 1.279802608863929159, 12.09643368198983104 ) ) ;
#22037=CARTESIAN_POINT ( 'NONE',  ( -5.871322893123449127, -8.081182679344781405, 10.50674201446023304 ) ) ;
#22048=CARTESIAN_POINT ( 'NONE',  ( 7.022953521755574080, -5.102474405759714671, 12.43316557810918788 ) ) ;
#22053=ORIENTED_EDGE ( 'NONE', *, *, #843, .T. ) ;
#22056=CARTESIAN_POINT ( 'NONE',  ( -2.935661446562617183, 9.035036904803758873, -8.659589141758143427 ) ) ;
#22061=CARTESIAN_POINT ( 'NONE',  ( -5.976739099259236459E-13, 9.226949318570335734, 3.515549869009883643 ) ) ;
#22063=B_SPLINE_CURVE_WITH_KNOTS ( 'NONE', 3,
 ( #19057, #16521, #22702, #2330, #22033, #4292, #7921, #15371, #14566, #5316, #11695, #2446, #23973, #3917 ),
 .UNSPECIFIED., .F., .F.,
 ( 4, 2, 2, 2, 2, 2, 4 ),
 ( 0.01861151281497951115, 0.01937988632622441448, 0.02014825983746932128, 0.02168500685995913141, 0.02245338037120403474, 0.02322175388244893807, 0.02475850090493875166 ),
 .UNSPECIFIED. ) ;
#22065=DIRECTION ( 'NONE',  ( -0.000000000000000000, -0.000000000000000000, 1.000000000000000000 ) ) ;
#22067=CARTESIAN_POINT ( 'NONE',  ( 2.935661446562616295, -9.035036904803758873, -6.806742014460233747 ) ) ;
#22081=CARTESIAN_POINT ( 'NONE',  ( -9.499999999999790390, -3.086737114213257804, 8.306742014460233747 ) ) ;
#22082=CARTESIAN_POINT ( 'NONE',  ( -7.685661446562381371, 5.583959896777970222, 8.006742014460233037 ) ) ;
#22084=ORIENTED_EDGE ( 'NONE', *, *, #6585, .F. ) ;
#22094=CARTESIAN_POINT ( 'NONE',  ( 0.000000000000000000, 0.000000000000000000, 3.499999999999999556 ) ) ;
#22100=ORIENTED_EDGE ( 'NONE', *, *, #10790, .T. ) ;
#22112=CARTESIAN_POINT ( 'NONE',  ( 9.499999999999790390, 3.086737114213260025, 8.159589141758143427 ) ) ;
#22122=CARTESIAN_POINT ( 'NONE',  ( -6.153822176767817416E-13, 9.500000000000000000, -2.559589141758142894 ) ) ;
#22127=CARTESIAN_POINT ( 'NONE',  ( 5.871322893124553133, -8.081182679343980269, -7.759589141758143072 ) ) ;
#22140=CARTESIAN_POINT ( 'NONE',  ( -8.680847955711200825, 2.820578480813073607, 3.533165578109187965 ) ) ;
#22151=ORIENTED_EDGE ( 'NONE', *, *, #11828, .F. ) ;
#22157=CARTESIAN_POINT ( 'NONE',  ( 9.500000000000000000, 6.470877716354879437E-13, 11.20674201446023410 ) ) ;
#22161=DIRECTION ( 'NONE',  ( 1.000000000000000000, 0.000000000000000000, 0.000000000000000000 ) ) ;
#22163=CARTESIAN_POINT ( 'NONE',  ( 7.022953521754877748, 5.102474405760673903, 8.833165578109190008 ) ) ;
#22173=CARTESIAN_POINT ( 'NONE',  ( -7.685661446561619314, -5.583959896779019161, -3.259589141758143516 ) ) ;
#22176=ORIENTED_EDGE ( 'NONE', *, *, #13087, .F. ) ;
#22182=ORIENTED_EDGE ( 'NONE', *, *, #8278, .T. ) ;
#22183=CARTESIAN_POINT ( 'NONE',  ( -2.935661446561384391, -9.035036904804158553, -6.606742014460233570 ) ) ;
#22196=CARTESIAN_POINT ( 'NONE',  ( 7.685661446561619314, 5.583959896779020049, 9.406742014460235168 ) ) ;
#22199=ADVANCED_FACE ( 'NONE', ( #21334 ), #23606, .F. ) ;
#22207=CARTESIAN_POINT ( 'NONE',  ( 5.871322893123448239, 8.081182679344781405, -10.35958914175814449 ) ) ;
#22211=DIRECTION ( 'NONE',  ( 1.224646799147353207E-16, 1.000000000000000000, -0.000000000000000000 ) ) ;
#22219=ORIENTED_EDGE ( 'NONE', *, *, #6037, .T. ) ;
#22230=CARTESIAN_POINT ( 'NONE',  ( 2.935661446561383503, 9.035036904804158553, -4.459589141758144137 ) ) ;
#22242=DIRECTION ( 'NONE',  ( -6.485355633664482599E-14, 1.000000000000000000, 0.000000000000000000 ) ) ;
#22244=CARTESIAN_POINT ( 'NONE',  ( 7.564539288232146497, -4.357045548396729195, 12.46583266205520246 ) ) ;
#22247=CARTESIAN_POINT ( 'NONE',  ( -1.374911245008260563, 8.680847955710920161, 3.184419859656034024 ) ) ;
#22258=LINE ( 'NONE', #1881, #10826 ) ;
#22270=ORIENTED_EDGE ( 'NONE', *, *, #9904, .F. ) ;
#22272=CARTESIAN_POINT ( 'NONE',  ( 8.680847955711007202, 5.912916378492122225E-13, 12.63316557810918894 ) ) ;
#22280=CARTESIAN_POINT ( 'NONE',  ( 8.680847955711007202, 5.912916378492122225E-13, -12.63316557810918894 ) ) ;
#22289=FACE_OUTER_BOUND ( 'NONE', #19360, .T. ) ;
#22309=CARTESIAN_POINT ( 'NONE',  ( 9.500000000000000000, 6.470877716354879437E-13, 11.20674201446023410 ) ) ;
#22324=AXIS2_PLACEMENT_3D ( 'NONE', #12239, #21771, #1159 ) ;
#22325=DIRECTION ( 'NONE',  ( 1.000000000000000000, 0.000000000000000000, 0.000000000000000000 ) ) ;
#22331=LINE ( 'NONE', #16455, #6230 ) ;
#22333=CARTESIAN_POINT ( 'NONE',  ( -8.680847955710813579, -2.820578480814258437, -9.733165578109186811 ) ) ;
#22344=DIRECTION ( 'NONE',  ( 0.000000000000000000, 0.000000000000000000, 1.000000000000000000 ) ) ;
#22351=CARTESIAN_POINT ( 'NONE',  ( 9.499999999999790390, 3.086737114213260025, -8.159589141758143427 ) ) ;
#22362=ORIENTED_EDGE ( 'NONE', *, *, #23581, .F. ) ;
#22403=CARTESIAN_POINT ( 'NONE',  ( 5.365059087798938364, 7.384370330707087149, 4.933165578109187877 ) ) ;
#22410=CARTESIAN_POINT ( 'NONE',  ( -2.935661446562617183, 9.035036904803758873, -2.659589141758143871 ) ) ;
#22433=CARTESIAN_POINT ( 'NONE',  ( 6.222797240145152671E-13, -9.127583699786111282, -12.13316557810918717 ) ) ;
#22434=CARTESIAN_POINT ( 'NONE',  ( 7.685661446562381371, -5.583959896777971110, 9.006742014460233037 ) ) ;
#22463=VERTEX_POINT ( 'NONE', #1874 ) ;
#22465=ORIENTED_EDGE ( 'NONE', *, *, #17424, .T. ) ;
#22479=CARTESIAN_POINT ( 'NONE',  ( -9.500000000000000000, -6.482511860946779655E-13, -7.059589141758143782 ) ) ;
#22482=CARTESIAN_POINT ( 'NONE',  ( 0.000000000000000000, 0.000000000000000000, 2.500000000000000000 ) ) ;
#22484=CARTESIAN_POINT ( 'NONE',  ( 2.935661446561383503, 9.035036904804158553, 5.606742014460233570 ) ) ;
#22491=DIRECTION ( 'NONE',  ( -1.000000000000000000, 0.000000000000000000, 0.000000000000000000 ) ) ;
#22520=CARTESIAN_POINT ( 'NONE',  ( 7.022953521754877748, 5.102474405760673903, 6.833165578109188232 ) ) ;
#22525=ORIENTED_EDGE ( 'NONE', *, *, #15175, .F. ) ;
#22526=ADVANCED_FACE ( 'NONE', ( #50 ), #18470, .F. ) ;
#22528=CARTESIAN_POINT ( 'NONE',  ( -8.680847955711200825, 2.820578480813073607, -7.533165578109188409 ) ) ;
#22538=CARTESIAN_POINT ( 'NONE',  ( -9.500000000000000000, -6.482511860946779655E-13, -7.059589141758143782 ) ) ;
#22544=CARTESIAN_POINT ( 'NONE',  ( -7.022953521755574080, 5.102474405759713783, -11.43316557810918965 ) ) ;
#22559=PLANE ( 'NONE',  #17593 ) ;
#22565=CARTESIAN_POINT ( 'NONE',  ( 12.50000000000000178, 5.755434930044642846E-15, 2.500000000000000000 ) ) ;
#22567=CARTESIAN_POINT ( 'NONE',  ( 5.871322893123449127, 8.081182679344781405, 10.35958914175814627 ) ) ;
#22572=CARTESIAN_POINT ( 'NONE',  ( -6.153822176767817416E-13, 9.500000000000000000, -2.559589141758142894 ) ) ;
#22578=CARTESIAN_POINT ( 'NONE',  ( 5.871322893124553133, -8.081182679343980269, -5.759589141758144848 ) ) ;
#22582=LINE ( 'NONE', #10661, #132 ) ;
#22601=FACE_OUTER_BOUND ( 'NONE', #3084, .T. ) ;
#22619=LINE ( 'NONE', #16871, #1367 ) ;
#22628=CARTESIAN_POINT ( 'NONE',  ( 8.680847955710813579, 2.820578480814259326, 4.733165578109188587 ) ) ;
#22630=CARTESIAN_POINT ( 'NONE',  ( 9.500000000000000000, 6.470877716354879437E-13, 6.059589141758143782 ) ) ;
#22634=CARTESIAN_POINT ( 'NONE',  ( 2.682529543899157876, 8.255977015246598327, -11.03316557810918752 ) ) ;
#22643=ORIENTED_EDGE ( 'NONE', *, *, #21365, .T. ) ;
#22648=CARTESIAN_POINT ( 'NONE',  ( 5.871322893124551356, -8.081182679343980269, -7.759589141758143072 ) ) ;
#22649=CARTESIAN_POINT ( 'NONE',  ( -5.622572944242077574E-13, 8.680847955711007202, 3.133165578109187610 ) ) ;
#22653=CARTESIAN_POINT ( 'NONE',  ( 5.365059087799947335, -7.384370330706356178, -12.33316557810918823 ) ) ;
#22656=ORIENTED_EDGE ( 'NONE', *, *, #23098, .F. ) ;
#22670=VERTEX_POINT ( 'NONE', #2347 ) ;
#22679=EDGE_LOOP ( 'NONE', ( #13215, #23453, #3662, #18754 ) ) ;
#22683=CARTESIAN_POINT ( 'NONE',  ( -7.685661446562381371, 5.583959896777970222, 8.859589141758144493 ) ) ;
#22692=CIRCLE ( 'NONE', #15262, 8.999999999999998224 ) ;
#22696=CARTESIAN_POINT ( 'NONE',  ( 6.809999908187194197E-13, -9.988891130263535700, -3.559589141758143338 ) ) ;
#22697=DIRECTION ( 'NONE',  ( 0.000000000000000000, 0.000000000000000000, 1.000000000000000000 ) ) ;
#22702=CARTESIAN_POINT ( 'NONE',  ( -9.377778780038873663, 0.5146052038006584395, 12.11160675903709816 ) ) ;
#22710=VECTOR ( 'NONE', #9130, 1000.000000000000114 ) ;
#22713=CARTESIAN_POINT ( 'NONE',  ( -9.499999999999790390, -3.086737114213257804, -4.306742014460233747 ) ) ;
#22714=ORIENTED_EDGE ( 'NONE', *, *, #2189, .F. ) ;
#22717=CARTESIAN_POINT ( 'NONE',  ( 8.680847955711007202, 5.912916378492122225E-13, 8.633165578109188942 ) ) ;
#22722=ORIENTED_EDGE ( 'NONE', *, *, #17133, .F. ) ;
#22732=CARTESIAN_POINT ( 'NONE',  ( 5.871322893124553133, -8.081182679343980269, -10.90674201446023339 ) ) ;
#22740=ORIENTED_EDGE ( 'NONE', *, *, #19498, .T. ) ;
#22741=CARTESIAN_POINT ( 'NONE',  ( -5.279840276022249590, -7.916949377623846651, -3.501202454935721686 ) ) ;
#22754=CARTESIAN_POINT ( 'NONE',  ( 2.935661446562616295, -9.035036904803758873, 11.65958914175814520 ) ) ;
#22765=CARTESIAN_POINT ( 'NONE',  ( -5.622572944242076564E-13, 8.680847955711007202, -3.133165578109187166 ) ) ;
#22778=CARTESIAN_POINT ( 'NONE',  ( 9.500000000000209610, -3.086737114211962396, -7.959589141758143249 ) ) ;
#22789=CARTESIAN_POINT ( 'NONE',  ( 7.022953521754877748, 5.102474405760673903, 10.83316557810919001 ) ) ;
#22800=CARTESIAN_POINT ( 'NONE',  ( 2.935661446562616295, -9.035036904803758873, -10.80674201446023197 ) ) ;
#22802=CARTESIAN_POINT ( 'NONE',  ( 5.871322893124551356, -8.081182679343980269, 6.906742014460233392 ) ) ;
#22813=( BOUNDED_CURVE ( )  B_SPLINE_CURVE ( 2, ( #8972, #23875, #7156, #14722, #22067, #12766, #22183, #697, #11758, #19111, #9938 ),
 .UNSPECIFIED., .F., .T. ) 
 B_SPLINE_CURVE_WITH_KNOTS ( ( 3, 2, 2, 2, 2, 3 ),
 ( 0.6000000000000000888, 0.6200000000000001066, 0.6400000000000001243, 0.6600000000000001421, 0.6800000000000001599, 0.7000000000000000666 ),
 .UNSPECIFIED. ) 
 CURVE ( )  GEOMETRIC_REPRESENTATION_ITEM ( )  RATIONAL_B_SPLINE_CURVE ( ( 0.9999999999999997780, 0.9510565162951537532, 1.000000000000000000, 0.9510565162951535312, 1.000000000000000000, 0.9510565162951535312, 1.000000000000000000, 0.9510565162951535312, 1.000000000000000000, 0.9510565162951533091, 1.000000000000000222 ) ) 
 REPRESENTATION_ITEM ( '' )  );
#22820=CARTESIAN_POINT ( 'NONE',  ( 9.500000000000209610, -3.086737114211962396, 9.959589141758145914 ) ) ;
#22829=ORIENTED_EDGE ( 'NONE', *, *, #10044, .F. ) ;
#22831=CYLINDRICAL_SURFACE ( 'NONE', #15000, 9.500000000000000000 ) ;
#22839=PLANE ( 'NONE',  #10589 ) ;
#22842=FACE_BOUND ( 'NONE', #7033, .T. ) ;
#22848=DIRECTION ( 'NONE',  ( -0.7071067811865487940, -4.816422645751019675E-14, -0.7071067811865463515 ) ) ;
#22850=CARTESIAN_POINT ( 'NONE',  ( -5.871322893123450015, -8.081182679344781405, -4.506742014460231260 ) ) ;
#22852=DIRECTION ( 'NONE',  ( -1.000000000000000000, 0.000000000000000000, 0.000000000000000000 ) ) ;
#22853=CARTESIAN_POINT ( 'NONE',  ( -2.682529543900285862, 8.255977015246234174, 7.233165578109188587 ) ) ;
#22863=AXIS2_PLACEMENT_3D ( 'NONE', #22094, #12790, #5478 ) ;
#22867=CARTESIAN_POINT ( 'NONE',  ( 7.685661446562381371, -5.583959896777971110, -13.00674201446023304 ) ) ;
#22873=CARTESIAN_POINT ( 'NONE',  ( -3.828533837984870125, -8.711343052635822204, -3.501988579199554863 ) ) ;
#22877=LINE ( 'NONE', #11495, #9097 ) ;
#22886=ORIENTED_EDGE ( 'NONE', *, *, #18761, .F. ) ;
#22887=CARTESIAN_POINT ( 'NONE',  ( 6.222797240145152671E-13, -9.127583699786111282, 6.133165578109188942 ) ) ;
#22896=EDGE_LOOP ( 'NONE', ( #13089, #17098, #21801, #22714, #21064 ) ) ;
#22904=CARTESIAN_POINT ( 'NONE',  ( 5.871322893124551356, -8.081182679343980269, 3.759589141758144404 ) ) ;
#22909=CARTESIAN_POINT ( 'NONE',  ( 8.680847955711199049, -2.820578480813074496, -6.533165578109188409 ) ) ;
#22914=CARTESIAN_POINT ( 'NONE',  ( 7.022953521755574080, -5.102474405759714671, 12.43316557810918788 ) ) ;
#22922=CARTESIAN_POINT ( 'NONE',  ( 9.500000000000000000, 6.470877716354879437E-13, -10.05958914175814378 ) ) ;
#22925=CARTESIAN_POINT ( 'NONE',  ( 2.935661446562616295, -9.035036904803758873, 6.806742014460233747 ) ) ;
#22937=CARTESIAN_POINT ( 'NONE',  ( -5.365059087799947335, 7.384370330706355290, -7.333165578109188232 ) ) ;
#22943=CARTESIAN_POINT ( 'NONE',  ( -2.935661446561384391, -9.035036904804158553, 12.60674201446023446 ) ) ;
#22952=( BOUNDED_CURVE ( )  B_SPLINE_CURVE ( 2, ( #2988, #21770, #7232, #21880, #3337, #3097, #20179, #10519, #1271, #3458, #10760 ),
 .UNSPECIFIED., .F., .T. ) 
 B_SPLINE_CURVE_WITH_KNOTS ( ( 3, 2, 2, 2, 2, 3 ),
 ( 0.3000000000000000999, 0.3200000000000001177, 0.3400000000000000799, 0.3600000000000000422, 0.3800000000000000044, 0.4000000000000000222 ),
 .UNSPECIFIED. ) 
 CURVE ( )  GEOMETRIC_REPRESENTATION_ITEM ( )  RATIONAL_B_SPLINE_CURVE ( ( 0.9999999999999997780, 0.9510565162951537532, 1.000000000000000000, 0.9510565162951535312, 1.000000000000000000, 0.9510565162951535312, 1.000000000000000000, 0.9510565162951535312, 1.000000000000000000, 0.9510565162951535312, 1.000000000000000000 ) ) 
 REPRESENTATION_ITEM ( '' )  );
#22957=CARTESIAN_POINT ( 'NONE',  ( 0.2186765406003783607, -9.110087292425127714, 12.42023503934770901 ) ) ;
#22962=CARTESIAN_POINT ( 'NONE',  ( 9.500000000000000000, 1.163414459189985485E-15, 12.50000000000000000 ) ) ;
#22966=CARTESIAN_POINT ( 'NONE',  ( -6.153822176767817416E-13, 9.500000000000000000, -3.706742014460232326 ) ) ;
#22970=CARTESIAN_POINT ( 'NONE',  ( 8.680847955711199049, -2.820578480813074496, 6.533165578109188409 ) ) ;
#22978=CARTESIAN_POINT ( 'NONE',  ( 9.500000000000209610, -3.086737114211962396, -13.10674201446023091 ) ) ;
#22984=CARTESIAN_POINT ( 'NONE',  ( -9.122155368748954274, -2.709684805614216430, -3.500412170903221654 ) ) ;
#22997=CARTESIAN_POINT ( 'NONE',  ( 5.871322893123449127, 8.081182679344781405, 8.359589141758144493 ) ) ;
#22998=VERTEX_POINT ( 'NONE', #1607 ) ;
#23004=CARTESIAN_POINT ( 'NONE',  ( 8.680847955711199049, -2.820578480813074496, -6.533165578109188409 ) ) ;
#23005=CARTESIAN_POINT ( 'NONE',  ( -7.685661446562381371, 5.583959896777970222, 8.006742014460233037 ) ) ;
#23010=CARTESIAN_POINT ( 'NONE',  ( 3.934052222107095265, -8.094642247421083070, 12.50000000000000000 ) ) ;
#23020=CARTESIAN_POINT ( 'NONE',  ( -7.022953521755574080, 5.102474405759713783, -5.433165578109188765 ) ) ;
#23024=CARTESIAN_POINT ( 'NONE',  ( -8.680847955710813579, -2.820578480814258437, 9.733165578109186811 ) ) ;
#23034=CARTESIAN_POINT ( 'NONE',  ( -1.504652183083727168, 9.499999999999904077, 3.757996296007079184 ) ) ;
#23039=CARTESIAN_POINT ( 'NONE',  ( 0.000000000000000000, 0.000000000000000000, 12.50000000000000000 ) ) ;
#23049=CARTESIAN_POINT ( 'NONE',  ( -5.365059087798939252, -7.384370330707086261, -5.933165578109187877 ) ) ;
#23052=CARTESIAN_POINT ( 'NONE',  ( 6.809999908187194197E-13, -9.988891130263535700, 11.55958914175814201 ) ) ;
#23055=CARTESIAN_POINT ( 'NONE',  ( 5.365059087799946447, -7.384370330706356178, -12.33316557810918646 ) ) ;
#23059=CARTESIAN_POINT ( 'NONE',  ( 7.121611749575429862, -5.132745777193602699, -12.49999999999999289 ) ) ;
#23063=CARTESIAN_POINT ( 'NONE',  ( 9.500000000000000000, 6.470877716354879437E-13, -4.059589141758143782 ) ) ;
#23070=DIRECTION ( 'NONE',  ( 0.000000000000000000, 0.000000000000000000, 1.000000000000000000 ) ) ;
#23077=CARTESIAN_POINT ( 'NONE',  ( 5.871322893124553133, -8.081182679343980269, -4.906742014460232504 ) ) ;
#23082=CARTESIAN_POINT ( 'NONE',  ( -7.022953521755574080, 5.102474405759713783, 7.433165578109188765 ) ) ;
#23093=CARTESIAN_POINT ( 'NONE',  ( -5.871322893123450015, -8.081182679344781405, -12.50674201446023481 ) ) ;
#23098=EDGE_CURVE ( 'NONE', #17902, #3993, #14118, .T. ) ;
#23117=CARTESIAN_POINT ( 'NONE',  ( -7.685661446561619314, -5.583959896779019161, 9.259589141758143072 ) ) ;
#23125=AXIS2_PLACEMENT_3D ( 'NONE', #13338, #3840, #22161 ) ;
#23128=EDGE_CURVE ( 'NONE', #17902, #4813, #20727, .T. ) ;
#23133=DIRECTION ( 'NONE',  ( 1.000000000000000000, 0.000000000000000000, 0.000000000000000000 ) ) ;
#23138=CARTESIAN_POINT ( 'NONE',  ( 9.500000000000000000, 6.470877716354879437E-13, -5.206742014460234103 ) ) ;
#23140=CYLINDRICAL_SURFACE ( 'NONE', #8929, 9.500000000000000000 ) ;
#23142=CARTESIAN_POINT ( 'NONE',  ( -2.935661446561384391, -9.035036904804158553, 7.459589141758144137 ) ) ;
#23145=CARTESIAN_POINT ( 'NONE',  ( -9.500000000000000000, -6.482511860946779655E-13, 5.059589141758143782 ) ) ;
#23153=CARTESIAN_POINT ( 'NONE',  ( 6.222797240145152671E-13, -9.127583699786111282, -10.13316557810918894 ) ) ;
#23157=ORIENTED_EDGE ( 'NONE', *, *, #317, .F. ) ;
#23172=CARTESIAN_POINT ( 'NONE',  ( -1.749335460929532182, -9.337549220493269075, 3.500000000000028866 ) ) ;
#23180=CARTESIAN_POINT ( 'NONE',  ( 2.682529543900284974, -8.255977015246234174, -4.233165578109187699 ) ) ;
#23184=CARTESIAN_POINT ( 'NONE',  ( 2.935661446562616295, -9.035036904803758873, 7.659589141758144315 ) ) ;
#23185=CARTESIAN_POINT ( 'NONE',  ( 5.871322893123449127, 8.081182679344781405, 11.50674201446023126 ) ) ;
#23204=CARTESIAN_POINT ( 'NONE',  ( -5.618740543780279317, -7.334895587232010072, 12.29317507175855795 ) ) ;
#23216=EDGE_CURVE ( 'NONE', #17583, #17352, #4928, .T. ) ;
#23217=CARTESIAN_POINT ( 'NONE',  ( -7.685661446561619314, -5.583959896779019161, -6.406742014460233392 ) ) ;
#23220=CARTESIAN_POINT ( 'NONE',  ( 5.365059087798939252, 7.384370330707087149, 8.933165578109187877 ) ) ;
#23221=DIRECTION ( 'NONE',  ( -0.000000000000000000, -0.000000000000000000, 1.000000000000000000 ) ) ;
#23235=CARTESIAN_POINT ( 'NONE',  ( -9.499999999999790390, -3.086737114213257804, -8.306742014460233747 ) ) ;
#23238=CARTESIAN_POINT ( 'NONE',  ( -2.089646679935818430, -8.893998220852614267, -12.37209986270935502 ) ) ;
#23243=VECTOR ( 'NONE', #12506, 1000.000000000000227 ) ;
#23256=CARTESIAN_POINT ( 'NONE',  ( -7.685661446561619314, -5.583959896779019161, 5.259589141758143960 ) ) ;
#23259=EDGE_CURVE ( 'NONE', #12845, #21315, #15453, .T. ) ;
#23263=CARTESIAN_POINT ( 'NONE',  ( -1.374911245008260563, 8.680847955710920161, -3.184419859656034024 ) ) ;
#23282=EDGE_CURVE ( 'NONE', #23301, #14197, #18156, .T. ) ;
#23283=CARTESIAN_POINT ( 'NONE',  ( -5.365059087799948223, 7.384370330706355290, -5.333165578109190008 ) ) ;
#23288=CARTESIAN_POINT ( 'NONE',  ( -5.365059087799947335, 7.384370330706355290, 9.333165578109190008 ) ) ;
#23295=CARTESIAN_POINT ( 'NONE',  ( 6.809999908187194197E-13, -9.988891130263535700, -11.55958914175814201 ) ) ;
#23299=CARTESIAN_POINT ( 'NONE',  ( 9.500000000000000000, 1.163414459189985485E-15, 12.50000000000000000 ) ) ;
#23301=VERTEX_POINT ( 'NONE', #10801 ) ;
#23303=FACE_OUTER_BOUND ( 'NONE', #15142, .T. ) ;
#23305=CARTESIAN_POINT ( 'NONE',  ( 0.000000000000000000, 0.000000000000000000, -12.00000000000000000 ) ) ;
#23315=CARTESIAN_POINT ( 'NONE',  ( -9.499999999999790390, -3.086737114213257804, 3.159589141758143871 ) ) ;
#23316=CARTESIAN_POINT ( 'NONE',  ( -7.685661446561619314, -5.583959896779019161, 10.40674201446023339 ) ) ;
#23326=CARTESIAN_POINT ( 'NONE',  ( -10.49999999999999822, 1.285879139104720633E-15, -2.499999999999999556 ) ) ;
#23328=DIRECTION ( 'NONE',  ( -0.000000000000000000, -0.000000000000000000, -1.000000000000000000 ) ) ;
#23335=CARTESIAN_POINT ( 'NONE',  ( 9.366788983124319401, -0.5939584231417279758, -12.13321101687572146 ) ) ;
#23337=AXIS2_PLACEMENT_3D ( 'NONE', #7792, #1122, #1238 ) ;
#23355=CARTESIAN_POINT ( 'NONE',  ( -7.685661446562381371, 5.583959896777970222, -10.85958914175814449 ) ) ;
#23366=ADVANCED_FACE ( 'NONE', ( #21923 ), #1554, .F. ) ;
#23376=CARTESIAN_POINT ( 'NONE',  ( 2.935661446562616295, -9.035036904803758873, 9.659589141758143427 ) ) ;
#23378=AXIS2_PLACEMENT_3D ( 'NONE', #19733, #5317, #14696 ) ;
#23379=ORIENTED_EDGE ( 'NONE', *, *, #677, .F. ) ;
#23386=FACE_OUTER_BOUND ( 'NONE', #547, .T. ) ;
#23390=CARTESIAN_POINT ( 'NONE',  ( 9.500000000000209610, -3.086737114211962396, 5.106742014460234458 ) ) ;
#23393=EDGE_CURVE ( 'NONE', #8141, #21315, #19835, .T. ) ;
#23397=( BOUNDED_CURVE ( )  B_SPLINE_CURVE ( 2, ( #18549, #12546, #5254, #14501, #21967, #12680, #20150, #9255, #18305, #20020, #9011 ),
 .UNSPECIFIED., .F., .T. ) 
 B_SPLINE_CURVE_WITH_KNOTS ( ( 3, 2, 2, 2, 2, 3 ),
 ( 0.006042316813506577906, 0.01999999999999999001, 0.03999999999999997308, 0.05999999999999994921, 0.07999999999999993228, 0.09999999999999992228 ),
 .UNSPECIFIED. ) 
 CURVE ( )  GEOMETRIC_REPRESENTATION_ITEM ( )  RATIONAL_B_SPLINE_CURVE ( ( 0.9793613297716632360, 0.9658431180202224908, 1.000000000000000000, 0.9510565162951535312, 1.000000000000000000, 0.9510565162951535312, 1.000000000000000000, 0.9510565162951535312, 1.000000000000000000, 0.9510565162951537532, 0.9999999999999997780 ) ) 
 REPRESENTATION_ITEM ( '' )  );
#23399=DIRECTION ( 'NONE',  ( -0.7071067811865439090, 0.000000000000000000, -0.7071067811865512365 ) ) ;
#23400=CARTESIAN_POINT ( 'NONE',  ( -7.022953521755574080, 5.102474405759713783, -7.433165578109188765 ) ) ;
#23409=CARTESIAN_POINT ( 'NONE',  ( -9.499999999999790390, -3.086737114213257804, -5.159589141758141650 ) ) ;
#23417=CARTESIAN_POINT ( 'NONE',  ( 9.500000000000000000, 6.470877716354879437E-13, -11.20674201446023410 ) ) ;
#23424=CARTESIAN_POINT ( 'NONE',  ( -8.680847955710813579, -2.820578480814258437, -3.733165578109188587 ) ) ;
#23428=CARTESIAN_POINT ( 'NONE',  ( 7.685661446561619314, 5.583959896779020049, 4.259589141758143960 ) ) ;
#23429=CARTESIAN_POINT ( 'NONE',  ( -9.500000000000211386, 3.086737114211961064, 10.10674201446023446 ) ) ;
#23446=CARTESIAN_POINT ( 'NONE',  ( 2.935661446561383503, 9.035036904804158553, 10.45958914175814414 ) ) ;
#23447=CARTESIAN_POINT ( 'NONE',  ( -9.500000000000000000, -6.482511860946779655E-13, -10.20674201446023233 ) ) ;
#23452=CARTESIAN_POINT ( 'NONE',  ( 9.500000000000000000, 6.470877716354879437E-13, 4.059589141758143782 ) ) ;
#23453=ORIENTED_EDGE ( 'NONE', *, *, #10125, .T. ) ;
#23456=SHAPE_REPRESENTATION ( 'Nipple', ( #8005 ), #10756 ) ;
#23458=CIRCLE ( 'NONE', #3563, 9.000000000000001776 ) ;
#23476=CARTESIAN_POINT ( 'NONE',  ( 6.250000000000000000, 10.82531754730548279, -2.500000000000000000 ) ) ;
#23482=CARTESIAN_POINT ( 'NONE',  ( -7.685661446562381371, 5.583959896777970222, 8.859589141758144493 ) ) ;
#23484=ADVANCED_FACE ( 'NONE', ( #20822 ), #2266, .T. ) ;
#23486=VERTEX_POINT ( 'NONE', #11261 ) ;
#23492=EDGE_CURVE ( 'NONE', #1372, #18218, #9686, .T. ) ;
#23507=CARTESIAN_POINT ( 'NONE',  ( 9.500000000000000000, 1.163414459189985485E-15, -12.00000000000000000 ) ) ;
#23508=CARTESIAN_POINT ( 'NONE',  ( -8.680847955711007202, -5.923547351154968927E-13, -3.633165578109188054 ) ) ;
#23516=CARTESIAN_POINT ( 'NONE',  ( -5.365059087798939252, -7.384370330707086261, 5.933165578109187877 ) ) ;
#23524=CARTESIAN_POINT ( 'NONE',  ( 5.871322893123449127, 8.081182679344781405, -6.359589141758142716 ) ) ;
#23527=DIRECTION ( 'NONE',  ( -0.8660254037844387076, 0.4999999999999999445, 0.000000000000000000 ) ) ;
#23533=AXIS2_PLACEMENT_3D ( 'NONE', #15662, #19720, #23133 ) ;
#23545=CARTESIAN_POINT ( 'NONE',  ( 5.871322893123449127, 8.081182679344781405, 4.359589141758143604 ) ) ;
#23546=CARTESIAN_POINT ( 'NONE',  ( 9.499999999999790390, 3.086737114213260025, 7.306742014460234635 ) ) ;
#23561=CARTESIAN_POINT ( 'NONE',  ( -12.50000000000000178, 1.672973214995343413E-15, -2.500000000000000000 ) ) ;
#23568=CARTESIAN_POINT ( 'NONE',  ( -7.725160277709925083, 5.537733574950152615, -3.500137086806215603 ) ) ;
#23576=DIRECTION ( 'NONE',  ( 0.000000000000000000, 0.000000000000000000, 1.000000000000000000 ) ) ;
#23581=EDGE_CURVE ( 'NONE', #9768, #14927, #20944, .T. ) ;
#23582=CARTESIAN_POINT ( 'NONE',  ( -5.622572944242077574E-13, 8.680847955711007202, 3.133165578109187610 ) ) ;
#23594=CARTESIAN_POINT ( 'NONE',  ( -2.935661446561384391, -9.035036904804158553, -4.606742014460233570 ) ) ;
#23603=EDGE_CURVE ( 'NONE', #5195, #14197, #4225, .T. ) ;
#23606=( BOUNDED_SURFACE ( )  B_SPLINE_SURFACE ( 1, 2, ( 
 ( #12024, #15568, #21449, #1086, #12147, #23295, #10330, #19497, #21203, #19256, #2774, #6305, #15323, #6078, #20964, #2405, #4249, #589, #8008, #17418, #22922, #13753, #13629, #10556, #8963, #1551, #19974, #10451, #23758, #1317, #3134, #6806, #20220, #18021, #22056, #5203, #5333, #3491, #17911, #10681, #14345, #4868, #1197, #1450, #23652, #21806, #18152, #10904, #12503, #3032, #21576, #14232, #5087, #18374, #23868, #8860, #3254, #23524, #12280, #8741, #16193, #12757, #21694, #3379, #8505, #16299, #7028, #19753, #15947, #23409, #14585, #7149, #4987, #6683, #6924, #8611, #14115, #12635, #16060, #14456, #12400, #21921, #20103, #19862, #10798, #18263, #16411, #18622, #22173, #14935, #5915, #9433, #5802, #13354, #22410, #20446, #15164 ),
 ( #22280, #18730, #16541, #3737, #9565, #20816, #206, #9094, #18859, #13118, #5447, #13228, #12866, #16891, #2140, #23992, #22634, #17017, #7610, #7732, #1788, #322, #4102, #11258, #16664, #2008, #12991, #16763, #7274, #14712, #11516, #5693, #11148, #5558, #1903, #3606, #20575, #20325, #9217, #1669, #9319, #11028, #80, #7485, #18502, #11381, #20536, #7378, #14815, #3852, #15059, #22528, #20682, #3965, #13601, #6164, #17132, #19355, #15537, #11745, #21046, #23004, #19101, #11996, #2374, #17614, #2262, #7979, #2507, #21169, #4473, #4595, #19224, #21302, #13718, #686, #8348, #19467, #17389, #2631, #11630, #4220, #4336, #2744, #10159, #20940, #9928, #21417, #8093, #923, #6275, #558, #15426, #9791, #11884, #23263, #22765 ) ),
 .UNSPECIFIED., .F., .F., .T. ) 
 B_SPLINE_SURFACE_WITH_KNOTS ( ( 2, 2 ),
 ( 3, 2, 2, 2, 2, 2, 2, 2, 2, 2, 2, 2, 2, 2, 2, 2, 2, 2, 2, 2, 2, 2, 2, 2, 2, 2, 2, 2, 2, 2, 2, 2, 2, 2, 2, 2, 2, 2, 2, 2, 2, 2, 2, 2, 2, 2, 2, 2, 3 ),
 ( 0.000000000000000000, 1.000000000000000000 ),
 ( 0.000000000000000000, 0.02000000000000000042, 0.04000000000000000083, 0.05999999999999999778, 0.08000000000000000167, 0.1000000000000000056, 0.1199999999999999956, 0.1400000000000000133, 0.1600000000000000033, 0.1799999999999999933, 0.2000000000000000111, 0.2200000000000000011, 0.2399999999999999911, 0.2600000000000000089, 0.2800000000000000266, 0.2999999999999999889, 0.3200000000000000067, 0.3400000000000000244, 0.3599999999999999867, 0.3800000000000000044, 0.4000000000000000222, 0.4199999999999999845, 0.4400000000000000022, 0.4600000000000000200, 0.4799999999999999822, 0.5000000000000000000, 0.5200000000000000178, 0.5400000000000000355, 0.5600000000000000533, 0.5799999999999999600, 0.5999999999999999778, 0.6199999999999999956, 0.6400000000000000133, 0.6600000000000000311, 0.6800000000000000488, 0.6999999999999999556, 0.7199999999999999734, 0.7399999999999999911, 0.7600000000000000089, 0.7800000000000000266, 0.8000000000000000444, 0.8199999999999999512, 0.8399999999999999689, 0.8599999999999999867, 0.8800000000000000044, 0.9000000000000000222, 0.9200000000000000400, 0.9399999999999999467, 0.9500000000000000666 ),
 .UNSPECIFIED. ) 
 GEOMETRIC_REPRESENTATION_ITEM ( )  RATIONAL_B_SPLINE_SURFACE ( (
 ( 1.000000000000000000, 0.9510565162951535312, 1.000000000000000000, 0.9510565162951535312, 1.000000000000000000, 0.9510565162951535312, 1.000000000000000000, 0.9510565162951535312, 1.000000000000000000, 0.9510565162951535312, 1.000000000000000000, 0.9510565162951535312, 1.000000000000000000, 0.9510565162951535312, 1.000000000000000000, 0.9510565162951535312, 1.000000000000000000, 0.9510565162951535312, 1.000000000000000000, 0.9510565162951535312, 1.000000000000000000, 0.9510565162951535312, 1.000000000000000000, 0.9510565162951535312, 1.000000000000000000, 0.9510565162951535312, 1.000000000000000000, 0.9510565162951535312, 1.000000000000000000, 0.9510565162951535312, 1.000000000000000000, 0.9510565162951535312, 1.000000000000000000, 0.9510565162951535312, 1.000000000000000000, 0.9510565162951535312, 1.000000000000000000, 0.9510565162951535312, 1.000000000000000000, 0.9510565162951535312, 1.000000000000000000, 0.9510565162951535312, 1.000000000000000000, 0.9510565162951535312, 1.000000000000000000, 0.9510565162951535312, 1.000000000000000000, 0.9510565162951535312, 1.000000000000000000, 0.9510565162951535312, 1.000000000000000000, 0.9510565162951535312, 1.000000000000000000, 0.9510565162951535312, 1.000000000000000000, 0.9510565162951535312, 1.000000000000000000, 0.9510565162951535312, 1.000000000000000000, 0.9510565162951535312, 1.000000000000000000, 0.9510565162951535312, 1.000000000000000000, 0.9510565162951535312, 1.000000000000000000, 0.9510565162951535312, 1.000000000000000000, 0.9510565162951535312, 1.000000000000000000, 0.9510565162951535312, 1.000000000000000000, 0.9510565162951535312, 1.000000000000000000, 0.9510565162951535312, 1.000000000000000000, 0.9510565162951535312, 1.000000000000000000, 0.9510565162951535312, 1.000000000000000000, 0.9510565162951535312, 1.000000000000000000, 0.9510565162951535312, 1.000000000000000000, 0.9510565162951535312, 1.000000000000000000, 0.9510565162951535312, 1.000000000000000000, 0.9510565162951535312, 1.000000000000000000, 0.9510565162951535312, 1.000000000000000000, 0.9510565162951535312, 1.000000000000000000, 0.9510565162951535312, 1.000000000000000000, 0.9755282581475764880, 0.9755282581475768211),
 ( 1.000000000000000000, 0.9510565162951535312, 1.000000000000000000, 0.9510565162951535312, 1.000000000000000000, 0.9510565162951535312, 1.000000000000000000, 0.9510565162951535312, 1.000000000000000000, 0.9510565162951535312, 1.000000000000000000, 0.9510565162951535312, 1.000000000000000000, 0.9510565162951535312, 1.000000000000000000, 0.9510565162951535312, 1.000000000000000000, 0.9510565162951535312, 1.000000000000000000, 0.9510565162951535312, 1.000000000000000000, 0.9510565162951535312, 1.000000000000000000, 0.9510565162951535312, 1.000000000000000000, 0.9510565162951535312, 1.000000000000000000, 0.9510565162951535312, 1.000000000000000000, 0.9510565162951535312, 1.000000000000000000, 0.9510565162951535312, 1.000000000000000000, 0.9510565162951535312, 1.000000000000000000, 0.9510565162951535312, 1.000000000000000000, 0.9510565162951535312, 1.000000000000000000, 0.9510565162951535312, 1.000000000000000000, 0.9510565162951535312, 1.000000000000000000, 0.9510565162951535312, 1.000000000000000000, 0.9510565162951535312, 1.000000000000000000, 0.9510565162951535312, 1.000000000000000000, 0.9510565162951535312, 1.000000000000000000, 0.9510565162951535312, 1.000000000000000000, 0.9510565162951535312, 1.000000000000000000, 0.9510565162951535312, 1.000000000000000000, 0.9510565162951535312, 1.000000000000000000, 0.9510565162951535312, 1.000000000000000000, 0.9510565162951535312, 1.000000000000000000, 0.9510565162951535312, 1.000000000000000000, 0.9510565162951535312, 1.000000000000000000, 0.9510565162951535312, 1.000000000000000000, 0.9510565162951535312, 1.000000000000000000, 0.9510565162951535312, 1.000000000000000000, 0.9510565162951535312, 1.000000000000000000, 0.9510565162951535312, 1.000000000000000000, 0.9510565162951535312, 1.000000000000000000, 0.9510565162951535312, 1.000000000000000000, 0.9510565162951535312, 1.000000000000000000, 0.9510565162951535312, 1.000000000000000000, 0.9510565162951535312, 1.000000000000000000, 0.9510565162951535312, 1.000000000000000000, 0.9510565162951535312, 1.000000000000000000, 0.9510565162951535312, 1.000000000000000000, 0.9510565162951535312, 1.000000000000000000, 0.9755282581475764880, 0.9755282581475768211) ) ) 
 REPRESENTATION_ITEM ( '' )  SURFACE ( )  );
#23612=CARTESIAN_POINT ( 'NONE',  ( 9.500000000000000000, 6.470877716354879437E-13, -7.206742014460234103 ) ) ;
#23621=ORIENTED_EDGE ( 'NONE', *, *, #5462, .F. ) ;
#23636=CARTESIAN_POINT ( 'NONE',  ( 2.935661446561383503, 9.035036904804158553, 4.459589141758144137 ) ) ;
#23646=CARTESIAN_POINT ( 'NONE',  ( -5.365059087798939252, -7.384370330707086261, 3.933165578109188321 ) ) ;
#23652=CARTESIAN_POINT ( 'NONE',  ( 2.935661446562616295, -9.035036904803758873, -7.659589141758144315 ) ) ;
#23656=CARTESIAN_POINT ( 'NONE',  ( -6.153822176767817416E-13, 9.500000000000000000, 3.637828009640154736 ) ) ;
#23665=CARTESIAN_POINT ( 'NONE',  ( 0.000000000000000000, 0.000000000000000000, -2.500000000000000000 ) ) ;
#23676=CARTESIAN_POINT ( 'NONE',  ( -9.499999999999790390, -3.086737114213257804, 12.30674201446023197 ) ) ;
#23690=CARTESIAN_POINT ( 'NONE',  ( -4.199395741333246335, 8.543843702856307232, -3.498976002706156496 ) ) ;
#23695=CARTESIAN_POINT ( 'NONE',  ( 8.680847955711007202, 5.912916378492122225E-13, -10.63316557810918894 ) ) ;
#23696=EDGE_CURVE ( 'NONE', #16661, #14137, #13305, .T. ) ;
#23709=CARTESIAN_POINT ( 'NONE',  ( 9.499999999999790390, 3.086737114213260025, -5.306742014460231971 ) ) ;
#23710=VERTEX_POINT ( 'NONE', #15017 ) ;
#23713=DIRECTION ( 'NONE',  ( 0.000000000000000000, 0.000000000000000000, 1.000000000000000000 ) ) ;
#23718=CARTESIAN_POINT ( 'NONE',  ( -1.749335460928132413, -9.337549220493531976, -3.500000000000076383 ) ) ;
#23724=CARTESIAN_POINT ( 'NONE',  ( 9.500000000000209610, -3.086737114211962396, 3.959589141758145026 ) ) ;
#23728=B_SPLINE_CURVE_WITH_KNOTS ( 'NONE', 3,
 ( #5726, #828, #13756, #594, #7761, #21205, #6082, #9710, #2541, #15195, #17290, #11658, #19129, #11551 ),
 .UNSPECIFIED., .F., .F.,
 ( 4, 2, 2, 2, 2, 2, 4 ),
 ( 4.128177188600459851E-16, 0.001553140985941505034, 0.002329711478912049709, 0.003106281971882594601, 0.004659422957823682217, 0.005435993450794225808, 0.006212563943764767664 ),
 .UNSPECIFIED. ) ;
#23744=CARTESIAN_POINT ( 'NONE',  ( -1.504652183083727168, 9.499999999999904077, 3.757996296007079184 ) ) ;
#23752=CARTESIAN_POINT ( 'NONE',  ( 2.682529543900284974, -8.255977015246234174, 10.23316557810918859 ) ) ;
#23754=PRODUCT_CONTEXT ( 'NONE', #3548, 'mechanical' ) ;
#23757=CARTESIAN_POINT ( 'NONE',  ( -9.209619485559194629, 2.039334951465706869, -12.08108701042788979 ) ) ;
#23758=CARTESIAN_POINT ( 'NONE',  ( -7.685661446561619314, -5.583959896779019161, -9.259589141758143072 ) ) ;
#23763=ADVANCED_FACE ( 'NONE', ( #22601 ), #18593, .T. ) ;
#23774=ORIENTED_EDGE ( 'NONE', *, *, #5470, .T. ) ;
#23776=CARTESIAN_POINT ( 'NONE',  ( -5.871322893124554021, 8.081182679343978492, 9.906742014460235168 ) ) ;
#23777=CARTESIAN_POINT ( 'NONE',  ( -9.500000000000211386, 3.086737114211961064, 6.106742014460234458 ) ) ;
#23784=CARTESIAN_POINT ( 'NONE',  ( 2.935661446562616295, -9.035036904803758873, -4.806742014460232859 ) ) ;
#23786=LINE ( 'NONE', #10719, #10975 ) ;
#23793=CARTESIAN_POINT ( 'NONE',  ( -12.50000000000000178, 1.672973214995343413E-15, 2.500000000000000000 ) ) ;
#23795=CARTESIAN_POINT ( 'NONE',  ( -6.153822176767817416E-13, 9.500000000000000000, -3.500000000000014211 ) ) ;
#23799=CARTESIAN_POINT ( 'NONE',  ( 7.022953521755574080, -5.102474405759714671, -8.433165578109187877 ) ) ;
#23806=ORIENTED_EDGE ( 'NONE', *, *, #166, .T. ) ;
#23809=CARTESIAN_POINT ( 'NONE',  ( -7.685661446562381371, 5.583959896777970222, -2.859589141758144493 ) ) ;
#23815=CARTESIAN_POINT ( 'NONE',  ( -2.935661446562617183, 9.035036904803758873, -5.806742014460233747 ) ) ;
#23831=ORIENTED_EDGE ( 'NONE', *, *, #1808, .T. ) ;
#23847=CARTESIAN_POINT ( 'NONE',  ( 6.809999908187194197E-13, -9.988891130263535700, 10.70674201446023410 ) ) ;
#23848=DIRECTION ( 'NONE',  ( -0.000000000000000000, -0.000000000000000000, -1.000000000000000000 ) ) ;
#23852=CARTESIAN_POINT ( 'NONE',  ( -7.022953521754877748, -5.102474405760673015, 9.833165578109188232 ) ) ;
#23867=CARTESIAN_POINT ( 'NONE',  ( -9.355838966532735057, 1.029750461815885476, -12.10148668281140871 ) ) ;
#23868=CARTESIAN_POINT ( 'NONE',  ( -2.935661446562617183, 9.035036904803758873, -6.659589141758144315 ) ) ;
#23869=( BOUNDED_CURVE ( )  B_SPLINE_CURVE ( 2, ( #3997, #7873, #6197, #11418, #22800, #19385, #17531, #19259, #20713, #6306, #15697 ),
 .UNSPECIFIED., .F., .T. ) 
 B_SPLINE_CURVE_WITH_KNOTS ( ( 3, 2, 2, 2, 2, 3 ),
 ( 0.2000000000000000111, 0.2200000000000000289, 0.2400000000000000466, 0.2600000000000000644, 0.2800000000000001377, 0.3000000000000000999 ),
 .UNSPECIFIED. ) 
 CURVE ( )  GEOMETRIC_REPRESENTATION_ITEM ( )  RATIONAL_B_SPLINE_CURVE ( ( 1.000000000000000000, 0.9510565162951535312, 1.000000000000000000, 0.9510565162951535312, 1.000000000000000000, 0.9510565162951535312, 1.000000000000000000, 0.9510565162951535312, 1.000000000000000000, 0.9510565162951533091, 1.000000000000000222 ) ) 
 REPRESENTATION_ITEM ( '' )  );
#23872=CARTESIAN_POINT ( 'NONE',  ( -8.000000000000000000, 9.797174393178825657E-16, 12.50000000000000000 ) ) ;
#23875=CARTESIAN_POINT ( 'NONE',  ( 9.500000000000200728, -3.086737114211976607, -7.106742014460232681 ) ) ;
#23876=VECTOR ( 'NONE', #17800, 1000.000000000000000 ) ;
#23889=CARTESIAN_POINT ( 'NONE',  ( -2.935661446561384391, -9.035036904804158553, -10.60674201446023446 ) ) ;
#23895=CARTESIAN_POINT ( 'NONE',  ( -2.935661446562617183, 9.035036904803758873, 11.80674201446023375 ) ) ;
#23897=CARTESIAN_POINT ( 'NONE',  ( -7.685661446561619314, -5.583959896779019161, 6.406742014460233392 ) ) ;
#23928=CARTESIAN_POINT ( 'NONE',  ( 9.500000000000209610, -3.086737114211962396, -9.959589141758144137 ) ) ;
#23941=CARTESIAN_POINT ( 'NONE',  ( 9.499999999999790390, 3.086737114213260025, -10.15958914175814520 ) ) ;
#23954=CARTESIAN_POINT ( 'NONE',  ( -6.153822176767817416E-13, 9.500000000000000000, -2.873059427838766222 ) ) ;
#23962=ORIENTED_EDGE ( 'NONE', *, *, #15659, .T. ) ;
#23964=EDGE_LOOP ( 'NONE', ( #8317, #21926, #16862, #3683 ) ) ;
#23973=CARTESIAN_POINT ( 'NONE',  ( -7.866007474251193621, 5.334205555521198683, 12.00988687156538148 ) ) ;
#23984=ADVANCED_FACE ( 'NONE', ( #10124 ), #17576, .F. ) ;
#23985=CARTESIAN_POINT ( 'NONE',  ( -5.365059087798939252, -7.384370330707086261, 11.93316557810918965 ) ) ;
#23992=CARTESIAN_POINT ( 'NONE',  ( -6.233975306307046963E-13, 9.127583699786111282, -11.13316557810918894 ) ) ;
#24004=EDGE_CURVE ( 'NONE', #3425, #10554, #17960, .T. ) ;
#24012=VECTOR ( 'NONE', #11388, 1000.000000000000000 ) ;
#24018=CARTESIAN_POINT ( 'NONE',  ( -6.822232771736903637E-13, 9.988891130263535700, 7.706742014460232326 ) ) ;
#24024=CARTESIAN_POINT ( 'NONE',  ( 9.500000000000000000, 6.470877716354879437E-13, -5.206742014460234103 ) ) ;
#24027=DIRECTION ( 'NONE',  ( -1.000000000000000000, 0.000000000000000000, 0.000000000000000000 ) ) ;
#24029=VECTOR ( 'NONE', #4059, 1000.000000000000000 ) ;
#24042=LINE ( 'NONE', #16808, #2534 ) ;
#24044=CARTESIAN_POINT ( 'NONE',  ( -5.871322893123449127, -8.081182679344781405, -9.359589141758144493 ) ) ;
#24051=CARTESIAN_POINT ( 'NONE',  ( -5.871322893124554021, 8.081182679343978492, -4.759589141758144848 ) ) ;
#24073=CARTESIAN_POINT ( 'NONE',  ( -6.250000000000000888, 10.82531754730548279, 2.500000000000000000 ) ) ;
#24074=EDGE_CURVE ( 'NONE', #16852, #566, #11943, .T. ) ;
#24094=CARTESIAN_POINT ( 'NONE',  ( -8.680847955711007202, -5.923547351154968927E-13, 9.633165578109188942 ) ) ;
#24163=COLOUR_RGB('Off White',0.89,0.88,0.83);
#24164=FILL_AREA_STYLE_COLOUR('',#24163);
#24165=FILL_AREA_STYLE('',(#24164));
#24166=SURFACE_STYLE_FILL_AREA(#24165);
#24167=SURFACE_SIDE_STYLE('',(#24166));
#24168=SURFACE_STYLE_USAGE(.BOTH.,#24167);
#24169=PRESENTATION_STYLE_ASSIGNMENT((#24168));
ENDSEC;
END-ISO-10303-21;
